ISO-10303-21;
HEADER;
FILE_DESCRIPTION (('STEP AP214'),
    '1' );
FILE_NAME ('LINEAR ACTUATOR.step',
    '2026-10-09T16:01:55',
    ( '' ),
    ( '' ),
    'SwSTEP 2.0',
    'SolidWorks 2024',
    '' );
FILE_SCHEMA (( 'AUTOMOTIVE_DESIGN' ));
ENDSEC;

DATA;
#2=AXIS2_PLACEMENT_3D ( 'NONE', #65024, #57963, #9532 ) ;
#6=DIRECTION ( 'NONE',  ( -1.000000000000000000, 0.000000000000000000, 0.000000000000000000 ) ) ;
#11=LINE ( 'NONE', #65402, #38696 ) ;
#20=CARTESIAN_POINT ( 'NONE',  ( 7.000000000000000000, -26.50000000000000000, 9.080000000000000071 ) ) ;
#46=LINE ( 'NONE', #38894, #69673 ) ;
#55=LINE ( 'NONE', #58414, #51365 ) ;
#69=AXIS2_PLACEMENT_3D ( 'NONE', #9677, #37599, #64471 ) ;
#79=VECTOR ( 'NONE', #901, 1000.000000000000000 ) ;
#90=LINE ( 'NONE', #39288, #28849 ) ;
#94=LINE ( 'NONE', #53844, #47687 ) ;
#95=ORIENTED_EDGE ( 'NONE', *, *, #37069, .T. ) ;
#98=CARTESIAN_POINT ( 'NONE',  ( 275.0000000000000000, -0.5000000000000000000, -26.50000000000000000 ) ) ;
#116=VECTOR ( 'NONE', #2061, 1000.000000000000000 ) ;
#128=ORIENTED_EDGE ( 'NONE', *, *, #65488, .T. ) ;
#135=VERTEX_POINT ( 'NONE', #54425 ) ;
#138=DIRECTION ( 'NONE',  ( 1.000000000000000000, -0.000000000000000000, -0.000000000000000000 ) ) ;
#141=CARTESIAN_POINT ( 'NONE',  ( 275.0000000000000000, -21.00000000000000000, 12.50000000000000000 ) ) ;
#166=CARTESIAN_POINT ( 'NONE',  ( 275.2500000000000000, -42.25000000000000000, 26.75000000000000000 ) ) ;
#174=LINE ( 'NONE', #65556, #3686 ) ;
#179=ORIENTED_EDGE ( 'NONE', *, *, #39700, .T. ) ;
#186=ORIENTED_EDGE ( 'NONE', *, *, #14388, .F. ) ;
#187=VERTEX_POINT ( 'NONE', #23532 ) ;
#193=ORIENTED_EDGE ( 'NONE', *, *, #5564, .T. ) ;
#195=EDGE_CURVE ( 'NONE', #57192, #24019, #50407, .T. ) ;
#200=CARTESIAN_POINT ( 'NONE',  ( 7.000000000000000000, -42.00000000000000000, -7.000000000000000000 ) ) ;
#202=DIRECTION ( 'NONE',  ( -0.7071067811865480168, -0.7071067811865470176, 0.000000000000000000 ) ) ;
#204=CARTESIAN_POINT ( 'NONE',  ( 7.000000000000000000, -26.50000000000000000, -0.5000000000000000000 ) ) ;
#215=ORIENTED_EDGE ( 'NONE', *, *, #61304, .T. ) ;
#231=CARTESIAN_POINT ( 'NONE',  ( 0.000000000000000000, -42.00000000000000000, 26.50000000000000000 ) ) ;
#249=AXIS2_PLACEMENT_3D ( 'NONE', #24240, #50751, #62765 ) ;
#273=FACE_OUTER_BOUND ( 'NONE', #58305, .T. ) ;
#288=VERTEX_POINT ( 'NONE', #14671 ) ;
#306=ORIENTED_EDGE ( 'NONE', *, *, #47365, .T. ) ;
#308=VECTOR ( 'NONE', #40044, 1000.000000000000000 ) ;
#323=CARTESIAN_POINT ( 'NONE',  ( 275.5000000000000000, -42.50000000000000000, -30.09999999999999787 ) ) ;
#341=VERTEX_POINT ( 'NONE', #10421 ) ;
#344=CARTESIAN_POINT ( 'NONE',  ( 7.000000000000000000, -28.94999999999999929, -13.50000000000000000 ) ) ;
#378=DIRECTION ( 'NONE',  ( -1.000000000000000000, 0.000000000000000000, 0.000000000000000000 ) ) ;
#384=AXIS2_PLACEMENT_3D ( 'NONE', #58436, #19880, #25191 ) ;
#392=CARTESIAN_POINT ( 'NONE',  ( 7.000000000000000000, -20.40000000000000213, 12.40000000000000213 ) ) ;
#397=( LENGTH_UNIT ( ) NAMED_UNIT ( * ) SI_UNIT ( .MILLI., .METRE. ) );
#413=EDGE_CURVE ( 'NONE', #57464, #29889, #25280, .T. ) ;
#428=LINE ( 'NONE', #32247, #49859 ) ;
#439=EDGE_LOOP ( 'NONE', ( #63217, #45203, #8235, #44713 ) ) ;
#460=ADVANCED_FACE ( 'NONE', ( #5816 ), #59558, .F. ) ;
#466=DIRECTION ( 'NONE',  ( 0.000000000000000000, 0.000000000000000000, 1.000000000000000000 ) ) ;
#489=CARTESIAN_POINT ( 'NONE',  ( 283.0000000000000568, -23.70411739045900390, 12.50000000000000000 ) ) ;
#496=ORIENTED_EDGE ( 'NONE', *, *, #56762, .T. ) ;
#513=DIRECTION ( 'NONE',  ( 0.000000000000000000, 0.000000000000000000, -1.000000000000000000 ) ) ;
#520=VERTEX_POINT ( 'NONE', #38678 ) ;
#546=ORIENTED_EDGE ( 'NONE', *, *, #54338, .T. ) ;
#578=DIRECTION ( 'NONE',  ( 0.000000000000000000, 0.000000000000000000, 1.000000000000000000 ) ) ;
#581=CYLINDRICAL_SURFACE ( 'NONE', #36803, 8.000000000000000000 ) ;
#586=EDGE_CURVE ( 'NONE', #18944, #24350, #18136, .T. ) ;
#596=VERTEX_POINT ( 'NONE', #12818 ) ;
#598=CARTESIAN_POINT ( 'NONE',  ( 7.000000000000000000, -42.50000000000000000, 9.950000000000001066 ) ) ;
#605=CARTESIAN_POINT ( 'NONE',  ( 14.50000000000000000, -42.50000000000000000, 26.50000000000000000 ) ) ;
#634=DIRECTION ( 'NONE',  ( 0.000000000000000000, 0.000000000000000000, -1.000000000000000000 ) ) ;
#666=DIRECTION ( 'NONE',  ( 1.000000000000000000, 0.000000000000000000, 0.000000000000000000 ) ) ;
#677=AXIS2_PLACEMENT_3D ( 'NONE', #17605, #24303, #7681 ) ;
#681=CARTESIAN_POINT ( 'NONE',  ( 7.000000000000000000, -30.80000000000000071, -12.20000000000000107 ) ) ;
#710=ORIENTED_EDGE ( 'NONE', *, *, #11155, .T. ) ;
#712=LINE ( 'NONE', #9935, #52492 ) ;
#726=DIRECTION ( 'NONE',  ( -1.000000000000000000, 0.000000000000000000, 0.000000000000000000 ) ) ;
#731=VECTOR ( 'NONE', #46911, 1000.000000000000000 ) ;
#745=LINE ( 'NONE', #59085, #36041 ) ;
#747=CARTESIAN_POINT ( 'NONE',  ( 15.00000000000000000, -20.40000000000000213, -12.40000000000000213 ) ) ;
#749=VERTEX_POINT ( 'NONE', #42155 ) ;
#753=VECTOR ( 'NONE', #10732, 1000.000000000000114 ) ;
#760=EDGE_LOOP ( 'NONE', ( #11877, #61842, #65585, #14010, #43398, #6520 ) ) ;
#762=CARTESIAN_POINT ( 'NONE',  ( 275.5000000000000000, 50.00000000000000000, 27.00000000000000000 ) ) ;
#824=VECTOR ( 'NONE', #5850, 1000.000000000000000 ) ;
#825=( GEOMETRIC_REPRESENTATION_CONTEXT ( 3 ) GLOBAL_UNCERTAINTY_ASSIGNED_CONTEXT ( ( #21060 ) ) GLOBAL_UNIT_ASSIGNED_CONTEXT ( ( #4006, #36892, #47144 ) ) REPRESENTATION_CONTEXT ( 'NONE', 'WORKASPACE' ) );
#841=CARTESIAN_POINT ( 'NONE',  ( 277.1811023147819810, -20.65270074880750428, -17.15270074880750784 ) ) ;
#876=EDGE_LOOP ( 'NONE', ( #22779, #36516, #11658, #58619 ) ) ;
#893=ORIENTED_EDGE ( 'NONE', *, *, #55404, .T. ) ;
#901=DIRECTION ( 'NONE',  ( -1.000000000000000000, 0.000000000000000000, 0.000000000000000000 ) ) ;
#911=FACE_OUTER_BOUND ( 'NONE', #18961, .T. ) ;
#914=ADVANCED_FACE ( 'NONE', ( #64433 ), #11706, .F. ) ;
#916=EDGE_CURVE ( 'NONE', #53994, #5435, #428, .T. ) ;
#926=CARTESIAN_POINT ( 'NONE',  ( 275.5000000000000000, -42.50000000000000000, 26.50000000000000000 ) ) ;
#928=VECTOR ( 'NONE', #4450, 1000.000000000000000 ) ;
#949=ADVANCED_FACE ( 'NONE', ( #38260 ), #49211, .F. ) ;
#950=ORIENTED_EDGE ( 'NONE', *, *, #46963, .T. ) ;
#955=VECTOR ( 'NONE', #42136, 1000.000000000000000 ) ;
#988=DIRECTION ( 'NONE',  ( 0.000000000000000000, 1.000000000000000000, 1.880440247955360336E-12 ) ) ;
#992=VERTEX_POINT ( 'NONE', #55548 ) ;
#1005=VERTEX_POINT ( 'NONE', #2144 ) ;
#1022=CIRCLE ( 'NONE', #10201, 1.999999999999315436 ) ;
#1037=DIRECTION ( 'NONE',  ( 0.000000000000000000, -1.000000000000000000, 0.000000000000000000 ) ) ;
#1038=DIRECTION ( 'NONE',  ( 0.000000000000000000, 0.000000000000000000, 1.000000000000000000 ) ) ;
#1040=VERTEX_POINT ( 'NONE', #39957 ) ;
#1048=CARTESIAN_POINT ( 'NONE',  ( 283.0000000000000568, -39.80000000000000426, -8.400000000000000355 ) ) ;
#1060=ORIENTED_EDGE ( 'NONE', *, *, #2553, .T. ) ;
#1067=DIRECTION ( 'NONE',  ( 1.000000000000000000, 0.000000000000000000, 0.000000000000000000 ) ) ;
#1068=FACE_OUTER_BOUND ( 'NONE', #61139, .T. ) ;
#1078=ORIENTED_EDGE ( 'NONE', *, *, #7206, .F. ) ;
#1089=ORIENTED_EDGE ( 'NONE', *, *, #21994, .T. ) ;
#1096=CARTESIAN_POINT ( 'NONE',  ( 283.0000000000000568, -23.70411739045900390, 12.50000000000000000 ) ) ;
#1111=CARTESIAN_POINT ( 'NONE',  ( 283.0000000000000568, -42.50000000000000000, -7.500000000000000000 ) ) ;
#1117=ORIENTED_EDGE ( 'NONE', *, *, #195, .F. ) ;
#1120=ORIENTED_EDGE ( 'NONE', *, *, #57494, .F. ) ;
#1141=VERTEX_POINT ( 'NONE', #34665 ) ;
#1146=ORIENTED_EDGE ( 'NONE', *, *, #32037, .F. ) ;
#1147=CARTESIAN_POINT ( 'NONE',  ( 14.50000000000000000, -0.5000000000000000000, -27.00000000000000000 ) ) ;
#1162=FACE_OUTER_BOUND ( 'NONE', #57497, .T. ) ;
#1166=PRODUCT_DEFINITION ( 'UNKNOWN', '', #16619, #28930 ) ;
#1167=DIRECTION ( 'NONE',  ( 0.000000000000000000, -1.000000000000000000, 0.000000000000000000 ) ) ;
#1174=CARTESIAN_POINT ( 'NONE',  ( 10.62249899919920004, -53.81370849898476649, -17.50000000000000000 ) ) ;
#1184=ORIENTED_EDGE ( 'NONE', *, *, #68443, .T. ) ;
#1197=DIRECTION ( 'NONE',  ( 1.000000000000000000, 0.000000000000000000, 0.000000000000000000 ) ) ;
#1205=DIRECTION ( 'NONE',  ( 0.000000000000000000, -1.000000000000000000, 0.000000000000000000 ) ) ;
#1214=AXIS2_PLACEMENT_3D ( 'NONE', #27801, #65298, #22835 ) ;
#1215=ORIENTED_EDGE ( 'NONE', *, *, #57311, .T. ) ;
#1232=PLANE ( 'NONE',  #35006 ) ;
#1244=EDGE_CURVE ( 'NONE', #17331, #9620, #3201, .T. ) ;
#1251=ORIENTED_EDGE ( 'NONE', *, *, #54904, .F. ) ;
#1268=DIRECTION ( 'NONE',  ( -1.000000000000000000, 0.000000000000000000, 0.000000000000000000 ) ) ;
#1269=ORIENTED_EDGE ( 'NONE', *, *, #4748, .T. ) ;
#1279=CIRCLE ( 'NONE', #3559, 0.5000000000009372503 ) ;
#1308=DIRECTION ( 'NONE',  ( 0.000000000000000000, -0.7075259945833242137, 0.7066873191085842887 ) ) ;
#1310=CARTESIAN_POINT ( 'NONE',  ( 283.0000000000000568, -25.60000000000000142, 15.10000000000000142 ) ) ;
#1322=EDGE_CURVE ( 'NONE', #33439, #58687, #16057, .T. ) ;
#1330=ORIENTED_EDGE ( 'NONE', *, *, #63237, .T. ) ;
#1343=CIRCLE ( 'NONE', #12574, 4.000000000000000000 ) ;
#1344=CARTESIAN_POINT ( 'NONE',  ( 7.000000000000000000, -21.00000000000000000, 0.000000000000000000 ) ) ;
#1346=CARTESIAN_POINT ( 'NONE',  ( 283.0000000000000568, -42.50000000000000000, -15.10000000000000142 ) ) ;
#1353=FACE_OUTER_BOUND ( 'NONE', #2216, .T. ) ;
#1379=ORIENTED_EDGE ( 'NONE', *, *, #7734, .F. ) ;
#1403=FACE_OUTER_BOUND ( 'NONE', #19703, .T. ) ;
#1405=EDGE_CURVE ( 'NONE', #49901, #24890, #6667, .T. ) ;
#1408=ORIENTED_EDGE ( 'NONE', *, *, #33147, .F. ) ;
#1409=VECTOR ( 'NONE', #51524, 1000.000000000000000 ) ;
#1411=CARTESIAN_POINT ( 'NONE',  ( 7.000000000000000000, -32.45000000000000995, 15.00000000000000000 ) ) ;
#1416=ORIENTED_EDGE ( 'NONE', *, *, #51944, .F. ) ;
#1429=CARTESIAN_POINT ( 'NONE',  ( 7.000000000000000000, -20.40000000000000213, 16.03137303340311348 ) ) ;
#1431=VECTOR ( 'NONE', #21426, 1000.000000000000000 ) ;
#1462=VERTEX_POINT ( 'NONE', #49806 ) ;
#1466=CARTESIAN_POINT ( 'NONE',  ( 7.000000000000000000, -38.65000000000095781, -14.49999999999903899 ) ) ;
#1487=EDGE_CURVE ( 'NONE', #16822, #52439, #21549, .T. ) ;
#1493=EDGE_CURVE ( 'NONE', #44134, #53260, #54471, .T. ) ;
#1500=AXIS2_PLACEMENT_3D ( 'NONE', #56590, #57295, #62959 ) ;
#1503=VECTOR ( 'NONE', #29338, 1000.000000000000000 ) ;
#1507=CIRCLE ( 'NONE', #18452, 0.5000000000009459100 ) ;
#1518=DIRECTION ( 'NONE',  ( 0.000000000000000000, -0.7071067811865875408, -0.7071067811865076047 ) ) ;
#1523=DIRECTION ( 'NONE',  ( 0.000000000000000000, 1.000000000000000000, 0.000000000000000000 ) ) ;
#1531=DIRECTION ( 'NONE',  ( 0.7071067811865463515, 0.7071067811865487940, 0.000000000000000000 ) ) ;
#1535=CARTESIAN_POINT ( 'NONE',  ( 277.3542486889354564, -20.50000000000000000, 17.00000000000000000 ) ) ;
#1544=DIRECTION ( 'NONE',  ( 0.000000000000000000, 1.000000000000000000, 0.000000000000000000 ) ) ;
#1566=CARTESIAN_POINT ( 'NONE',  ( 275.0000000000000000, -0.5000000000000000000, 50.00000000000000000 ) ) ;
#1578=ORIENTED_EDGE ( 'NONE', *, *, #61062, .F. ) ;
#1582=CARTESIAN_POINT ( 'NONE',  ( 283.0000000000000568, -31.30000000000045191, 8.900000000000430234 ) ) ;
#1598=VECTOR ( 'NONE', #19788, 1000.000000000000000 ) ;
#1599=VERTEX_POINT ( 'NONE', #35984 ) ;
#1604=VECTOR ( 'NONE', #54096, 1000.000000000000000 ) ;
#1633=ORIENTED_EDGE ( 'NONE', *, *, #51084, .F. ) ;
#1645=ADVANCED_FACE ( 'NONE', ( #67474 ), #19022, .F. ) ;
#1665=LINE ( 'NONE', #45144, #10556 ) ;
#1679=FACE_OUTER_BOUND ( 'NONE', #12903, .T. ) ;
#1680=EDGE_CURVE ( 'NONE', #55748, #40253, #35619, .T. ) ;
#1737=VECTOR ( 'NONE', #21797, 1000.000000000000000 ) ;
#1738=CARTESIAN_POINT ( 'NONE',  ( 283.0000000000000568, -20.50000000000000000, -17.00000000000000000 ) ) ;
#1749=ORIENTED_EDGE ( 'NONE', *, *, #28904, .F. ) ;
#1750=EDGE_CURVE ( 'NONE', #68268, #288, #69045, .T. ) ;
#1751=CARTESIAN_POINT ( 'NONE',  ( 7.000000000000000000, -40.30000000000000426, 8.900000000000000355 ) ) ;
#1759=DIRECTION ( 'NONE',  ( 0.000000000000000000, 1.000000000000000000, 0.000000000000000000 ) ) ;
#1768=AXIS2_PLACEMENT_3D ( 'NONE', #6717, #60465, #33930 ) ;
#1770=ORIENTED_EDGE ( 'NONE', *, *, #65264, .F. ) ;
#1776=DIRECTION ( 'NONE',  ( 0.000000000000000000, 0.7071067811865474617, 0.7071067811865474617 ) ) ;
#1785=CARTESIAN_POINT ( 'NONE',  ( 7.000000000000000000, -23.50007830495750127, -12.28007262201345995 ) ) ;
#1791=ORIENTED_EDGE ( 'NONE', *, *, #45815, .F. ) ;
#1799=CARTESIAN_POINT ( 'NONE',  ( 283.0000000000000568, -25.56180396883900130, 14.25872597390799967 ) ) ;
#1833=ORIENTED_EDGE ( 'NONE', *, *, #58480, .T. ) ;
#1856=VECTOR ( 'NONE', #60431, 1000.000000000000114 ) ;
#1865=ORIENTED_EDGE ( 'NONE', *, *, #69497, .F. ) ;
#1869=( BOUNDED_CURVE ( )  B_SPLINE_CURVE ( 3, ( #40623, #13401, #30014, #8805 ),
 .UNSPECIFIED., .F., .F. ) 
 B_SPLINE_CURVE_WITH_KNOTS ( ( 4, 4 ),
 ( 0.7227342478134164416, 0.8480620789814840021 ),
 .UNSPECIFIED. ) 
 CURVE ( )  GEOMETRIC_REPRESENTATION_ITEM ( )  RATIONAL_B_SPLINE_CURVE ( ( 1.000000000000000000, 0.9986915061577686936, 0.9986915061577686936, 1.000000000000000000 ) ) 
 REPRESENTATION_ITEM ( '' )  );
#1874=ORIENTED_EDGE ( 'NONE', *, *, #23682, .T. ) ;
#1876=FACE_OUTER_BOUND ( 'NONE', #61635, .T. ) ;
#1887=CARTESIAN_POINT ( 'NONE',  ( 7.000000000000000000, -38.09999999999885034, 7.900000000002049383 ) ) ;
#1916=ORIENTED_EDGE ( 'NONE', *, *, #29294, .F. ) ;
#1930=EDGE_LOOP ( 'NONE', ( #25395, #45905, #27603, #50848, #50229, #47234 ) ) ;
#1943=CARTESIAN_POINT ( 'NONE',  ( 283.0000000000000568, -27.13000000000000611, 13.50000000000000000 ) ) ;
#1956=DIRECTION ( 'NONE',  ( 0.000000000000000000, 1.000000000000000000, 0.000000000000000000 ) ) ;
#1979=ORIENTED_EDGE ( 'NONE', *, *, #51944, .T. ) ;
#1986=ORIENTED_EDGE ( 'NONE', *, *, #3138, .T. ) ;
#1998=DIRECTION ( 'NONE',  ( 0.000000000000000000, 0.000000000000000000, -1.000000000000000000 ) ) ;
#2019=ORIENTED_EDGE ( 'NONE', *, *, #43767, .T. ) ;
#2037=CARTESIAN_POINT ( 'NONE',  ( 275.0000000000000000, -21.00000000000000000, -5.000000000000000000 ) ) ;
#2050=VERTEX_POINT ( 'NONE', #29891 ) ;
#2051=CARTESIAN_POINT ( 'NONE',  ( 283.0000000000000568, -39.79999999999905214, 12.19999999999906315 ) ) ;
#2061=DIRECTION ( 'NONE',  ( -1.000000000000000000, 0.000000000000000000, 0.000000000000000000 ) ) ;
#2071=CARTESIAN_POINT ( 'NONE',  ( 7.000000000000000000, -31.30000000000000071, 12.69999999999999929 ) ) ;
#2086=EDGE_CURVE ( 'NONE', #68211, #36802, #45805, .T. ) ;
#2097=EDGE_CURVE ( 'NONE', #45523, #65979, #94, .T. ) ;
#2103=ORIENTED_EDGE ( 'NONE', *, *, #44517, .T. ) ;
#2127=CARTESIAN_POINT ( 'NONE',  ( 15.00000000000000000, -25.60000000000000142, -15.10000000000000142 ) ) ;
#2130=CARTESIAN_POINT ( 'NONE',  ( 14.75000000000000355, -0.2500000000000096589, 26.74999999999999289 ) ) ;
#2143=ORIENTED_EDGE ( 'NONE', *, *, #36742, .F. ) ;
#2144=CARTESIAN_POINT ( 'NONE',  ( 275.5000000000000000, -42.50000000000000000, -26.50000000000000000 ) ) ;
#2160=ORIENTED_EDGE ( 'NONE', *, *, #21520, .T. ) ;
#2162=AXIS2_PLACEMENT_3D ( 'NONE', #53607, #42635, #58908 ) ;
#2165=VECTOR ( 'NONE', #62454, 1000.000000000000000 ) ;
#2176=EDGE_CURVE ( 'NONE', #69782, #34171, #6089, .T. ) ;
#2183=VECTOR ( 'NONE', #64370, 1000.000000000000000 ) ;
#2189=LINE ( 'NONE', #18090, #57170 ) ;
#2193=LINE ( 'NONE', #23761, #7915 ) ;
#2206=CARTESIAN_POINT ( 'NONE',  ( 283.0000000000000568, -27.13000000000000611, -13.50000000000000000 ) ) ;
#2215=DIRECTION ( 'NONE',  ( 1.000000000000000000, -0.000000000000000000, -0.000000000000000000 ) ) ;
#2216=EDGE_LOOP ( 'NONE', ( #62847, #12809, #40061, #13416 ) ) ;
#2236=EDGE_CURVE ( 'NONE', #61067, #1462, #21311, .T. ) ;
#2238=LINE ( 'NONE', #51027, #30787 ) ;
#2262=ORIENTED_EDGE ( 'NONE', *, *, #11342, .F. ) ;
#2265=DIRECTION ( 'NONE',  ( 0.000000000000000000, 0.000000000000000000, 1.000000000000000000 ) ) ;
#2280=EDGE_LOOP ( 'NONE', ( #11523, #12923, #40662, #61638 ) ) ;
#2284=LINE ( 'NONE', #8636, #61637 ) ;
#2285=CIRCLE ( 'NONE', #12462, 0.5000000000023407942 ) ;
#2333=EDGE_CURVE ( 'NONE', #25742, #5708, #39967, .T. ) ;
#2362=ORIENTED_EDGE ( 'NONE', *, *, #6675, .F. ) ;
#2388=CARTESIAN_POINT ( 'NONE',  ( 275.0000000000000000, -42.00000000000000000, -26.50000000000000000 ) ) ;
#2417=AXIS2_PLACEMENT_3D ( 'NONE', #12115, #45675, #38655 ) ;
#2418=CARTESIAN_POINT ( 'NONE',  ( 275.0000000000000000, -30.80000000000000071, -8.900000000000000355 ) ) ;
#2428=DIRECTION ( 'NONE',  ( 0.000000000000000000, 0.000000000000000000, 1.000000000000000000 ) ) ;
#2432=LINE ( 'NONE', #62882, #54244 ) ;
#2448=ORIENTED_EDGE ( 'NONE', *, *, #36008, .F. ) ;
#2454=CARTESIAN_POINT ( 'NONE',  ( 7.500000000000000000, -20.40000000000000213, 20.00000000000000000 ) ) ;
#2457=DIRECTION ( 'NONE',  ( 0.000000000000000000, 0.000000000000000000, 1.000000000000000000 ) ) ;
#2461=LINE ( 'NONE', #66123, #65157 ) ;
#2471=CARTESIAN_POINT ( 'NONE',  ( 7.000000000000000000, -31.30000000000000071, -12.69999999999999929 ) ) ;
#2478=EDGE_CURVE ( 'NONE', #49993, #10776, #37604, .T. ) ;
#2507=EDGE_CURVE ( 'NONE', #11767, #61271, #48445, .T. ) ;
#2515=CARTESIAN_POINT ( 'NONE',  ( 15.00000000000000000, -42.50000000000000000, -27.00000000000000000 ) ) ;
#2551=VERTEX_POINT ( 'NONE', #27566 ) ;
#2553=EDGE_CURVE ( 'NONE', #65808, #53260, #11, .T. ) ;
#2564=CARTESIAN_POINT ( 'NONE',  ( 275.0000000000000000, -26.50000000000000000, -0.5000000000000000000 ) ) ;
#2583=DIRECTION ( 'NONE',  ( 0.000000000000000000, 0.000000000000000000, -1.000000000000000000 ) ) ;
#2588=ORIENTED_EDGE ( 'NONE', *, *, #65248, .F. ) ;
#2589=ORIENTED_EDGE ( 'NONE', *, *, #30303, .F. ) ;
#2597=DIRECTION ( 'NONE',  ( 0.000000000000000000, -1.000000000000000000, -1.880440247955360336E-12 ) ) ;
#2600=ORIENTED_EDGE ( 'NONE', *, *, #41043, .T. ) ;
#2602=ORIENTED_EDGE ( 'NONE', *, *, #12840, .T. ) ;
#2616=ORIENTED_EDGE ( 'NONE', *, *, #10169, .F. ) ;
#2626=EDGE_CURVE ( 'NONE', #32093, #14268, #47783, .T. ) ;
#2669=AXIS2_PLACEMENT_3D ( 'NONE', #16360, #11061, #48540 ) ;
#2676=EDGE_CURVE ( 'NONE', #17055, #62668, #23629, .T. ) ;
#2677=ORIENTED_EDGE ( 'NONE', *, *, #39393, .T. ) ;
#2683=VERTEX_POINT ( 'NONE', #61107 ) ;
#2686=PLANE ( 'NONE',  #43491 ) ;
#2711=AXIS2_PLACEMENT_3D ( 'NONE', #13802, #15221, #20864 ) ;
#2712=DIRECTION ( 'NONE',  ( 1.000000000000000000, 0.000000000000000000, 0.000000000000000000 ) ) ;
#2713=EDGE_CURVE ( 'NONE', #42484, #9816, #11972, .T. ) ;
#2748=ORIENTED_EDGE ( 'NONE', *, *, #56140, .F. ) ;
#2786=DIRECTION ( 'NONE',  ( 1.000000000000000000, 0.000000000000000000, 0.000000000000000000 ) ) ;
#2793=CARTESIAN_POINT ( 'NONE',  ( 15.00000000000000000, -25.60000000000000142, -15.10000000000000142 ) ) ;
#2824=ADVANCED_FACE ( 'NONE', ( #19036 ), #35272, .T. ) ;
#2847=VERTEX_POINT ( 'NONE', #63218 ) ;
#2860=ORIENTED_EDGE ( 'NONE', *, *, #47589, .F. ) ;
#2869=LINE ( 'NONE', #67225, #43226 ) ;
#2884=LINE ( 'NONE', #7829, #35784 ) ;
#2905=ORIENTED_EDGE ( 'NONE', *, *, #21002, .F. ) ;
#2917=ORIENTED_EDGE ( 'NONE', *, *, #58860, .F. ) ;
#2937=DIRECTION ( 'NONE',  ( 1.000000000000000000, 0.000000000000000000, 0.000000000000000000 ) ) ;
#2947=EDGE_CURVE ( 'NONE', #49494, #4296, #40474, .T. ) ;
#2951=AXIS2_PLACEMENT_3D ( 'NONE', #45058, #66632, #18187 ) ;
#2953=DIRECTION ( 'NONE',  ( -1.000000000000000000, 0.000000000000000000, 0.000000000000000000 ) ) ;
#2955=AXIS2_PLACEMENT_3D ( 'NONE', #18935, #33791, #7958 ) ;
#2979=VECTOR ( 'NONE', #44158, 1000.000000000000000 ) ;
#2985=LINE ( 'NONE', #67338, #6758 ) ;
#2999=DIRECTION ( 'NONE',  ( 1.000000000000000000, 0.000000000000000000, 0.000000000000000000 ) ) ;
#3019=LINE ( 'NONE', #18565, #62458 ) ;
#3033=LINE ( 'NONE', #34475, #62310 ) ;
#3046=ORIENTED_EDGE ( 'NONE', *, *, #17068, .F. ) ;
#3070=AXIS2_PLACEMENT_3D ( 'NONE', #68809, #35286, #30973 ) ;
#3076=VERTEX_POINT ( 'NONE', #19602 ) ;
#3085=CARTESIAN_POINT ( 'NONE',  ( 7.000000000000000000, -20.49999999999999645, 16.03137303340311348 ) ) ;
#3096=VERTEX_POINT ( 'NONE', #4760 ) ;
#3117=VERTEX_POINT ( 'NONE', #15012 ) ;
#3121=LINE ( 'NONE', #28582, #7836 ) ;
#3129=LINE ( 'NONE', #57558, #62023 ) ;
#3138=EDGE_CURVE ( 'NONE', #34214, #37466, #14659, .T. ) ;
#3163=LINE ( 'NONE', #57943, #37545 ) ;
#3168=LINE ( 'NONE', #58320, #47025 ) ;
#3191=CARTESIAN_POINT ( 'NONE',  ( 7.000000000000000000, -32.45000000000000995, 12.69999999999999929 ) ) ;
#3192=ORIENTED_EDGE ( 'NONE', *, *, #52966, .T. ) ;
#3194=VERTEX_POINT ( 'NONE', #38667 ) ;
#3197=LINE ( 'NONE', #39608, #25745 ) ;
#3201=LINE ( 'NONE', #30417, #21667 ) ;
#3229=ORIENTED_EDGE ( 'NONE', *, *, #51999, .T. ) ;
#3238=EDGE_LOOP ( 'NONE', ( #61198, #10889, #1184, #15590, #5381, #30874, #63407, #27845, #43213, #49891, #12745, #26400, #49474, #15884, #11198, #61357, #41052, #52342, #10629, #38416, #27315, #43348, #47848, #18286, #15373, #67091, #24435, #31034, #54275, #64877, #17293, #56855, #11270, #38580, #54597 ) ) ;
#3249=ORIENTED_EDGE ( 'NONE', *, *, #62051, .F. ) ;
#3254=CARTESIAN_POINT ( 'NONE',  ( 283.0000000000000568, -20.50000000000000000, -13.00000000000000178 ) ) ;
#3259=EDGE_CURVE ( 'NONE', #49352, #54496, #52434, .T. ) ;
#3264=ORIENTED_EDGE ( 'NONE', *, *, #33454, .T. ) ;
#3270=FACE_OUTER_BOUND ( 'NONE', #56070, .T. ) ;
#3273=FACE_OUTER_BOUND ( 'NONE', #61987, .T. ) ;
#3289=CARTESIAN_POINT ( 'NONE',  ( 283.0000000000000568, -31.30000000000000071, -8.400000000000000355 ) ) ;
#3314=EDGE_CURVE ( 'NONE', #28510, #61067, #38835, .T. ) ;
#3322=DIRECTION ( 'NONE',  ( 0.000000000000000000, 0.000000000000000000, -1.000000000000000000 ) ) ;
#3323=LINE ( 'NONE', #18174, #21152 ) ;
#3346=DIRECTION ( 'NONE',  ( 0.000000000000000000, 0.7066873191084661610, -0.7075259945834421194 ) ) ;
#3367=AXIS2_PLACEMENT_3D ( 'NONE', #28552, #666, #6648 ) ;
#3402=CARTESIAN_POINT ( 'NONE',  ( 283.0000000000000568, -39.80000000000000426, -8.400000000000000355 ) ) ;
#3434=EDGE_CURVE ( 'NONE', #69122, #11772, #8482, .T. ) ;
#3448=LINE ( 'NONE', #13349, #32751 ) ;
#3452=DIRECTION ( 'NONE',  ( 0.000000000000000000, -1.000000000000000000, 0.000000000000000000 ) ) ;
#3453=CIRCLE ( 'NONE', #42975, 0.5000000000023371305 ) ;
#3460=ADVANCED_FACE ( 'NONE', ( #35342 ), #56238, .F. ) ;
#3469=EDGE_CURVE ( 'NONE', #53282, #48333, #29350, .T. ) ;
#3486=EDGE_CURVE ( 'NONE', #61959, #17055, #48428, .T. ) ;
#3493=ORIENTED_EDGE ( 'NONE', *, *, #45198, .F. ) ;
#3501=EDGE_LOOP ( 'NONE', ( #50528, #8821, #8600, #31541, #54176, #52794 ) ) ;
#3507=ORIENTED_EDGE ( 'NONE', *, *, #58339, .T. ) ;
#3514=VERTEX_POINT ( 'NONE', #40360 ) ;
#3536=EDGE_CURVE ( 'NONE', #30152, #40696, #20853, .T. ) ;
#3540=DIRECTION ( 'NONE',  ( 1.000000000000000000, -0.000000000000000000, -0.000000000000000000 ) ) ;
#3559=AXIS2_PLACEMENT_3D ( 'NONE', #54291, #5849, #21760 ) ;
#3571=VECTOR ( 'NONE', #17072, 1000.000000000000000 ) ;
#3581=AXIS2_PLACEMENT_3D ( 'NONE', #32433, #68861, #42328 ) ;
#3593=VECTOR ( 'NONE', #52772, 1000.000000000000114 ) ;
#3628=PLANE ( 'NONE',  #12760 ) ;
#3644=DIRECTION ( 'NONE',  ( 0.000000000000000000, 1.000000000000000000, 0.000000000000000000 ) ) ;
#3646=ORIENTED_EDGE ( 'NONE', *, *, #28667, .F. ) ;
#3647=VERTEX_POINT ( 'NONE', #44145 ) ;
#3650=DIRECTION ( 'NONE',  ( 0.000000000000000000, 0.000000000000000000, 1.000000000000000000 ) ) ;
#3657=ADVANCED_FACE ( 'NONE', ( #7001 ), #43813, .T. ) ;
#3658=ADVANCED_FACE ( 'NONE', ( #60402 ), #28233, .F. ) ;
#3673=CARTESIAN_POINT ( 'NONE',  ( 275.0000000000000000, -23.50007830495750127, 12.58007262201399890 ) ) ;
#3674=DIRECTION ( 'NONE',  ( -1.000000000000000000, 0.000000000000000000, 0.000000000000000000 ) ) ;
#3678=CARTESIAN_POINT ( 'NONE',  ( 289.5000000000001705, -42.50000000000007105, -26.49999999999997158 ) ) ;
#3686=VECTOR ( 'NONE', #21728, 1000.000000000000114 ) ;
#3695=VECTOR ( 'NONE', #64312, 1000.000000000000000 ) ;
#3699=CARTESIAN_POINT ( 'NONE',  ( 283.0000000000000568, -31.30000000000000071, -12.69999999999999929 ) ) ;
#3701=CYLINDRICAL_SURFACE ( 'NONE', #24787, 0.4999999999945534124 ) ;
#3704=DIRECTION ( 'NONE',  ( 0.000000000000000000, 0.000000000000000000, 1.000000000000000000 ) ) ;
#3730=CARTESIAN_POINT ( 'NONE',  ( 283.0000000000000568, -40.30000000000000426, -12.20000000000000107 ) ) ;
#3763=CARTESIAN_POINT ( 'NONE',  ( 7.000000000000000000, -38.64999999999999858, 15.00000000000000000 ) ) ;
#3770=CYLINDRICAL_SURFACE ( 'NONE', #5363, 4.000000000000000000 ) ;
#3803=CARTESIAN_POINT ( 'NONE',  ( 275.0000000000000000, -37.15000000000001279, -7.700000000000000178 ) ) ;
#3807=ORIENTED_EDGE ( 'NONE', *, *, #24948, .T. ) ;
#3845=VECTOR ( 'NONE', #35074, 1000.000000000000000 ) ;
#3894=ORIENTED_EDGE ( 'NONE', *, *, #14685, .T. ) ;
#3914=DIRECTION ( 'NONE',  ( -1.000000000000000000, 0.000000000000000000, 0.000000000000000000 ) ) ;
#3917=ORIENTED_EDGE ( 'NONE', *, *, #41787, .F. ) ;
#3918=DIRECTION ( 'NONE',  ( 0.000000000000000000, 0.000000000000000000, 1.000000000000000000 ) ) ;
#3925=ORIENTED_EDGE ( 'NONE', *, *, #14477, .T. ) ;
#3929=EDGE_CURVE ( 'NONE', #65979, #60826, #35981, .T. ) ;
#3953=DIRECTION ( 'NONE',  ( 0.000000000000000000, 0.000000000000000000, -1.000000000000000000 ) ) ;
#3960=AXIS2_PLACEMENT_3D ( 'NONE', #16038, #37608, #44969 ) ;
#3965=CARTESIAN_POINT ( 'NONE',  ( 275.5000000000000000, 0.000000000000000000, -26.50000000000000000 ) ) ;
#3976=ORIENTED_EDGE ( 'NONE', *, *, #61797, .F. ) ;
#3997=LINE ( 'NONE', #26262, #51289 ) ;
#4005=LINE ( 'NONE', #36519, #59211 ) ;
#4006=( LENGTH_UNIT ( ) NAMED_UNIT ( * ) SI_UNIT ( .MILLI., .METRE. ) );
#4030=ADVANCED_FACE ( 'NONE', ( #16858 ), #28154, .T. ) ;
#4042=CARTESIAN_POINT ( 'NONE',  ( 283.0000000000000568, -25.60000000000000142, -17.60000000000000142 ) ) ;
#4057=CARTESIAN_POINT ( 'NONE',  ( 276.8775010008008053, -25.00000000000000000, 17.50000000000000000 ) ) ;
#4066=VECTOR ( 'NONE', #40194, 1000.000000000000000 ) ;
#4076=LINE ( 'NONE', #15728, #48655 ) ;
#4077=ORIENTED_EDGE ( 'NONE', *, *, #16945, .T. ) ;
#4083=ORIENTED_EDGE ( 'NONE', *, *, #31977, .F. ) ;
#4093=LINE ( 'NONE', #63834, #21903 ) ;
#4103=VECTOR ( 'NONE', #43325, 1000.000000000000000 ) ;
#4108=ORIENTED_EDGE ( 'NONE', *, *, #19014, .T. ) ;
#4113=EDGE_CURVE ( 'NONE', #35743, #69116, #6306, .T. ) ;
#4131=DIRECTION ( 'NONE',  ( 1.000000000000000000, -0.000000000000000000, -0.000000000000000000 ) ) ;
#4149=DIRECTION ( 'NONE',  ( 0.7071067811865475727, 0.000000000000000000, -0.7071067811865475727 ) ) ;
#4200=DIRECTION ( 'NONE',  ( -1.000000000000000000, 0.000000000000000000, 0.000000000000000000 ) ) ;
#4202=EDGE_CURVE ( 'NONE', #3514, #39584, #34836, .T. ) ;
#4264=ORIENTED_EDGE ( 'NONE', *, *, #54338, .F. ) ;
#4284=ADVANCED_FACE ( 'NONE', ( #40497 ), #45098, .F. ) ;
#4296=VERTEX_POINT ( 'NONE', #52805 ) ;
#4301=DIRECTION ( 'NONE',  ( -1.000000000000000000, 0.000000000000000000, 0.000000000000000000 ) ) ;
#4305=CARTESIAN_POINT ( 'NONE',  ( 275.5000000000000000, -42.50000000000000000, 15.10000000000000142 ) ) ;
#4325=DIRECTION ( 'NONE',  ( 1.000000000000000000, 0.000000000000000000, 0.000000000000000000 ) ) ;
#4329=ORIENTED_EDGE ( 'NONE', *, *, #49172, .T. ) ;
#4335=CARTESIAN_POINT ( 'NONE',  ( 275.0000000000000000, -31.30000000000095284, 12.19999999999906315 ) ) ;
#4345=DIRECTION ( 'NONE',  ( 0.000000000000000000, 0.6801302850037830305, 0.7330912599538155217 ) ) ;
#4346=LINE ( 'NONE', #14235, #19810 ) ;
#4348=CARTESIAN_POINT ( 'NONE',  ( 283.0000000000000568, -25.93000000000544958, -9.412893218815410634 ) ) ;
#4354=ORIENTED_EDGE ( 'NONE', *, *, #19983, .F. ) ;
#4381=EDGE_LOOP ( 'NONE', ( #56656, #9144, #23807, #28461 ) ) ;
#4404=CARTESIAN_POINT ( 'NONE',  ( 15.00000000000000000, -21.00000000000000000, 8.000000000000000000 ) ) ;
#4405=DIRECTION ( 'NONE',  ( -1.000000000000000000, 0.000000000000000000, 0.000000000000000000 ) ) ;
#4434=ADVANCED_FACE ( 'NONE', ( #65481 ), #6760, .F. ) ;
#4439=LINE ( 'NONE', #63822, #53806 ) ;
#4450=DIRECTION ( 'NONE',  ( -0.5773502691896246208, 0.5773502691896263972, -0.5773502691896263972 ) ) ;
#4455=DIRECTION ( 'NONE',  ( 0.000000000000000000, -1.000000000000000000, 0.000000000000000000 ) ) ;
#4482=CARTESIAN_POINT ( 'NONE',  ( 283.0000000000000568, -27.13000000000000611, -13.50000000000000000 ) ) ;
#4485=DIRECTION ( 'NONE',  ( 1.000000000000000000, 0.000000000000000000, 0.000000000000000000 ) ) ;
#4495=VECTOR ( 'NONE', #47777, 1000.000000000000000 ) ;
#4523=ORIENTED_EDGE ( 'NONE', *, *, #7471, .T. ) ;
#4524=CARTESIAN_POINT ( 'NONE',  ( 283.0000000000000568, -25.14575131106458272, -17.35424868893542083 ) ) ;
#4545=ORIENTED_EDGE ( 'NONE', *, *, #18365, .T. ) ;
#4561=PLANE ( 'NONE',  #41420 ) ;
#4568=CARTESIAN_POINT ( 'NONE',  ( 15.00000000000000000, -42.00000000000000000, -26.50000000000000000 ) ) ;
#4591=VECTOR ( 'NONE', #64046, 1000.000000000000000 ) ;
#4616=CARTESIAN_POINT ( 'NONE',  ( 14.50000000000000178, -42.50000000000000000, 26.50000000000000000 ) ) ;
#4638=ORIENTED_EDGE ( 'NONE', *, *, #9454, .F. ) ;
#4656=EDGE_LOOP ( 'NONE', ( #51797, #21497, #10771, #16036, #186 ) ) ;
#4699=ADVANCED_FACE ( 'NONE', ( #24430 ), #19462, .T. ) ;
#4725=DIRECTION ( 'NONE',  ( -1.000000000000000000, 0.000000000000000000, 0.000000000000000000 ) ) ;
#4727=CARTESIAN_POINT ( 'NONE',  ( 274.9999999999998863, -42.00000000000005684, 26.50000000000005329 ) ) ;
#4728=ORIENTED_EDGE ( 'NONE', *, *, #8290, .F. ) ;
#4748=EDGE_CURVE ( 'NONE', #3096, #42177, #31495, .T. ) ;
#4760=CARTESIAN_POINT ( 'NONE',  ( 7.000000000000000000, -25.50000000000000355, -14.74860679774999994 ) ) ;
#4781=CARTESIAN_POINT ( 'NONE',  ( 14.50000000000000000, -0.5000000000000000000, 27.00000000000000000 ) ) ;
#4793=LINE ( 'NONE', #62781, #68911 ) ;
#4824=CARTESIAN_POINT ( 'NONE',  ( 14.50000000000000000, 0.000000000000000000, -26.50000000000000000 ) ) ;
#4832=VECTOR ( 'NONE', #64916, 999.9999999999998863 ) ;
#4836=CARTESIAN_POINT ( 'NONE',  ( 283.0000000000000568, -20.40000000000000213, -17.60000000000000142 ) ) ;
#4842=LINE ( 'NONE', #36308, #45647 ) ;
#4855=EDGE_CURVE ( 'NONE', #14910, #35722, #6345, .T. ) ;
#4863=AXIS2_PLACEMENT_3D ( 'NONE', #10909, #32487, #38142 ) ;
#4891=PLANE ( 'NONE',  #31265 ) ;
#4895=PLANE ( 'NONE',  #47185 ) ;
#4919=CARTESIAN_POINT ( 'NONE',  ( 275.0000000000000000, -25.50000000000000355, 17.00000000000000000 ) ) ;
#4959=PLANE ( 'NONE',  #22165 ) ;
#4971=LINE ( 'NONE', #26536, #2183 ) ;
#4975=ORIENTED_EDGE ( 'NONE', *, *, #12525, .T. ) ;
#4988=DIRECTION ( 'NONE',  ( 0.000000000000000000, 0.000000000000000000, -1.000000000000000000 ) ) ;
#4990=DIRECTION ( 'NONE',  ( 0.000000000000000000, 0.000000000000000000, -1.000000000000000000 ) ) ;
#4993=CARTESIAN_POINT ( 'NONE',  ( 7.000000000000000000, -31.30000000000045191, -8.900000000000430234 ) ) ;
#4998=CYLINDRICAL_SURFACE ( 'NONE', #56408, 0.5000000000009441337 ) ;
#5011=DIRECTION ( 'NONE',  ( 0.7071067811865480168, 0.7071067811865470176, 0.000000000000000000 ) ) ;
#5029=ORIENTED_EDGE ( 'NONE', *, *, #51056, .F. ) ;
#5060=PLANE ( 'NONE',  #34492 ) ;
#5064=AXIS2_PLACEMENT_3D ( 'NONE', #41643, #31407, #20081 ) ;
#5067=EDGE_LOOP ( 'NONE', ( #27138, #45544, #17339, #51747, #16203 ) ) ;
#5095=ORIENTED_EDGE ( 'NONE', *, *, #35435, .T. ) ;
#5096=LINE ( 'NONE', #26667, #26843 ) ;
#5098=VECTOR ( 'NONE', #39583, 1000.000000000000000 ) ;
#5108=VECTOR ( 'NONE', #26798, 1000.000000000000000 ) ;
#5109=AXIS2_PLACEMENT_3D ( 'NONE', #31128, #19447, #62945 ) ;
#5110=ORIENTED_EDGE ( 'NONE', *, *, #12381, .T. ) ;
#5124=CARTESIAN_POINT ( 'NONE',  ( 0.5000000000000000000, -0.5000000000000000000, -27.00000000000000000 ) ) ;
#5132=CYLINDRICAL_SURFACE ( 'NONE', #50097, 0.5000000000009372503 ) ;
#5165=EDGE_CURVE ( 'NONE', #16165, #26713, #20778, .T. ) ;
#5179=EDGE_CURVE ( 'NONE', #31769, #62248, #69584, .T. ) ;
#5193=DIRECTION ( 'NONE',  ( 1.000000000000000000, -0.000000000000000000, -0.000000000000000000 ) ) ;
#5202=EDGE_CURVE ( 'NONE', #50939, #37548, #15826, .T. ) ;
#5204=VECTOR ( 'NONE', #40108, 1000.000000000000000 ) ;
#5210=EDGE_CURVE ( 'NONE', #28379, #36190, #44593, .T. ) ;
#5218=AXIS2_PLACEMENT_3D ( 'NONE', #41926, #20361, #63508 ) ;
#5229=ORIENTED_EDGE ( 'NONE', *, *, #69960, .T. ) ;
#5247=CARTESIAN_POINT ( 'NONE',  ( 283.0000000000000568, -25.60000000000000142, -15.10000000000000142 ) ) ;
#5256=EDGE_CURVE ( 'NONE', #1599, #61271, #28167, .T. ) ;
#5262=ORIENTED_EDGE ( 'NONE', *, *, #29993, .F. ) ;
#5286=DIRECTION ( 'NONE',  ( 0.000000000000000000, 0.000000000000000000, 1.000000000000000000 ) ) ;
#5293=DIRECTION ( 'NONE',  ( 0.5773502691896257311, -0.5773502691896257311, -0.5773502691896257311 ) ) ;
#5295=ORIENTED_EDGE ( 'NONE', *, *, #62799, .T. ) ;
#5307=AXIS2_PLACEMENT_3D ( 'NONE', #19057, #45932, #7042 ) ;
#5319=LINE ( 'NONE', #26881, #26818 ) ;
#5327=CARTESIAN_POINT ( 'NONE',  ( 10.47821035407136137, -25.18021646000299540, 17.31978353999700460 ) ) ;
#5357=DIRECTION ( 'NONE',  ( 1.000000000000000000, -0.000000000000000000, -0.000000000000000000 ) ) ;
#5360=DIRECTION ( 'NONE',  ( 0.000000000000000000, 0.000000000000000000, 1.000000000000000000 ) ) ;
#5363=AXIS2_PLACEMENT_3D ( 'NONE', #52937, #4485, #9079 ) ;
#5370=VECTOR ( 'NONE', #21761, 1000.000000000000114 ) ;
#5371=DIRECTION ( 'NONE',  ( 0.000000000000000000, 1.000000000000000000, 0.000000000000000000 ) ) ;
#5381=ORIENTED_EDGE ( 'NONE', *, *, #24597, .F. ) ;
#5383=DIRECTION ( 'NONE',  ( 0.000000000000000000, -0.7075494706728322480, 0.7066638143775262337 ) ) ;
#5403=CARTESIAN_POINT ( 'NONE',  ( 275.0000000000000000, -41.99999999999906208, -14.49999999999903899 ) ) ;
#5424=ORIENTED_EDGE ( 'NONE', *, *, #68240, .T. ) ;
#5432=EDGE_LOOP ( 'NONE', ( #41029, #66035, #12162, #13730, #68902, #33731, #1269, #59984, #38672 ) ) ;
#5435=VERTEX_POINT ( 'NONE', #21826 ) ;
#5437=LINE ( 'NONE', #48551, #16713 ) ;
#5452=EDGE_LOOP ( 'NONE', ( #30410, #1916, #40791, #41088, #41742, #37734 ) ) ;
#5456=DIRECTION ( 'NONE',  ( 1.000000000000000000, 0.000000000000000000, 0.000000000000000000 ) ) ;
#5477=ADVANCED_FACE ( 'NONE', ( #18241 ), #61022, .F. ) ;
#5501=VERTEX_POINT ( 'NONE', #23902 ) ;
#5509=CARTESIAN_POINT ( 'NONE',  ( 14.50000000000000000, -42.50000000000000000, 15.10000000000000142 ) ) ;
#5533=CARTESIAN_POINT ( 'NONE',  ( 0.2500000000000124345, -0.2499999999999875933, -26.74999999999999289 ) ) ;
#5536=ORIENTED_EDGE ( 'NONE', *, *, #53905, .F. ) ;
#5547=ORIENTED_EDGE ( 'NONE', *, *, #25288, .F. ) ;
#5549=EDGE_CURVE ( 'NONE', #21753, #59333, #30610, .T. ) ;
#5556=VECTOR ( 'NONE', #68758, 1000.000000000000000 ) ;
#5560=DIRECTION ( 'NONE',  ( 1.000000000000000000, -0.000000000000000000, -0.000000000000000000 ) ) ;
#5564=EDGE_CURVE ( 'NONE', #18299, #36802, #4793, .T. ) ;
#5567=CARTESIAN_POINT ( 'NONE',  ( 15.00000000000000000, 0.000000000000000000, 0.000000000000000000 ) ) ;
#5575=EDGE_CURVE ( 'NONE', #35722, #52775, #46861, .T. ) ;
#5632=CARTESIAN_POINT ( 'NONE',  ( 7.000000000000000000, -26.42999999999999972, -9.412893218813501051 ) ) ;
#5639=ORIENTED_EDGE ( 'NONE', *, *, #63017, .F. ) ;
#5647=ORIENTED_EDGE ( 'NONE', *, *, #48646, .F. ) ;
#5653=ORIENTED_EDGE ( 'NONE', *, *, #14984, .F. ) ;
#5655=CARTESIAN_POINT ( 'NONE',  ( 14.50000000000000000, -42.50000000000000000, -26.50000000000000000 ) ) ;
#5658=CARTESIAN_POINT ( 'NONE',  ( 0.000000000000000000, -42.00000000000000000, -26.50000000000000000 ) ) ;
#5699=DIRECTION ( 'NONE',  ( -1.000000000000000000, 0.000000000000000000, 0.000000000000000000 ) ) ;
#5705=DIRECTION ( 'NONE',  ( 0.000000000000000000, 0.000000000000000000, 1.000000000000000000 ) ) ;
#5708=VERTEX_POINT ( 'NONE', #65576 ) ;
#5715=DIRECTION ( 'NONE',  ( 1.000000000000000000, 0.000000000000000000, 0.000000000000000000 ) ) ;
#5722=VECTOR ( 'NONE', #54210, 1000.000000000000000 ) ;
#5743=EDGE_CURVE ( 'NONE', #12124, #56899, #37669, .T. ) ;
#5751=ORIENTED_EDGE ( 'NONE', *, *, #23728, .T. ) ;
#5774=CARTESIAN_POINT ( 'NONE',  ( 283.0000000000000568, -25.56180396883900130, 14.25872597390799967 ) ) ;
#5816=FACE_OUTER_BOUND ( 'NONE', #69491, .T. ) ;
#5849=DIRECTION ( 'NONE',  ( 1.000000000000000000, -0.000000000000000000, -0.000000000000000000 ) ) ;
#5850=DIRECTION ( 'NONE',  ( -1.000000000000000000, 0.000000000000000000, 0.000000000000000000 ) ) ;
#5852=VECTOR ( 'NONE', #61519, 1000.000000000000000 ) ;
#5866=VECTOR ( 'NONE', #15628, 1000.000000000000000 ) ;
#5875=EDGE_CURVE ( 'NONE', #25678, #25149, #29475, .T. ) ;
#5885=CARTESIAN_POINT ( 'NONE',  ( 275.5000000000000000, -42.50000000000000000, 30.09999999999999787 ) ) ;
#5945=DIRECTION ( 'NONE',  ( 0.000000000000000000, -1.000000000000000000, 0.000000000000000000 ) ) ;
#5954=CARTESIAN_POINT ( 'NONE',  ( 275.0000000000000000, -20.50000000000000000, 17.00000000000000000 ) ) ;
#5955=ORIENTED_EDGE ( 'NONE', *, *, #49483, .T. ) ;
#5965=FACE_OUTER_BOUND ( 'NONE', #47364, .T. ) ;
#5986=ORIENTED_EDGE ( 'NONE', *, *, #7426, .T. ) ;
#5994=CARTESIAN_POINT ( 'NONE',  ( 7.000000000000000000, -25.60000000000000142, -17.60000000000000142 ) ) ;
#5995=ORIENTED_EDGE ( 'NONE', *, *, #30212, .T. ) ;
#5997=CYLINDRICAL_SURFACE ( 'NONE', #67335, 3.999999999999993339 ) ;
#6015=AXIS2_PLACEMENT_3D ( 'NONE', #32065, #10837, #20750 ) ;
#6019=EDGE_CURVE ( 'NONE', #6255, #63002, #2285, .T. ) ;
#6022=CARTESIAN_POINT ( 'NONE',  ( 283.0000000000000568, -26.50000000000000000, 9.080000000000000071 ) ) ;
#6031=DIRECTION ( 'NONE',  ( 0.000000000000000000, 0.000000000000000000, -1.000000000000000000 ) ) ;
#6076=ORIENTED_EDGE ( 'NONE', *, *, #29983, .T. ) ;
#6089=LINE ( 'NONE', #49230, #66845 ) ;
#6132=CIRCLE ( 'NONE', #18523, 0.5000000000009372503 ) ;
#6140=DIRECTION ( 'NONE',  ( 1.000000000000000000, -0.000000000000000000, -0.000000000000000000 ) ) ;
#6142=ORIENTED_EDGE ( 'NONE', *, *, #50305, .T. ) ;
#6157=FACE_OUTER_BOUND ( 'NONE', #19128, .T. ) ;
#6161=PLANE ( 'NONE',  #63860 ) ;
#6165=EDGE_CURVE ( 'NONE', #52181, #59688, #38287, .T. ) ;
#6172=EDGE_CURVE ( 'NONE', #18944, #57384, #3453, .T. ) ;
#6196=DIRECTION ( 'NONE',  ( 1.000000000000000000, 0.000000000000000000, 0.000000000000000000 ) ) ;
#6200=VECTOR ( 'NONE', #61145, 1000.000000000000000 ) ;
#6209=AXIS2_PLACEMENT_3D ( 'NONE', #16940, #1037, #6663 ) ;
#6211=FACE_OUTER_BOUND ( 'NONE', #59346, .T. ) ;
#6226=ORIENTED_EDGE ( 'NONE', *, *, #68431, .T. ) ;
#6255=VERTEX_POINT ( 'NONE', #67499 ) ;
#6264=VECTOR ( 'NONE', #58673, 1000.000000000000000 ) ;
#6273=ORIENTED_EDGE ( 'NONE', *, *, #58140, .T. ) ;
#6276=CARTESIAN_POINT ( 'NONE',  ( 7.000000000000000000, -25.93000000000544958, -9.412893218815410634 ) ) ;
#6291=EDGE_CURVE ( 'NONE', #56517, #39731, #2432, .T. ) ;
#6294=ORIENTED_EDGE ( 'NONE', *, *, #40134, .F. ) ;
#6306=CIRCLE ( 'NONE', #45819, 0.2500000000000002220 ) ;
#6308=CARTESIAN_POINT ( 'NONE',  ( 283.0000000000000568, -42.50000000000000000, -7.500000000000000000 ) ) ;
#6337=DIRECTION ( 'NONE',  ( -1.000000000000000000, 0.000000000000000000, 0.000000000000000000 ) ) ;
#6343=DIRECTION ( 'NONE',  ( -1.000000000000000000, 0.000000000000000000, 0.000000000000000000 ) ) ;
#6345=LINE ( 'NONE', #22606, #69356 ) ;
#6347=ORIENTED_EDGE ( 'NONE', *, *, #68038, .T. ) ;
#6349=EDGE_CURVE ( 'NONE', #65495, #38703, #19387, .T. ) ;
#6357=CIRCLE ( 'NONE', #43604, 0.5000000000004236611 ) ;
#6370=VECTOR ( 'NONE', #27754, 1000.000000000000114 ) ;
#6375=ADVANCED_FACE ( 'NONE', ( #57227 ), #20446, .F. ) ;
#6404=CARTESIAN_POINT ( 'NONE',  ( 275.0000000000000000, -25.50000000000000355, -14.74860679774999994 ) ) ;
#6446=CARTESIAN_POINT ( 'NONE',  ( 7.000000000000000000, -25.60000000000000142, 17.60000000000000142 ) ) ;
#6448=MECHANICAL_DESIGN_GEOMETRIC_PRESENTATION_REPRESENTATION('',(#51559),#45951);
#6470=VECTOR ( 'NONE', #6337, 1000.000000000000000 ) ;
#6476=LINE ( 'NONE', #28370, #15706 ) ;
#6495=DIRECTION ( 'NONE',  ( 0.000000000000000000, 0.000000000000000000, -1.000000000000000000 ) ) ;
#6499=EDGE_CURVE ( 'NONE', #11348, #54703, #48715, .T. ) ;
#6501=LINE ( 'NONE', #26675, #66932 ) ;
#6520=ORIENTED_EDGE ( 'NONE', *, *, #27290, .F. ) ;
#6523=FACE_OUTER_BOUND ( 'NONE', #51360, .T. ) ;
#6524=LINE ( 'NONE', #22086, #31905 ) ;
#6527=VERTEX_POINT ( 'NONE', #22193 ) ;
#6538=VERTEX_POINT ( 'NONE', #60004 ) ;
#6542=CARTESIAN_POINT ( 'NONE',  ( 289.7499999999998863, -42.24999999999996447, 26.75000000000004619 ) ) ;
#6545=LINE ( 'NONE', #200, #6370 ) ;
#6552=DIRECTION ( 'NONE',  ( 1.000000000000000000, 0.000000000000000000, 0.000000000000000000 ) ) ;
#6563=VECTOR ( 'NONE', #63837, 1000.000000000000000 ) ;
#6599=DIRECTION ( 'NONE',  ( -1.000000000000000000, 0.000000000000000000, 0.000000000000000000 ) ) ;
#6615=AXIS2_PLACEMENT_3D ( 'NONE', #37450, #36753, #19509 ) ;
#6640=DIRECTION ( 'NONE',  ( 0.000000000000000000, 0.7071067811865474617, -0.7071067811865474617 ) ) ;
#6648=DIRECTION ( 'NONE',  ( 0.000000000000000000, 0.000000000000000000, -1.000000000000000000 ) ) ;
#6661=CARTESIAN_POINT ( 'NONE',  ( 283.0000000000000568, -32.44999999999905071, 14.49999999999906031 ) ) ;
#6663=DIRECTION ( 'NONE',  ( 0.000000000000000000, 0.000000000000000000, -1.000000000000000000 ) ) ;
#6667=LINE ( 'NONE', #22933, #116 ) ;
#6675=EDGE_CURVE ( 'NONE', #9656, #1005, #9053, .T. ) ;
#6717=CARTESIAN_POINT ( 'NONE',  ( 283.0000000000000568, -38.65000000000095781, -13.20000000000094253 ) ) ;
#6724=EDGE_CURVE ( 'NONE', #12315, #57464, #13302, .T. ) ;
#6739=DIRECTION ( 'NONE',  ( 0.000000000000000000, 0.7840980155806945850, 0.6206370130458033207 ) ) ;
#6740=ORIENTED_EDGE ( 'NONE', *, *, #1405, .F. ) ;
#6758=VECTOR ( 'NONE', #18895, 1000.000000000000000 ) ;
#6760=CYLINDRICAL_SURFACE ( 'NONE', #8625, 5.000000000000000000 ) ;
#6762=DIRECTION ( 'NONE',  ( -1.000000000000000000, 0.000000000000000000, 0.000000000000000000 ) ) ;
#6763=ORIENTED_EDGE ( 'NONE', *, *, #21267, .T. ) ;
#6783=FACE_OUTER_BOUND ( 'NONE', #36535, .T. ) ;
#6800=ORIENTED_EDGE ( 'NONE', *, *, #195, .T. ) ;
#6804=CARTESIAN_POINT ( 'NONE',  ( 283.0000000000000568, -31.30000000000045191, 8.400000000000000355 ) ) ;
#6810=EDGE_LOOP ( 'NONE', ( #29839, #1979, #65178, #37240 ) ) ;
#6820=DIRECTION ( 'NONE',  ( 0.000000000000000000, 0.7071067811865076047, -0.7071067811865875408 ) ) ;
#6825=LINE ( 'NONE', #29437, #17056 ) ;
#6831=CARTESIAN_POINT ( 'NONE',  ( 283.0000000000000568, -20.50000000000000000, -13.00000000000000178 ) ) ;
#6840=VECTOR ( 'NONE', #18217, 1000.000000000000000 ) ;
#6842=ORIENTED_EDGE ( 'NONE', *, *, #14984, .T. ) ;
#6843=CARTESIAN_POINT ( 'NONE',  ( 283.0000000000000568, -26.50000000000000000, 0.5000000000000000000 ) ) ;
#6851=ORIENTED_EDGE ( 'NONE', *, *, #62341, .F. ) ;
#6859=ORIENTED_EDGE ( 'NONE', *, *, #39692, .T. ) ;
#6860=FACE_OUTER_BOUND ( 'NONE', #50682, .T. ) ;
#6865=CARTESIAN_POINT ( 'NONE',  ( 283.0000000000000568, -42.50000000000000000, 9.950000000000001066 ) ) ;
#6974=CARTESIAN_POINT ( 'NONE',  ( 275.0000000000000000, -25.60000000000000142, -17.60000000000000142 ) ) ;
#6977=LINE ( 'NONE', #49449, #36035 ) ;
#7001=FACE_OUTER_BOUND ( 'NONE', #12507, .T. ) ;
#7013=EDGE_CURVE ( 'NONE', #66290, #26713, #1279, .T. ) ;
#7015=DIRECTION ( 'NONE',  ( 0.000000000000000000, 1.000000000000000000, 0.000000000000000000 ) ) ;
#7033=ORIENTED_EDGE ( 'NONE', *, *, #32037, .T. ) ;
#7035=FACE_OUTER_BOUND ( 'NONE', #49035, .T. ) ;
#7042=DIRECTION ( 'NONE',  ( 0.000000000000000000, 0.000000000000000000, 1.000000000000000000 ) ) ;
#7049=LINE ( 'NONE', #1751, #34754 ) ;
#7051=FACE_OUTER_BOUND ( 'NONE', #16173, .T. ) ;
#7061=VERTEX_POINT ( 'NONE', #27759 ) ;
#7064=EDGE_CURVE ( 'NONE', #11694, #21614, #27064, .T. ) ;
#7066=EDGE_CURVE ( 'NONE', #30690, #3076, #69067, .T. ) ;
#7071=ADVANCED_FACE ( 'NONE', ( #911 ), #28434, .T. ) ;
#7095=LINE ( 'NONE', #12060, #18393 ) ;
#7118=ORIENTED_EDGE ( 'NONE', *, *, #1487, .T. ) ;
#7121=VECTOR ( 'NONE', #38621, 1000.000000000000000 ) ;
#7123=EDGE_CURVE ( 'NONE', #10609, #52775, #62006, .T. ) ;
#7135=CARTESIAN_POINT ( 'NONE',  ( 283.0000000000000568, -20.85424868893542083, 17.35424868893542083 ) ) ;
#7138=CARTESIAN_POINT ( 'NONE',  ( 0.5000000000000000000, 0.000000000000000000, 30.00000000000000000 ) ) ;
#7191=ADVANCED_FACE ( 'NONE', ( #45042, #51763, #66619 ), #30193, .F. ) ;
#7198=ORIENTED_EDGE ( 'NONE', *, *, #19421, .F. ) ;
#7206=EDGE_CURVE ( 'NONE', #69116, #35743, #62354, .T. ) ;
#7211=DIRECTION ( 'NONE',  ( -1.000000000000000000, 0.000000000000000000, 0.000000000000000000 ) ) ;
#7221=( BOUNDED_CURVE ( )  B_SPLINE_CURVE ( 3, ( #38405, #33092, #55362, #27789 ),
 .UNSPECIFIED., .F., .F. ) 
 B_SPLINE_CURVE_WITH_KNOTS ( ( 4, 4 ),
 ( 5.435123228198102119, 5.560451059366170234 ),
 .UNSPECIFIED. ) 
 CURVE ( )  GEOMETRIC_REPRESENTATION_ITEM ( )  RATIONAL_B_SPLINE_CURVE ( ( 1.000000000000000000, 0.9986915061577686936, 0.9986915061577686936, 1.000000000000000000 ) ) 
 REPRESENTATION_ITEM ( '' )  );
#7227=DIRECTION ( 'NONE',  ( 0.000000000000000000, -1.000000000000000000, 0.000000000000000000 ) ) ;
#7228=DIRECTION ( 'NONE',  ( 0.000000000000000000, -0.6787500000000000755, -0.7343694148723788340 ) ) ;
#7230=EDGE_CURVE ( 'NONE', #749, #62902, #57054, .T. ) ;
#7243=DIRECTION ( 'NONE',  ( 0.000000000000000000, 0.000000000000000000, 1.000000000000000000 ) ) ;
#7248=PLANE ( 'NONE',  #11338 ) ;
#7260=EDGE_CURVE ( 'NONE', #17425, #39081, #47166, .T. ) ;
#7278=PLANE ( 'NONE',  #47044 ) ;
#7289=DIRECTION ( 'NONE',  ( 0.000000000000000000, 0.000000000000000000, 1.000000000000000000 ) ) ;
#7298=CIRCLE ( 'NONE', #15212, 0.4999999999945534124 ) ;
#7309=FACE_OUTER_BOUND ( 'NONE', #20979, .T. ) ;
#7310=EDGE_CURVE ( 'NONE', #15923, #26457, #35843, .T. ) ;
#7321=FACE_OUTER_BOUND ( 'NONE', #19121, .T. ) ;
#7341=ORIENTED_EDGE ( 'NONE', *, *, #15534, .F. ) ;
#7346=EDGE_CURVE ( 'NONE', #69782, #15754, #67576, .T. ) ;
#7357=VECTOR ( 'NONE', #55354, 1000.000000000000000 ) ;
#7372=EDGE_CURVE ( 'NONE', #2050, #19031, #66856, .T. ) ;
#7374=CARTESIAN_POINT ( 'NONE',  ( 283.0000000000000568, -31.99999999999889866, 7.899999999997660893 ) ) ;
#7398=VECTOR ( 'NONE', #3914, 1000.000000000000000 ) ;
#7402=AXIS2_PLACEMENT_3D ( 'NONE', #67744, #24262, #7289 ) ;
#7426=EDGE_CURVE ( 'NONE', #17601, #35918, #40693, .T. ) ;
#7445=VECTOR ( 'NONE', #67074, 1000.000000000000000 ) ;
#7467=VERTEX_POINT ( 'NONE', #56260 ) ;
#7471=EDGE_CURVE ( 'NONE', #16868, #53126, #62253, .T. ) ;
#7477=CARTESIAN_POINT ( 'NONE',  ( 283.0000000000000568, -32.45000000000000995, 15.00000000000000000 ) ) ;
#7488=DIRECTION ( 'NONE',  ( 1.000000000000000000, -0.000000000000000000, -0.000000000000000000 ) ) ;
#7508=ORIENTED_EDGE ( 'NONE', *, *, #50298, .F. ) ;
#7531=ORIENTED_EDGE ( 'NONE', *, *, #57006, .F. ) ;
#7534=LINE ( 'NONE', #39707, #26692 ) ;
#7562=EDGE_CURVE ( 'NONE', #57384, #12410, #31154, .T. ) ;
#7582=CYLINDRICAL_SURFACE ( 'NONE', #2951, 0.4999999999979777288 ) ;
#7603=CARTESIAN_POINT ( 'NONE',  ( 10.47821035407136314, -25.18021646000299896, -17.31978353999700460 ) ) ;
#7613=EDGE_CURVE ( 'NONE', #13015, #341, #27036, .T. ) ;
#7616=CARTESIAN_POINT ( 'NONE',  ( 283.0000000000000568, -39.80000000000000426, 12.69999999999999929 ) ) ;
#7638=VERTEX_POINT ( 'NONE', #42790 ) ;
#7642=ORIENTED_EDGE ( 'NONE', *, *, #54549, .T. ) ;
#7643=AXIS2_PLACEMENT_3D ( 'NONE', #58823, #47845, #3674 ) ;
#7649=VECTOR ( 'NONE', #35411, 1000.000000000000114 ) ;
#7653=EDGE_CURVE ( 'NONE', #68084, #44582, #4971, .T. ) ;
#7665=ADVANCED_FACE ( 'NONE', ( #29201 ), #50082, .F. ) ;
#7681=DIRECTION ( 'NONE',  ( -0.7071067811865460184, 0.000000000000000000, -0.7071067811865489050 ) ) ;
#7691=EDGE_LOOP ( 'NONE', ( #1833, #31271, #4728, #19873, #32014, #32358, #69329, #18586, #42810, #2019, #5110, #8489, #66936, #45028, #41578, #49822, #68741, #32976, #60976, #43725, #1215, #63254, #21573, #46297, #55528, #22805, #33279, #66851, #47135, #25446, #68879, #26343, #45155, #31721, #11547 ) ) ;
#7701=DIRECTION ( 'NONE',  ( 0.000000000000000000, 1.000000000000000000, 8.604228440837611257E-13 ) ) ;
#7724=ORIENTED_EDGE ( 'NONE', *, *, #7260, .T. ) ;
#7734=EDGE_CURVE ( 'NONE', #29731, #54503, #64389, .T. ) ;
#7761=DIRECTION ( 'NONE',  ( -1.000000000000000000, 0.000000000000000000, 0.000000000000000000 ) ) ;
#7773=EDGE_CURVE ( 'NONE', #8637, #36514, #7979, .T. ) ;
#7774=DIRECTION ( 'NONE',  ( 0.000000000000000000, 0.000000000000000000, -1.000000000000000000 ) ) ;
#7784=ORIENTED_EDGE ( 'NONE', *, *, #61279, .T. ) ;
#7802=VECTOR ( 'NONE', #30288, 1000.000000000000000 ) ;
#7803=CARTESIAN_POINT ( 'NONE',  ( 283.0000000000000568, -20.50000000000000000, -13.00000000000000178 ) ) ;
#7823=DIRECTION ( 'NONE',  ( 0.000000000000000000, 0.000000000000000000, 1.000000000000000000 ) ) ;
#7828=DIRECTION ( 'NONE',  ( -1.000000000000000000, 0.000000000000000000, 0.000000000000000000 ) ) ;
#7829=CARTESIAN_POINT ( 'NONE',  ( 275.0000000000000000, -0.5000000000000000000, 26.50000000000000000 ) ) ;
#7836=VECTOR ( 'NONE', #34217, 1000.000000000000000 ) ;
#7838=ORIENTED_EDGE ( 'NONE', *, *, #53709, .F. ) ;
#7854=DIRECTION ( 'NONE',  ( 0.000000000000000000, -1.000000000000000000, 0.000000000000000000 ) ) ;
#7874=DIRECTION ( 'NONE',  ( 1.000000000000000000, 0.000000000000000000, 0.000000000000000000 ) ) ;
#7915=VECTOR ( 'NONE', #22392, 1000.000000000000000 ) ;
#7940=CARTESIAN_POINT ( 'NONE',  ( 15.00000000000002132, -0.4999999999999964473, -26.50000000000003197 ) ) ;
#7943=EDGE_CURVE ( 'NONE', #46313, #55046, #26716, .T. ) ;
#7944=CARTESIAN_POINT ( 'NONE',  ( 10.62249899919920004, -25.00000000000000000, -17.50000000000000000 ) ) ;
#7958=DIRECTION ( 'NONE',  ( 0.000000000000000000, 0.000000000000000000, -1.000000000000000000 ) ) ;
#7976=ORIENTED_EDGE ( 'NONE', *, *, #27621, .T. ) ;
#7979=LINE ( 'NONE', #20, #14657 ) ;
#7990=AXIS2_PLACEMENT_3D ( 'NONE', #56901, #9180, #35324 ) ;
#8002=EDGE_LOOP ( 'NONE', ( #39884, #61912, #50546 ) ) ;
#8022=VERTEX_POINT ( 'NONE', #53592 ) ;
#8029=VECTOR ( 'NONE', #23058, 1000.000000000000114 ) ;
#8032=AXIS2_PLACEMENT_3D ( 'NONE', #66193, #67235, #7823 ) ;
#8055=CIRCLE ( 'NONE', #2417, 0.2999999999994933386 ) ;
#8058=VERTEX_POINT ( 'NONE', #42966 ) ;
#8068=AXIS2_PLACEMENT_3D ( 'NONE', #1566, #48632, #202 ) ;
#8091=DIRECTION ( 'NONE',  ( 0.000000000000000000, 0.000000000000000000, 1.000000000000000000 ) ) ;
#8092=EDGE_CURVE ( 'NONE', #27791, #68548, #17834, .T. ) ;
#8128=DIRECTION ( 'NONE',  ( 1.000000000000000000, 0.000000000000000000, 0.000000000000000000 ) ) ;
#8136=DIRECTION ( 'NONE',  ( 0.000000000000000000, 0.000000000000000000, -1.000000000000000000 ) ) ;
#8139=ADVANCED_FACE ( 'NONE', ( #6860 ), #1232, .T. ) ;
#8146=ORIENTED_EDGE ( 'NONE', *, *, #15835, .T. ) ;
#8164=DIRECTION ( 'NONE',  ( -1.000000000000000000, 0.000000000000000000, 0.000000000000000000 ) ) ;
#8173=CARTESIAN_POINT ( 'NONE',  ( 283.0000000000000568, -42.50000000000000000, -14.50000000000000000 ) ) ;
#8179=LINE ( 'NONE', #24097, #49269 ) ;
#8187=ORIENTED_EDGE ( 'NONE', *, *, #23177, .F. ) ;
#8191=DIRECTION ( 'NONE',  ( -1.000000000000000000, 0.000000000000000000, 0.000000000000000000 ) ) ;
#8212=CARTESIAN_POINT ( 'NONE',  ( 283.0000000000000568, -23.65000000000000568, 12.40000000000000213 ) ) ;
#8219=ADVANCED_FACE ( 'NONE', ( #40793 ), #51396, .T. ) ;
#8227=LINE ( 'NONE', #30155, #52409 ) ;
#8228=CARTESIAN_POINT ( 'NONE',  ( 10.14575131106465378, -25.50000000000000355, -17.00000000000000000 ) ) ;
#8230=CARTESIAN_POINT ( 'NONE',  ( 275.0000000000000000, -21.00000000000000000, 0.000000000000000000 ) ) ;
#8235=ORIENTED_EDGE ( 'NONE', *, *, #33503, .T. ) ;
#8245=CARTESIAN_POINT ( 'NONE',  ( 283.0000000000000568, -20.50000000000000000, -17.00000000000000000 ) ) ;
#8246=ORIENTED_EDGE ( 'NONE', *, *, #31685, .F. ) ;
#8263=CIRCLE ( 'NONE', #44390, 8.000000000000000000 ) ;
#8268=LINE ( 'NONE', #13584, #24426 ) ;
#8283=CARTESIAN_POINT ( 'NONE',  ( 7.000000000000000000, -32.44999999999905071, 13.20000000000091944 ) ) ;
#8290=EDGE_CURVE ( 'NONE', #44995, #5708, #46442, .T. ) ;
#8297=ADVANCED_FACE ( 'NONE', ( #8608 ), #30534, .F. ) ;
#8319=VECTOR ( 'NONE', #46699, 1000.000000000000000 ) ;
#8330=VERTEX_POINT ( 'NONE', #56703 ) ;
#8341=EDGE_CURVE ( 'NONE', #20615, #49129, #63299, .T. ) ;
#8358=CARTESIAN_POINT ( 'NONE',  ( 10.70000000000000107, -53.81370849898476649, -17.60000000000000142 ) ) ;
#8366=EDGE_CURVE ( 'NONE', #13089, #69122, #63770, .T. ) ;
#8383=FACE_OUTER_BOUND ( 'NONE', #23362, .T. ) ;
#8388=ORIENTED_EDGE ( 'NONE', *, *, #18627, .F. ) ;
#8402=PLANE ( 'NONE',  #50218 ) ;
#8410=ORIENTED_EDGE ( 'NONE', *, *, #69729, .T. ) ;
#8424=EDGE_CURVE ( 'NONE', #15754, #66149, #26634, .T. ) ;
#8425=VECTOR ( 'NONE', #14156, 1000.000000000000000 ) ;
#8441=DIRECTION ( 'NONE',  ( 0.000000000000000000, 0.000000000000000000, 1.000000000000000000 ) ) ;
#8466=DIRECTION ( 'NONE',  ( -1.000000000000000000, 0.000000000000000000, 0.000000000000000000 ) ) ;
#8482=LINE ( 'NONE', #68243, #47937 ) ;
#8489=ORIENTED_EDGE ( 'NONE', *, *, #11009, .F. ) ;
#8493=DIRECTION ( 'NONE',  ( -1.000000000000000000, 0.000000000000000000, 0.000000000000000000 ) ) ;
#8509=ORIENTED_EDGE ( 'NONE', *, *, #15425, .T. ) ;
#8516=ORIENTED_EDGE ( 'NONE', *, *, #59187, .F. ) ;
#8523=FACE_OUTER_BOUND ( 'NONE', #4381, .T. ) ;
#8530=LINE ( 'NONE', #48133, #15470 ) ;
#8543=CARTESIAN_POINT ( 'NONE',  ( 283.0000000000000568, -30.45000000000000639, 15.00000000000000000 ) ) ;
#8544=LINE ( 'NONE', #3254, #32968 ) ;
#8555=VECTOR ( 'NONE', #53976, 1000.000000000000000 ) ;
#8558=VERTEX_POINT ( 'NONE', #1147 ) ;
#8585=CARTESIAN_POINT ( 'NONE',  ( 0.5000000000000000000, -42.00000000000000000, 27.00000000000000000 ) ) ;
#8586=DIRECTION ( 'NONE',  ( -0.5773502691896257311, -0.5773502691896257311, 0.5773502691896257311 ) ) ;
#8590=ORIENTED_EDGE ( 'NONE', *, *, #56994, .F. ) ;
#8592=CARTESIAN_POINT ( 'NONE',  ( 289.7500000000000000, -0.2499999999999944766, 26.75000000000000000 ) ) ;
#8600=ORIENTED_EDGE ( 'NONE', *, *, #69921, .F. ) ;
#8602=VERTEX_POINT ( 'NONE', #23045 ) ;
#8608=FACE_OUTER_BOUND ( 'NONE', #58835, .T. ) ;
#8613=PLANE ( 'NONE',  #19885 ) ;
#8618=DIRECTION ( 'NONE',  ( 0.000000000000000000, 0.000000000000000000, -1.000000000000000000 ) ) ;
#8620=LINE ( 'NONE', #57056, #14353 ) ;
#8623=VECTOR ( 'NONE', #29750, 1000.000000000000114 ) ;
#8625=AXIS2_PLACEMENT_3D ( 'NONE', #17729, #33643, #61184 ) ;
#8634=VECTOR ( 'NONE', #31269, 1000.000000000000114 ) ;
#8636=CARTESIAN_POINT ( 'NONE',  ( 7.000000000000000000, -20.40000000000000213, -12.40000000000000213 ) ) ;
#8637=VERTEX_POINT ( 'NONE', #35384 ) ;
#8649=CARTESIAN_POINT ( 'NONE',  ( 275.0000000000000000, -23.70411739045900390, -12.50000000000000000 ) ) ;
#8651=CARTESIAN_POINT ( 'NONE',  ( 10.62249899919920004, -25.00000000000000000, -17.50000000000000000 ) ) ;
#8660=AXIS2_PLACEMENT_3D ( 'NONE', #59563, #28076, #53566 ) ;
#8667=ORIENTED_EDGE ( 'NONE', *, *, #47840, .T. ) ;
#8681=VECTOR ( 'NONE', #9059, 1000.000000000000114 ) ;
#8698=CARTESIAN_POINT ( 'NONE',  ( 282.6457513110646005, -20.50000000000000000, 17.00000000000000000 ) ) ;
#8702=DIRECTION ( 'NONE',  ( 0.000000000000000000, 1.000000000000000000, 0.000000000000000000 ) ) ;
#8710=CARTESIAN_POINT ( 'NONE',  ( 283.0000000000000568, -32.95000000000000284, -13.19999999999999929 ) ) ;
#8713=EDGE_CURVE ( 'NONE', #3514, #17105, #2869, .T. ) ;
#8737=DIRECTION ( 'NONE',  ( 0.000000000000000000, -1.000000000000000000, 0.000000000000000000 ) ) ;
#8749=DIRECTION ( 'NONE',  ( 1.000000000000000000, 0.000000000000000000, 0.000000000000000000 ) ) ;
#8767=CIRCLE ( 'NONE', #32507, 3.999999999999993339 ) ;
#8775=AXIS2_PLACEMENT_3D ( 'NONE', #5567, #20424, #10862 ) ;
#8805=CARTESIAN_POINT ( 'NONE',  ( 283.0000000000000568, -20.85424868893542083, 17.35424868893542083 ) ) ;
#8811=DIRECTION ( 'NONE',  ( 0.000000000000000000, 1.000000000000000000, 0.000000000000000000 ) ) ;
#8819=VECTOR ( 'NONE', #67548, 1000.000000000000000 ) ;
#8821=ORIENTED_EDGE ( 'NONE', *, *, #66951, .F. ) ;
#8833=DIRECTION ( 'NONE',  ( 1.000000000000000000, -0.000000000000000000, -0.000000000000000000 ) ) ;
#8866=DIRECTION ( 'NONE',  ( -1.000000000000000000, 0.000000000000000000, 0.000000000000000000 ) ) ;
#8870=LINE ( 'NONE', #14176, #42097 ) ;
#8886=PLANE ( 'NONE',  #40653 ) ;
#8899=CARTESIAN_POINT ( 'NONE',  ( 283.0000000000000568, -26.50000000000000000, 9.080000000000000071 ) ) ;
#8909=DIRECTION ( 'NONE',  ( 0.000000000000000000, 0.000000000000000000, 1.000000000000000000 ) ) ;
#8919=AXIS2_PLACEMENT_3D ( 'NONE', #62087, #28526, #12948 ) ;
#8927=VECTOR ( 'NONE', #46552, 1000.000000000000000 ) ;
#8935=ADVANCED_FACE ( 'NONE', ( #28609 ), #33575, .F. ) ;
#8963=DIRECTION ( 'NONE',  ( 0.000000000000000000, 0.7071067811865474617, -0.7071067811865474617 ) ) ;
#8968=VERTEX_POINT ( 'NONE', #11992 ) ;
#8982=FACE_OUTER_BOUND ( 'NONE', #11510, .T. ) ;
#8983=ORIENTED_EDGE ( 'NONE', *, *, #64572, .F. ) ;
#8985=CARTESIAN_POINT ( 'NONE',  ( 283.0000000000000568, -20.50000000000000000, 17.00000000000000000 ) ) ;
#9000=CARTESIAN_POINT ( 'NONE',  ( 283.0000000000000568, -23.50007830495750127, 12.58007262201399890 ) ) ;
#9005=DIRECTION ( 'NONE',  ( 0.000000000000000000, 0.7071067811865475727, -0.7071067811865475727 ) ) ;
#9032=VERTEX_POINT ( 'NONE', #6022 ) ;
#9053=LINE ( 'NONE', #45120, #17035 ) ;
#9059=DIRECTION ( 'NONE',  ( 0.000000000000000000, -0.7071067811865474617, 0.7071067811865474617 ) ) ;
#9071=CARTESIAN_POINT ( 'NONE',  ( 7.000000000000000000, -38.65000000000095781, -13.20000000000094253 ) ) ;
#9079=DIRECTION ( 'NONE',  ( 0.000000000000000000, 0.000000000000000000, -1.000000000000000000 ) ) ;
#9121=FACE_OUTER_BOUND ( 'NONE', #26367, .T. ) ;
#9144=ORIENTED_EDGE ( 'NONE', *, *, #58778, .F. ) ;
#9156=CARTESIAN_POINT ( 'NONE',  ( 282.6457513110646005, -25.50000000000000355, -17.00000000000000000 ) ) ;
#9169=LINE ( 'NONE', #40639, #25957 ) ;
#9173=ORIENTED_EDGE ( 'NONE', *, *, #2626, .T. ) ;
#9180=DIRECTION ( 'NONE',  ( 0.000000000000000000, 0.000000000000000000, 1.000000000000000000 ) ) ;
#9188=AXIS2_PLACEMENT_3D ( 'NONE', #26596, #32940, #54521 ) ;
#9190=DIRECTION ( 'NONE',  ( 0.000000000000000000, 0.000000000000000000, -1.000000000000000000 ) ) ;
#9193=FACE_OUTER_BOUND ( 'NONE', #64329, .T. ) ;
#9205=EDGE_CURVE ( 'NONE', #24682, #23628, #41311, .T. ) ;
#9206=ORIENTED_EDGE ( 'NONE', *, *, #31827, .T. ) ;
#9226=DIRECTION ( 'NONE',  ( -1.000000000000000000, 0.000000000000000000, 0.000000000000000000 ) ) ;
#9262=CARTESIAN_POINT ( 'NONE',  ( 7.000000000000000000, -25.93000000000544958, -9.412893218815410634 ) ) ;
#9263=AXIS2_PLACEMENT_3D ( 'NONE', #6865, #16459, #27413 ) ;
#9292=DIRECTION ( 'NONE',  ( -1.000000000000000000, 0.000000000000000000, 0.000000000000000000 ) ) ;
#9310=EDGE_LOOP ( 'NONE', ( #32981, #8509, #43663, #33807, #58784 ) ) ;
#9319=VERTEX_POINT ( 'NONE', #37424 ) ;
#9331=DIRECTION ( 'NONE',  ( 1.000000000000000000, 0.000000000000000000, 0.000000000000000000 ) ) ;
#9334=ADVANCED_FACE ( 'NONE', ( #53344 ), #4895, .T. ) ;
#9343=DIRECTION ( 'NONE',  ( 0.5773502691896298389, -0.5773502691896257311, 0.5773502691896216232 ) ) ;
#9353=LINE ( 'NONE', #3699, #5556 ) ;
#9372=EDGE_CURVE ( 'NONE', #33051, #37343, #66349, .T. ) ;
#9434=ADVANCED_FACE ( 'NONE', ( #33140, #55081 ), #22881, .T. ) ;
#9439=CIRCLE ( 'NONE', #33153, 0.3000000000005412781 ) ;
#9440=ORIENTED_EDGE ( 'NONE', *, *, #50782, .F. ) ;
#9442=DIRECTION ( 'NONE',  ( 0.000000000000000000, 0.000000000000000000, 1.000000000000000000 ) ) ;
#9444=EDGE_CURVE ( 'NONE', #57368, #24330, #43406, .T. ) ;
#9454=EDGE_CURVE ( 'NONE', #68361, #55546, #12597, .T. ) ;
#9465=ORIENTED_EDGE ( 'NONE', *, *, #2507, .F. ) ;
#9483=FACE_OUTER_BOUND ( 'NONE', #43480, .T. ) ;
#9489=CARTESIAN_POINT ( 'NONE',  ( 289.5000000000000000, -0.5000000000000000000, -27.00000000000000000 ) ) ;
#9497=CARTESIAN_POINT ( 'NONE',  ( 7.000000000000000000, -38.10000000000000142, 8.400000000000000355 ) ) ;
#9506=ORIENTED_EDGE ( 'NONE', *, *, #30187, .T. ) ;
#9524=( BOUNDED_CURVE ( )  B_SPLINE_CURVE ( 3, ( #59428, #38553, #54815, #69699 ),
 .UNSPECIFIED., .F., .F. ) 
 B_SPLINE_CURVE_WITH_KNOTS ( ( 4, 4 ),
 ( 0.7227342478134280990, 0.8956647938578748969 ),
 .UNSPECIFIED. ) 
 CURVE ( )  GEOMETRIC_REPRESENTATION_ITEM ( )  RATIONAL_B_SPLINE_CURVE ( ( 1.000000000000000000, 0.9975094710839675916, 0.9975094710839675916, 1.000000000000000000 ) ) 
 REPRESENTATION_ITEM ( '' )  );
#9532=DIRECTION ( 'NONE',  ( 0.000000000000000000, 0.000000000000000000, 1.000000000000000000 ) ) ;
#9549=CARTESIAN_POINT ( 'NONE',  ( 275.0000000000000000, -31.99999999999889866, 7.899999999997660893 ) ) ;
#9576=CARTESIAN_POINT ( 'NONE',  ( 283.0000000000000568, -32.46196062927499781, 8.091291340630698770 ) ) ;
#9577=ORIENTED_EDGE ( 'NONE', *, *, #25288, .T. ) ;
#9578=ORIENTED_EDGE ( 'NONE', *, *, #21127, .F. ) ;
#9588=AXIS2_PLACEMENT_3D ( 'NONE', #37193, #5371, #10644 ) ;
#9589=AXIS2_PLACEMENT_3D ( 'NONE', #34591, #50855, #2428 ) ;
#9590=DIRECTION ( 'NONE',  ( -0.5773502691896257311, -0.5773502691896257311, 0.5773502691896257311 ) ) ;
#9594=CARTESIAN_POINT ( 'NONE',  ( 275.0000000000000000, -38.15000000000000568, 13.19999999999999929 ) ) ;
#9605=VECTOR ( 'NONE', #52259, 1000.000000000000000 ) ;
#9610=DIRECTION ( 'NONE',  ( 0.000000000000000000, 1.000000000000000000, 0.000000000000000000 ) ) ;
#9617=CARTESIAN_POINT ( 'NONE',  ( 7.000000000000000000, -32.44999999999905071, 14.49999999999906031 ) ) ;
#9620=VERTEX_POINT ( 'NONE', #58828 ) ;
#9653=VECTOR ( 'NONE', #3644, 1000.000000000000000 ) ;
#9656=VERTEX_POINT ( 'NONE', #11077 ) ;
#9677=CARTESIAN_POINT ( 'NONE',  ( 280.0000000000000000, -25.50000000000000355, 20.00000000000000000 ) ) ;
#9686=ORIENTED_EDGE ( 'NONE', *, *, #11091, .T. ) ;
#9695=EDGE_CURVE ( 'NONE', #135, #19031, #63823, .T. ) ;
#9709=ORIENTED_EDGE ( 'NONE', *, *, #11207, .F. ) ;
#9711=DIRECTION ( 'NONE',  ( 0.000000000000000000, 0.000000000000000000, 1.000000000000000000 ) ) ;
#9738=CARTESIAN_POINT ( 'NONE',  ( 7.000000000000000000, -21.00000000000000000, 0.000000000000000000 ) ) ;
#9745=DIRECTION ( 'NONE',  ( -0.5773502691896257311, 0.5773502691896257311, -0.5773502691896257311 ) ) ;
#9764=LINE ( 'NONE', #20704, #41266 ) ;
#9776=DIRECTION ( 'NONE',  ( 0.000000000000000000, 0.000000000000000000, -1.000000000000000000 ) ) ;
#9779=AXIS2_PLACEMENT_3D ( 'NONE', #61228, #46037, #12792 ) ;
#9803=LINE ( 'NONE', #5533, #64657 ) ;
#9816=VERTEX_POINT ( 'NONE', #38639 ) ;
#9842=VERTEX_POINT ( 'NONE', #34340 ) ;
#9855=ORIENTED_EDGE ( 'NONE', *, *, #31515, .F. ) ;
#9870=PLANE ( 'NONE',  #41035 ) ;
#9898=AXIS2_PLACEMENT_3D ( 'NONE', #35417, #67263, #24827 ) ;
#9918=ORIENTED_EDGE ( 'NONE', *, *, #30212, .F. ) ;
#9924=ORIENTED_EDGE ( 'NONE', *, *, #64066, .T. ) ;
#9930=ADVANCED_FACE ( 'NONE', ( #40368 ), #8886, .F. ) ;
#9935=CARTESIAN_POINT ( 'NONE',  ( 7.000000000000000000, -26.42999999999999972, -9.412893218813501051 ) ) ;
#9946=ORIENTED_EDGE ( 'NONE', *, *, #17970, .T. ) ;
#9967=DIRECTION ( 'NONE',  ( 0.000000000000000000, 0.000000000000000000, 1.000000000000000000 ) ) ;
#9974=DIRECTION ( 'NONE',  ( 0.000000000000000000, 1.000000000000000000, 0.000000000000000000 ) ) ;
#9981=CARTESIAN_POINT ( 'NONE',  ( 283.0000000000000568, -20.40000000000000213, -17.60000000000000142 ) ) ;
#9985=EDGE_LOOP ( 'NONE', ( #69109, #1408, #40081, #25859 ) ) ;
#9998=CIRCLE ( 'NONE', #41624, 0.4999999999979497511 ) ;
#10001=DIRECTION ( 'NONE',  ( -1.000000000000000000, 0.000000000000000000, 0.000000000000000000 ) ) ;
#10006=DIRECTION ( 'NONE',  ( 1.000000000000000000, 0.000000000000000000, 0.000000000000000000 ) ) ;
#10015=SHAPE_REPRESENTATION_RELATIONSHIP ( 'NONE' , 'NONE' ,  #64253, #67252 ) ;
#10022=ORIENTED_EDGE ( 'NONE', *, *, #52243, .T. ) ;
#10032=CARTESIAN_POINT ( 'NONE',  ( 283.0000000000000568, -32.95000000000000284, -7.700000000000000178 ) ) ;
#10059=VECTOR ( 'NONE', #58926, 1000.000000000000000 ) ;
#10067=AXIS2_PLACEMENT_3D ( 'NONE', #60803, #1759, #61485 ) ;
#10068=CARTESIAN_POINT ( 'NONE',  ( 283.0000000000000568, -31.30000000000000071, 12.69999999999999929 ) ) ;
#10090=EDGE_CURVE ( 'NONE', #34171, #749, #49739, .T. ) ;
#10114=VECTOR ( 'NONE', #6552, 1000.000000000000000 ) ;
#10115=CARTESIAN_POINT ( 'NONE',  ( 7.000000000000000000, -25.56180396883900130, 14.25872597390799967 ) ) ;
#10137=ORIENTED_EDGE ( 'NONE', *, *, #68210, .T. ) ;
#10143=FACE_OUTER_BOUND ( 'NONE', #23292, .T. ) ;
#10146=VECTOR ( 'NONE', #8466, 1000.000000000000000 ) ;
#10169=EDGE_CURVE ( 'NONE', #25149, #40605, #68646, .T. ) ;
#10171=ORIENTED_EDGE ( 'NONE', *, *, #63972, .T. ) ;
#10186=DIRECTION ( 'NONE',  ( -1.000000000000000000, 0.000000000000000000, 0.000000000000000000 ) ) ;
#10187=ORIENTED_EDGE ( 'NONE', *, *, #61708, .F. ) ;
#10190=ORIENTED_EDGE ( 'NONE', *, *, #67550, .F. ) ;
#10193=DIRECTION ( 'NONE',  ( 0.000000000000000000, 1.000000000000000000, 1.922073611378672844E-12 ) ) ;
#10201=AXIS2_PLACEMENT_3D ( 'NONE', #18741, #40311, #6739 ) ;
#10206=CARTESIAN_POINT ( 'NONE',  ( 283.0000000000000568, -32.45000000000000995, -15.00000000000000000 ) ) ;
#10208=CARTESIAN_POINT ( 'NONE',  ( 15.00000000000000000, -0.5000000000000000000, -26.50000000000000000 ) ) ;
#10215=CARTESIAN_POINT ( 'NONE',  ( 7.000000000000000000, -32.00000000000000000, -8.400000000000000355 ) ) ;
#10217=LINE ( 'NONE', #67864, #18854 ) ;
#10220=CARTESIAN_POINT ( 'NONE',  ( 280.0000000000000000, -53.81370849898476649, -16.00000000000000711 ) ) ;
#10226=EDGE_CURVE ( 'NONE', #51967, #27626, #28280, .T. ) ;
#10250=DIRECTION ( 'NONE',  ( 1.000000000000000000, 0.000000000000000000, 0.000000000000000000 ) ) ;
#10262=EDGE_CURVE ( 'NONE', #39282, #3194, #7049, .T. ) ;
#10263=ORIENTED_EDGE ( 'NONE', *, *, #63874, .F. ) ;
#10308=EDGE_CURVE ( 'NONE', #13785, #46983, #56200, .T. ) ;
#10313=AXIS2_PLACEMENT_3D ( 'NONE', #43418, #61053, #33158 ) ;
#10330=DIRECTION ( 'NONE',  ( 0.000000000000000000, -1.000000000000000000, 0.000000000000000000 ) ) ;
#10336=ORIENTED_EDGE ( 'NONE', *, *, #63756, .F. ) ;
#10337=ORIENTED_EDGE ( 'NONE', *, *, #29112, .T. ) ;
#10354=EDGE_LOOP ( 'NONE', ( #36290, #45338 ) ) ;
#10375=ORIENTED_EDGE ( 'NONE', *, *, #54242, .F. ) ;
#10399=AXIS2_PLACEMENT_3D ( 'NONE', #58947, #63562, #27120 ) ;
#10410=AXIS2_PLACEMENT_3D ( 'NONE', #30394, #51963, #29326 ) ;
#10420=ORIENTED_EDGE ( 'NONE', *, *, #48125, .F. ) ;
#10421=CARTESIAN_POINT ( 'NONE',  ( 0.000000000000000000, -21.00000000000000000, -5.000000000000000000 ) ) ;
#10429=ORIENTED_EDGE ( 'NONE', *, *, #57163, .T. ) ;
#10448=VERTEX_POINT ( 'NONE', #21174 ) ;
#10459=ORIENTED_EDGE ( 'NONE', *, *, #55328, .T. ) ;
#10467=DIRECTION ( 'NONE',  ( 0.000000000000000000, 0.000000000000000000, 1.000000000000000000 ) ) ;
#10484=DIRECTION ( 'NONE',  ( 0.000000000000000000, -0.7071067811828075644, 0.7071067811902875810 ) ) ;
#10500=VECTOR ( 'NONE', #1956, 1000.000000000000000 ) ;
#10502=CARTESIAN_POINT ( 'NONE',  ( 7.000000000000000000, -30.45000000000094786, -14.49999999999906031 ) ) ;
#10503=VERTEX_POINT ( 'NONE', #10208 ) ;
#10512=LINE ( 'NONE', #36694, #30236 ) ;
#10529=VECTOR ( 'NONE', #10186, 1000.000000000000000 ) ;
#10536=AXIS2_PLACEMENT_3D ( 'NONE', #11629, #21237, #42783 ) ;
#10551=AXIS2_PLACEMENT_3D ( 'NONE', #60667, #33785, #12555 ) ;
#10556=VECTOR ( 'NONE', #2712, 1000.000000000000000 ) ;
#10588=ORIENTED_EDGE ( 'NONE', *, *, #35353, .F. ) ;
#10589=APPLICATION_CONTEXT ( 'automotive_design' ) ;
#10602=CARTESIAN_POINT ( 'NONE',  ( 275.0000000000000000, -42.00000000000000000, 15.10000000000000142 ) ) ;
#10609=VERTEX_POINT ( 'NONE', #65682 ) ;
#10622=CARTESIAN_POINT ( 'NONE',  ( 283.0000000000000568, -42.50000000000000000, 7.500000000000000000 ) ) ;
#10629=ORIENTED_EDGE ( 'NONE', *, *, #6172, .T. ) ;
#10636=FACE_OUTER_BOUND ( 'NONE', #48429, .T. ) ;
#10644=DIRECTION ( 'NONE',  ( 0.000000000000000000, 0.000000000000000000, 1.000000000000000000 ) ) ;
#10669=ORIENTED_EDGE ( 'NONE', *, *, #7260, .F. ) ;
#10671=VECTOR ( 'NONE', #10006, 1000.000000000000000 ) ;
#10684=AXIS2_PLACEMENT_3D ( 'NONE', #55885, #66834, #8128 ) ;
#10698=CIRCLE ( 'NONE', #26550, 0.5000000000009320322 ) ;
#10702=ORIENTED_EDGE ( 'NONE', *, *, #6165, .F. ) ;
#10704=VECTOR ( 'NONE', #43455, 1000.000000000000000 ) ;
#10705=EDGE_CURVE ( 'NONE', #14268, #8022, #66378, .T. ) ;
#10713=DIRECTION ( 'NONE',  ( 0.5773502691896257311, 0.5773502691896257311, -0.5773502691896257311 ) ) ;
#10727=LINE ( 'NONE', #43249, #35016 ) ;
#10732=DIRECTION ( 'NONE',  ( 0.000000000000000000, -0.7066873191084664940, 0.7075259945834416753 ) ) ;
#10742=AXIS2_PLACEMENT_3D ( 'NONE', #51245, #7761, #14481 ) ;
#10771=ORIENTED_EDGE ( 'NONE', *, *, #7064, .T. ) ;
#10776=VERTEX_POINT ( 'NONE', #29220 ) ;
#10781=CIRCLE ( 'NONE', #31146, 0.4999999999979843901 ) ;
#10783=VERTEX_POINT ( 'NONE', #45136 ) ;
#10795=CARTESIAN_POINT ( 'NONE',  ( 283.0000000000000568, -25.00000000000000000, -17.50000000000000000 ) ) ;
#10806=VERTEX_POINT ( 'NONE', #67762 ) ;
#10837=DIRECTION ( 'NONE',  ( 0.000000000000000000, 1.000000000000000000, 0.000000000000000000 ) ) ;
#10862=DIRECTION ( 'NONE',  ( 0.000000000000000000, 0.000000000000000000, -1.000000000000000000 ) ) ;
#10868=LINE ( 'NONE', #32780, #43667 ) ;
#10874=EDGE_CURVE ( 'NONE', #48603, #3647, #16956, .T. ) ;
#10889=ORIENTED_EDGE ( 'NONE', *, *, #60917, .T. ) ;
#10893=VECTOR ( 'NONE', #51314, 1000.000000000000114 ) ;
#10909=CARTESIAN_POINT ( 'NONE',  ( 290.0000000000000000, -21.00000000000000000, 0.000000000000000000 ) ) ;
#10938=DIRECTION ( 'NONE',  ( 1.000000000000000000, -0.000000000000000000, -0.000000000000000000 ) ) ;
#10944=VERTEX_POINT ( 'NONE', #3763 ) ;
#10957=VECTOR ( 'NONE', #17205, 1000.000000000000000 ) ;
#10966=ADVANCED_FACE ( 'NONE', ( #26387 ), #42289, .F. ) ;
#10975=VERTEX_POINT ( 'NONE', #29123 ) ;
#10978=ORIENTED_EDGE ( 'NONE', *, *, #56602, .F. ) ;
#10980=CARTESIAN_POINT ( 'NONE',  ( 7.000000000000000000, -23.65000000000000568, 12.40000000000000213 ) ) ;
#10984=DIRECTION ( 'NONE',  ( 0.5773502691896258421, -0.5773502691896257311, -0.5773502691896257311 ) ) ;
#10985=DIRECTION ( 'NONE',  ( -0.000000000000000000, -1.000000000000000000, -0.000000000000000000 ) ) ;
#10987=LINE ( 'NONE', #32564, #48748 ) ;
#10988=VERTEX_POINT ( 'NONE', #67653 ) ;
#10997=AXIS2_PLACEMENT_3D ( 'NONE', #51857, #51144, #15075 ) ;
#11000=CARTESIAN_POINT ( 'NONE',  ( 7.000000000000000000, -42.50000000000000000, -14.50000000000000000 ) ) ;
#11009=EDGE_CURVE ( 'NONE', #69932, #8602, #68136, .T. ) ;
#11010=AXIS2_PLACEMENT_3D ( 'NONE', #54307, #44710, #66297 ) ;
#11058=CARTESIAN_POINT ( 'NONE',  ( 14.50000000000000000, -0.5000000000000000000, 27.00000000000000000 ) ) ;
#11061=DIRECTION ( 'NONE',  ( -1.000000000000000000, 0.000000000000000000, 0.000000000000000000 ) ) ;
#11066=ORIENTED_EDGE ( 'NONE', *, *, #29356, .T. ) ;
#11077=CARTESIAN_POINT ( 'NONE',  ( 289.5000000000000000, -42.50000000000000000, -26.50000000000000000 ) ) ;
#11091=EDGE_CURVE ( 'NONE', #55546, #40253, #29718, .T. ) ;
#11124=LINE ( 'NONE', #38012, #26454 ) ;
#11134=ORIENTED_EDGE ( 'NONE', *, *, #51102, .F. ) ;
#11155=EDGE_CURVE ( 'NONE', #38091, #37343, #26270, .T. ) ;
#11193=ORIENTED_EDGE ( 'NONE', *, *, #11909, .F. ) ;
#11198=ORIENTED_EDGE ( 'NONE', *, *, #7013, .F. ) ;
#11206=CARTESIAN_POINT ( 'NONE',  ( 7.000000000000000000, -31.30000000000000071, -8.400000000000000355 ) ) ;
#11207=EDGE_CURVE ( 'NONE', #12942, #32305, #38620, .T. ) ;
#11216=ORIENTED_EDGE ( 'NONE', *, *, #6349, .F. ) ;
#11238=CARTESIAN_POINT ( 'NONE',  ( 290.0000000000000000, -0.5000000000000000000, -26.50000000000000000 ) ) ;
#11248=ORIENTED_EDGE ( 'NONE', *, *, #26448, .T. ) ;
#11270=ORIENTED_EDGE ( 'NONE', *, *, #3259, .T. ) ;
#11285=LINE ( 'NONE', #54439, #59520 ) ;
#11286=LINE ( 'NONE', #5994, #1604 ) ;
#11338=AXIS2_PLACEMENT_3D ( 'NONE', #50043, #44044, #578 ) ;
#11339=( NAMED_UNIT ( * ) SI_UNIT ( $, .STERADIAN. ) SOLID_ANGLE_UNIT ( ) );
#11342=EDGE_CURVE ( 'NONE', #66149, #66609, #1507, .T. ) ;
#11345=EDGE_CURVE ( 'NONE', #9620, #40700, #33982, .T. ) ;
#11348=VERTEX_POINT ( 'NONE', #19748 ) ;
#11362=DIRECTION ( 'NONE',  ( 0.000000000000000000, 1.000000000000000000, 0.000000000000000000 ) ) ;
#11372=ORIENTED_EDGE ( 'NONE', *, *, #38629, .T. ) ;
#11421=DIRECTION ( 'NONE',  ( 0.000000000000000000, -1.000000000000000000, -7.802196388977322746E-10 ) ) ;
#11459=ORIENTED_EDGE ( 'NONE', *, *, #47105, .T. ) ;
#11481=DIRECTION ( 'NONE',  ( 1.000000000000000000, 0.000000000000000000, 0.000000000000000000 ) ) ;
#11482=DIRECTION ( 'NONE',  ( 1.000000000000000000, 0.000000000000000000, 0.000000000000000000 ) ) ;
#11502=CARTESIAN_POINT ( 'NONE',  ( 283.0000000000000568, -40.30000000000000426, 8.900000000000000355 ) ) ;
#11510=EDGE_LOOP ( 'NONE', ( #56599, #38634, #2917, #54684 ) ) ;
#11516=EDGE_CURVE ( 'NONE', #55748, #65336, #26130, .T. ) ;
#11520=VECTOR ( 'NONE', #21855, 1000.000000000000000 ) ;
#11523=ORIENTED_EDGE ( 'NONE', *, *, #23861, .F. ) ;
#11547=ORIENTED_EDGE ( 'NONE', *, *, #1244, .T. ) ;
#11566=CARTESIAN_POINT ( 'NONE',  ( 14.50000000000000000, -42.50000000000000000, 26.50000000000000000 ) ) ;
#11583=FACE_OUTER_BOUND ( 'NONE', #26216, .T. ) ;
#11586=DIRECTION ( 'NONE',  ( 0.000000000000000000, -0.7051282051282052876, -0.7090798363602477394 ) ) ;
#11622=ORIENTED_EDGE ( 'NONE', *, *, #57126, .T. ) ;
#11627=ORIENTED_EDGE ( 'NONE', *, *, #68480, .F. ) ;
#11629=CARTESIAN_POINT ( 'NONE',  ( 283.0000000000000568, -25.93000000000544958, -9.412893218815410634 ) ) ;
#11635=DIRECTION ( 'NONE',  ( -1.000000000000000000, 0.000000000000000000, 0.000000000000000000 ) ) ;
#11656=EDGE_LOOP ( 'NONE', ( #20038, #7724, #39894, #41011 ) ) ;
#11658=ORIENTED_EDGE ( 'NONE', *, *, #5165, .F. ) ;
#11684=DIRECTION ( 'NONE',  ( 0.7071067811865474617, 0.000000000000000000, 0.7071067811865474617 ) ) ;
#11687=EDGE_CURVE ( 'NONE', #29731, #42484, #55342, .T. ) ;
#11694=VERTEX_POINT ( 'NONE', #55006 ) ;
#11706=PLANE ( 'NONE',  #39649 ) ;
#11731=DIRECTION ( 'NONE',  ( 1.000000000000000000, 0.000000000000000000, 0.000000000000000000 ) ) ;
#11741=VECTOR ( 'NONE', #45867, 1000.000000000000000 ) ;
#11751=CARTESIAN_POINT ( 'NONE',  ( 283.0000000000000568, -38.64999999999999858, 12.69999999999999929 ) ) ;
#11756=CARTESIAN_POINT ( 'NONE',  ( 7.000000000000000000, -23.65000000000000568, -12.40000000000000213 ) ) ;
#11765=DIRECTION ( 'NONE',  ( 0.000000000000000000, -1.000000000000000000, 0.000000000000000000 ) ) ;
#11767=VERTEX_POINT ( 'NONE', #14303 ) ;
#11769=DIRECTION ( 'NONE',  ( 0.000000000000000000, -1.000000000000000000, 0.000000000000000000 ) ) ;
#11770=( BOUNDED_CURVE ( )  B_SPLINE_CURVE ( 3, ( #28290, #43865, #39250, #38570 ),
 .UNSPECIFIED., .F., .F. ) 
 B_SPLINE_CURVE_WITH_KNOTS ( ( 4, 4 ),
 ( 2.293530574608309003, 2.418858405776377563 ),
 .UNSPECIFIED. ) 
 CURVE ( )  GEOMETRIC_REPRESENTATION_ITEM ( )  RATIONAL_B_SPLINE_CURVE ( ( 1.000000000000000000, 0.9986915061577686936, 0.9986915061577686936, 1.000000000000000000 ) ) 
 REPRESENTATION_ITEM ( '' )  );
#11772=VERTEX_POINT ( 'NONE', #4404 ) ;
#11785=ORIENTED_EDGE ( 'NONE', *, *, #9205, .T. ) ;
#11803=FACE_OUTER_BOUND ( 'NONE', #34134, .T. ) ;
#11810=AXIS2_PLACEMENT_3D ( 'NONE', #2418, #7015, #12657 ) ;
#11816=ORIENTED_EDGE ( 'NONE', *, *, #64569, .F. ) ;
#11817=DIRECTION ( 'NONE',  ( 1.000000000000000000, 0.000000000000000000, 0.000000000000000000 ) ) ;
#11834=VECTOR ( 'NONE', #20130, 1000.000000000000000 ) ;
#11843=CIRCLE ( 'NONE', #53674, 0.5000000000009284795 ) ;
#11844=DIRECTION ( 'NONE',  ( -0.7071067811865480168, 0.7071067811865470176, 0.000000000000000000 ) ) ;
#11861=CARTESIAN_POINT ( 'NONE',  ( 15.00000000000000000, -25.60000000000000142, 15.10000000000000142 ) ) ;
#11877=ORIENTED_EDGE ( 'NONE', *, *, #58771, .F. ) ;
#11886=ORIENTED_EDGE ( 'NONE', *, *, #55303, .F. ) ;
#11888=CARTESIAN_POINT ( 'NONE',  ( 289.5000000000000000, -42.50000000000000000, 26.50000000000000000 ) ) ;
#11909=EDGE_CURVE ( 'NONE', #53055, #37771, #44498, .T. ) ;
#11937=LINE ( 'NONE', #38157, #35457 ) ;
#11938=CARTESIAN_POINT ( 'NONE',  ( 283.0000000000000568, -42.50000000000000000, 7.500000000000000000 ) ) ;
#11956=VERTEX_POINT ( 'NONE', #54231 ) ;
#11972=LINE ( 'NONE', #61827, #43293 ) ;
#11982=FACE_OUTER_BOUND ( 'NONE', #44677, .T. ) ;
#11989=FACE_OUTER_BOUND ( 'NONE', #2280, .T. ) ;
#11990=CARTESIAN_POINT ( 'NONE',  ( 283.0000000000000568, -38.15000000000000568, 13.19999999999999929 ) ) ;
#11992=CARTESIAN_POINT ( 'NONE',  ( 7.000000000000000000, -25.60000000000000142, -15.10000000000000142 ) ) ;
#12005=CARTESIAN_POINT ( 'NONE',  ( 7.500000000000000000, -20.49999999999999645, -20.00000000000000000 ) ) ;
#12013=DIRECTION ( 'NONE',  ( -1.000000000000000000, 0.000000000000000000, 0.000000000000000000 ) ) ;
#12014=LINE ( 'NONE', #29672, #25460 ) ;
#12018=COLOUR_RGB ( '', 0.72549020, 0.75294118, 0.79215686) ;
#12022=FACE_OUTER_BOUND ( 'NONE', #45937, .T. ) ;
#12024=ORIENTED_EDGE ( 'NONE', *, *, #38961, .T. ) ;
#12027=LINE ( 'NONE', #38246, #19100 ) ;
#12028=VECTOR ( 'NONE', #34972, 1000.000000000000000 ) ;
#12029=VECTOR ( 'NONE', #10984, 999.9999999999998863 ) ;
#12042=CARTESIAN_POINT ( 'NONE',  ( 280.0000000000000000, -25.60000000000000142, -20.00000000000000000 ) ) ;
#12057=VECTOR ( 'NONE', #57410, 1000.000000000000000 ) ;
#12059=FACE_OUTER_BOUND ( 'NONE', #50767, .T. ) ;
#12060=CARTESIAN_POINT ( 'NONE',  ( 0.000000000000000000, -0.5000000000000000000, 26.50000000000000000 ) ) ;
#12074=CARTESIAN_POINT ( 'NONE',  ( 275.2500000000000000, -42.25000000000000000, -26.75000000000000000 ) ) ;
#12091=EDGE_CURVE ( 'NONE', #29737, #21069, #63766, .T. ) ;
#12093=VECTOR ( 'NONE', #48989, 1000.000000000000000 ) ;
#12113=DIRECTION ( 'NONE',  ( 0.000000000000000000, 0.9760787414516886029, 0.2174173187353931058 ) ) ;
#12115=CARTESIAN_POINT ( 'NONE',  ( 7.000000000000000000, -25.69999999999924967, 14.52500000000000213 ) ) ;
#12124=VERTEX_POINT ( 'NONE', #24108 ) ;
#12128=CARTESIAN_POINT ( 'NONE',  ( 283.0000000000000568, -23.65000000000000568, -12.40000000000000213 ) ) ;
#12141=AXIS2_PLACEMENT_3D ( 'NONE', #1785, #56576, #28652 ) ;
#12147=ORIENTED_EDGE ( 'NONE', *, *, #40003, .F. ) ;
#12148=VECTOR ( 'NONE', #9343, 999.9999999999998863 ) ;
#12155=ORIENTED_EDGE ( 'NONE', *, *, #54907, .F. ) ;
#12157=DIRECTION ( 'NONE',  ( 1.000000000000000000, -0.000000000000000000, -0.000000000000000000 ) ) ;
#12162=ORIENTED_EDGE ( 'NONE', *, *, #28904, .T. ) ;
#12168=ORIENTED_EDGE ( 'NONE', *, *, #42731, .F. ) ;
#12172=CARTESIAN_POINT ( 'NONE',  ( 275.5000000000000000, -42.50000000000000000, -26.50000000000000000 ) ) ;
#12177=LINE ( 'NONE', #10795, #31314 ) ;
#12184=EDGE_LOOP ( 'NONE', ( #34635, #20310, #12221, #34890 ) ) ;
#12211=EDGE_CURVE ( 'NONE', #22096, #30661, #12938, .T. ) ;
#12216=EDGE_CURVE ( 'NONE', #9032, #8637, #13856, .T. ) ;
#12221=ORIENTED_EDGE ( 'NONE', *, *, #5743, .T. ) ;
#12223=EDGE_LOOP ( 'NONE', ( #37494, #31111, #44735, #48529 ) ) ;
#12243=VERTEX_POINT ( 'NONE', #56980 ) ;
#12256=CARTESIAN_POINT ( 'NONE',  ( 15.00000000000000000, -21.00000000000000000, 0.000000000000000000 ) ) ;
#12278=DIRECTION ( 'NONE',  ( 0.000000000000000000, 0.000000000000000000, 1.000000000000000000 ) ) ;
#12289=VECTOR ( 'NONE', #634, 1000.000000000000000 ) ;
#12294=EDGE_CURVE ( 'NONE', #25376, #37466, #55, .T. ) ;
#12315=VERTEX_POINT ( 'NONE', #53798 ) ;
#12326=VECTOR ( 'NONE', #9610, 1000.000000000000000 ) ;
#12330=ADVANCED_FACE ( 'NONE', ( #69348 ), #21952, .F. ) ;
#12346=CARTESIAN_POINT ( 'NONE',  ( 282.6457513110646005, -20.49999999999999645, -17.00000000000000000 ) ) ;
#12348=EDGE_CURVE ( 'NONE', #6527, #60332, #53661, .T. ) ;
#12365=LINE ( 'NONE', #43877, #22558 ) ;
#12369=LINE ( 'NONE', #66137, #1503 ) ;
#12370=AXIS2_PLACEMENT_3D ( 'NONE', #38822, #44813, #12278 ) ;
#12371=ORIENTED_EDGE ( 'NONE', *, *, #55150, .F. ) ;
#12374=ORIENTED_EDGE ( 'NONE', *, *, #29200, .F. ) ;
#12381=EDGE_CURVE ( 'NONE', #18763, #8602, #48142, .T. ) ;
#12385=EDGE_LOOP ( 'NONE', ( #40884, #44006, #51539, #24198 ) ) ;
#12393=LINE ( 'NONE', #65810, #29232 ) ;
#12407=DIRECTION ( 'NONE',  ( 0.000000000000000000, 0.000000000000000000, -1.000000000000000000 ) ) ;
#12410=VERTEX_POINT ( 'NONE', #32582 ) ;
#12430=CYLINDRICAL_SURFACE ( 'NONE', #19929, 0.5000000000004306555 ) ;
#12436=ADVANCED_FACE ( 'NONE', ( #34271, #22316 ), #38903, .F. ) ;
#12445=EDGE_CURVE ( 'NONE', #57359, #20615, #11770, .T. ) ;
#12449=VECTOR ( 'NONE', #21946, 1000.000000000000000 ) ;
#12451=DIRECTION ( 'NONE',  ( -1.000000000000000000, 0.000000000000000000, 0.000000000000000000 ) ) ;
#12452=EDGE_CURVE ( 'NONE', #15205, #17604, #60122, .T. ) ;
#12462=AXIS2_PLACEMENT_3D ( 'NONE', #15673, #25938, #68008 ) ;
#12482=DIRECTION ( 'NONE',  ( 0.000000000000000000, 0.4606534372016282686, -0.8875800869748744493 ) ) ;
#12484=CARTESIAN_POINT ( 'NONE',  ( 283.0000000000000568, -25.93000000000544958, -9.412893218815410634 ) ) ;
#12488=CARTESIAN_POINT ( 'NONE',  ( 277.0217896459287203, -20.81978353999699749, 17.31978353999700104 ) ) ;
#12502=ORIENTED_EDGE ( 'NONE', *, *, #5179, .T. ) ;
#12507=EDGE_LOOP ( 'NONE', ( #42723, #47965, #55243, #8146 ) ) ;
#12525=EDGE_CURVE ( 'NONE', #32093, #38982, #44539, .T. ) ;
#12538=EDGE_CURVE ( 'NONE', #68548, #9656, #28984, .T. ) ;
#12547=DIRECTION ( 'NONE',  ( -0.7071067811865475727, 0.000000000000000000, -0.7071067811865475727 ) ) ;
#12555=DIRECTION ( 'NONE',  ( 0.000000000000000000, -0.7051282051282052876, -0.7090798363602477394 ) ) ;
#12573=CARTESIAN_POINT ( 'NONE',  ( 7.000000000000000000, -31.30000000000000071, 8.400000000000000355 ) ) ;
#12574=AXIS2_PLACEMENT_3D ( 'NONE', #63335, #49162, #6031 ) ;
#12592=ADVANCED_FACE ( 'NONE', ( #46998 ), #13768, .F. ) ;
#12597=LINE ( 'NONE', #44773, #32664 ) ;
#12607=EDGE_LOOP ( 'NONE', ( #59989, #50202, #28266, #60270 ) ) ;
#12618=DIRECTION ( 'NONE',  ( 0.000000000000000000, 0.000000000000000000, -1.000000000000000000 ) ) ;
#12629=DIRECTION ( 'NONE',  ( 0.000000000000000000, 1.000000000000000000, 0.000000000000000000 ) ) ;
#12635=CARTESIAN_POINT ( 'NONE',  ( 283.0000000000000568, -39.80000000000000426, 12.69999999999999929 ) ) ;
#12640=EDGE_CURVE ( 'NONE', #39282, #52775, #25437, .T. ) ;
#12657=DIRECTION ( 'NONE',  ( 0.000000000000000000, 0.000000000000000000, 1.000000000000000000 ) ) ;
#12667=ORIENTED_EDGE ( 'NONE', *, *, #28509, .F. ) ;
#12670=DIRECTION ( 'NONE',  ( -1.000000000000000000, 0.000000000000000000, 0.000000000000000000 ) ) ;
#12675=CARTESIAN_POINT ( 'NONE',  ( 290.0000000000000000, -21.00000000000000000, 5.000000000000000000 ) ) ;
#12681=DIRECTION ( 'NONE',  ( 0.000000000000000000, 0.000000000000000000, 1.000000000000000000 ) ) ;
#12737=VECTOR ( 'NONE', #18057, 1000.000000000000000 ) ;
#12745=ORIENTED_EDGE ( 'NONE', *, *, #24137, .T. ) ;
#12757=ORIENTED_EDGE ( 'NONE', *, *, #51675, .F. ) ;
#12760=AXIS2_PLACEMENT_3D ( 'NONE', #68322, #57711, #52419 ) ;
#12778=CARTESIAN_POINT ( 'NONE',  ( 7.000000000000000000, -27.13000000000000611, -13.50000000000000000 ) ) ;
#12792=DIRECTION ( 'NONE',  ( 0.000000000000000000, 0.000000000000000000, 1.000000000000000000 ) ) ;
#12793=DIRECTION ( 'NONE',  ( 0.000000000000000000, -2.206568261432184716E-12, 1.000000000000000000 ) ) ;
#12805=CARTESIAN_POINT ( 'NONE',  ( 275.5000000000000000, -42.00000000000000000, 27.00000000000000000 ) ) ;
#12809=ORIENTED_EDGE ( 'NONE', *, *, #59666, .F. ) ;
#12818=CARTESIAN_POINT ( 'NONE',  ( 290.0000000000000000, -0.5000000000000000000, 26.50000000000000000 ) ) ;
#12830=ORIENTED_EDGE ( 'NONE', *, *, #22755, .F. ) ;
#12840=EDGE_CURVE ( 'NONE', #13397, #52106, #27183, .T. ) ;
#12853=ORIENTED_EDGE ( 'NONE', *, *, #32941, .T. ) ;
#12857=LINE ( 'NONE', #13923, #50506 ) ;
#12897=EDGE_CURVE ( 'NONE', #13736, #11767, #55774, .T. ) ;
#12898=VECTOR ( 'NONE', #27911, 1000.000000000000000 ) ;
#12903=EDGE_LOOP ( 'NONE', ( #65189, #9506, #63458, #20887, #11627, #49588, #43664, #52441, #60339, #12371, #57974, #23053, #52464, #55501, #66227, #14587, #16985, #26111, #32083, #43573, #55941, #22691, #67620, #8590, #53348, #51474, #5262, #15077, #47264, #59925, #18598, #47211, #37560, #50345 ) ) ;
#12914=ORIENTED_EDGE ( 'NONE', *, *, #56140, .T. ) ;
#12915=ADVANCED_FACE ( 'NONE', ( #60372 ), #28543, .F. ) ;
#12923=ORIENTED_EDGE ( 'NONE', *, *, #22467, .F. ) ;
#12931=ADVANCED_FACE ( 'NONE', ( #11583 ), #23587, .F. ) ;
#12934=LINE ( 'NONE', #61028, #23633 ) ;
#12938=CIRCLE ( 'NONE', #54760, 5.000000000000000000 ) ;
#12942=VERTEX_POINT ( 'NONE', #23243 ) ;
#12948=DIRECTION ( 'NONE',  ( 0.000000000000000000, -2.123301534585676023E-12, 1.000000000000000000 ) ) ;
#12951=LINE ( 'NONE', #67426, #23344 ) ;
#12970=ORIENTED_EDGE ( 'NONE', *, *, #59029, .F. ) ;
#12971=CARTESIAN_POINT ( 'NONE',  ( 15.00000000000000000, -0.5000000000000000000, 26.50000000000000000 ) ) ;
#13011=FACE_OUTER_BOUND ( 'NONE', #26816, .T. ) ;
#13015=VERTEX_POINT ( 'NONE', #46202 ) ;
#13069=ORIENTED_EDGE ( 'NONE', *, *, #10226, .F. ) ;
#13081=CARTESIAN_POINT ( 'NONE',  ( 14.99999999999999822, -42.00000000000000000, 26.50000000000000000 ) ) ;
#13089=VERTEX_POINT ( 'NONE', #25350 ) ;
#13100=EDGE_CURVE ( 'NONE', #69664, #60907, #34884, .T. ) ;
#13116=AXIS2_PLACEMENT_3D ( 'NONE', #29952, #30314, #57876 ) ;
#13123=ORIENTED_EDGE ( 'NONE', *, *, #50782, .T. ) ;
#13162=ORIENTED_EDGE ( 'NONE', *, *, #35388, .T. ) ;
#13165=LINE ( 'NONE', #69279, #23214 ) ;
#13174=VERTEX_POINT ( 'NONE', #47963 ) ;
#13184=ORIENTED_EDGE ( 'NONE', *, *, #5549, .T. ) ;
#13192=DIRECTION ( 'NONE',  ( 0.000000000000000000, 1.000000000000000000, 0.000000000000000000 ) ) ;
#13196=AXIS2_PLACEMENT_3D ( 'NONE', #42735, #49082, #27518 ) ;
#13213=VERTEX_POINT ( 'NONE', #47612 ) ;
#13231=EDGE_CURVE ( 'NONE', #69664, #35311, #64239, .T. ) ;
#13257=DIRECTION ( 'NONE',  ( 0.000000000000000000, 0.000000000000000000, 1.000000000000000000 ) ) ;
#13265=DIRECTION ( 'NONE',  ( -0.5773502691896243988, 0.5773502691896263972, -0.5773502691896263972 ) ) ;
#13294=EDGE_CURVE ( 'NONE', #10448, #25545, #54317, .T. ) ;
#13302=LINE ( 'NONE', #3402, #20462 ) ;
#13318=ORIENTED_EDGE ( 'NONE', *, *, #54806, .F. ) ;
#13329=CARTESIAN_POINT ( 'NONE',  ( 7.000000000000000000, -42.50000000000000000, -15.10000000000000142 ) ) ;
#13346=LINE ( 'NONE', #51534, #30008 ) ;
#13349=CARTESIAN_POINT ( 'NONE',  ( 283.0000000000000568, -32.95000000000000284, 14.50000000000000000 ) ) ;
#13361=ORIENTED_EDGE ( 'NONE', *, *, #12445, .F. ) ;
#13380=ORIENTED_EDGE ( 'NONE', *, *, #36241, .F. ) ;
#13397=VERTEX_POINT ( 'NONE', #29514 ) ;
#13401=CARTESIAN_POINT ( 'NONE',  ( 282.7711612342632179, -20.61060115624107425, 17.11060115624107425 ) ) ;
#13412=DIRECTION ( 'NONE',  ( 0.000000000000000000, 1.000000000000000000, 0.000000000000000000 ) ) ;
#13416=ORIENTED_EDGE ( 'NONE', *, *, #17185, .T. ) ;
#13417=CARTESIAN_POINT ( 'NONE',  ( 283.0000000000000568, -25.60000000000000142, 17.60000000000000142 ) ) ;
#13425=FACE_OUTER_BOUND ( 'NONE', #22349, .T. ) ;
#13426=AXIS2_PLACEMENT_3D ( 'NONE', #52390, #42117, #3953 ) ;
#13432=EDGE_CURVE ( 'NONE', #10776, #21056, #45420, .T. ) ;
#13440=ORIENTED_EDGE ( 'NONE', *, *, #4855, .T. ) ;
#13449=ORIENTED_EDGE ( 'NONE', *, *, #48125, .T. ) ;
#13466=CIRCLE ( 'NONE', #57529, 3.999999999999993339 ) ;
#13473=LINE ( 'NONE', #36813, #8319 ) ;
#13481=CARTESIAN_POINT ( 'NONE',  ( 0.4999999999999920064, -7.105427357601001859E-15, 26.49999999999998579 ) ) ;
#13504=EDGE_LOOP ( 'NONE', ( #21889, #26928, #13123, #3229 ) ) ;
#13519=CARTESIAN_POINT ( 'NONE',  ( 275.0000000000000000, -26.42999999999999972, -9.412893218813501051 ) ) ;
#13522=ORIENTED_EDGE ( 'NONE', *, *, #13294, .F. ) ;
#13529=DIRECTION ( 'NONE',  ( 1.000000000000000000, -0.000000000000000000, -0.000000000000000000 ) ) ;
#13533=VERTEX_POINT ( 'NONE', #49189 ) ;
#13551=DIRECTION ( 'NONE',  ( 0.000000000000000000, -1.901256929667050114E-12, 1.000000000000000000 ) ) ;
#13581=VECTOR ( 'NONE', #32302, 1000.000000000000000 ) ;
#13584=CARTESIAN_POINT ( 'NONE',  ( 283.0000000000000568, -21.00000000000000000, -17.50000000000000000 ) ) ;
#13587=ORIENTED_EDGE ( 'NONE', *, *, #6349, .T. ) ;
#13590=LINE ( 'NONE', #29500, #34522 ) ;
#13596=DIRECTION ( 'NONE',  ( 1.000000000000000000, 0.000000000000000000, 0.000000000000000000 ) ) ;
#13620=LINE ( 'NONE', #46494, #30467 ) ;
#13639=DIRECTION ( 'NONE',  ( 0.000000000000000000, 0.000000000000000000, -1.000000000000000000 ) ) ;
#13649=PRODUCT_DEFINITION_SHAPE ( 'NONE', 'NONE',  #1166 ) ;
#13654=AXIS2_PLACEMENT_3D ( 'NONE', #67878, #68584, #46651 ) ;
#13656=CIRCLE ( 'NONE', #53221, 5.000000000000000000 ) ;
#13661=AXIS2_PLACEMENT_3D ( 'NONE', #33025, #21375, #16077 ) ;
#13668=VERTEX_POINT ( 'NONE', #53462 ) ;
#13692=CARTESIAN_POINT ( 'NONE',  ( 0.2499999999999982236, -42.25000000000000000, 26.75000000000000000 ) ) ;
#13698=CARTESIAN_POINT ( 'NONE',  ( 275.0000000000000000, -38.65000000000095781, 14.49999999999903899 ) ) ;
#13730=ORIENTED_EDGE ( 'NONE', *, *, #11345, .F. ) ;
#13736=VERTEX_POINT ( 'NONE', #17697 ) ;
#13737=FACE_OUTER_BOUND ( 'NONE', #12223, .T. ) ;
#13739=EDGE_CURVE ( 'NONE', #12315, #69253, #6357, .T. ) ;
#13757=VECTOR ( 'NONE', #18225, 1000.000000000000000 ) ;
#13760=CARTESIAN_POINT ( 'NONE',  ( 283.0000000000000568, -26.28355339059299922, 9.766446609406699508 ) ) ;
#13768=CYLINDRICAL_SURFACE ( 'NONE', #10742, 1.999999999999314770 ) ;
#13772=AXIS2_PLACEMENT_3D ( 'NONE', #62209, #67873, #25091 ) ;
#13780=DIRECTION ( 'NONE',  ( 0.000000000000000000, -1.000000000000000000, 0.000000000000000000 ) ) ;
#13785=VERTEX_POINT ( 'NONE', #2127 ) ;
#13799=ORIENTED_EDGE ( 'NONE', *, *, #1493, .F. ) ;
#13802=CARTESIAN_POINT ( 'NONE',  ( 280.0000000000000000, -53.81370849898476649, -20.00000000000000000 ) ) ;
#13837=CARTESIAN_POINT ( 'NONE',  ( 283.0000000000000568, -32.94999999999885176, 7.700000000000000178 ) ) ;
#13849=AXIS2_PLACEMENT_3D ( 'NONE', #42291, #37016, #25706 ) ;
#13856=LINE ( 'NONE', #8899, #59301 ) ;
#13866=LINE ( 'NONE', #39686, #68043 ) ;
#13870=ORIENTED_EDGE ( 'NONE', *, *, #23861, .T. ) ;
#13874=CARTESIAN_POINT ( 'NONE',  ( 283.0000000000000568, -23.50007830495750127, 12.28007262201345995 ) ) ;
#13911=ORIENTED_EDGE ( 'NONE', *, *, #44360, .F. ) ;
#13920=DIRECTION ( 'NONE',  ( 0.000000000000000000, 1.000000000000000000, 0.000000000000000000 ) ) ;
#13923=CARTESIAN_POINT ( 'NONE',  ( 7.000000000000000000, -42.50000000000000000, 15.10000000000000142 ) ) ;
#13928=AXIS2_PLACEMENT_3D ( 'NONE', #23876, #67004, #40122 ) ;
#13942=DIRECTION ( 'NONE',  ( 0.000000000000000000, 0.000000000000000000, -1.000000000000000000 ) ) ;
#13945=CIRCLE ( 'NONE', #384, 4.000000000000000000 ) ;
#13950=DIRECTION ( 'NONE',  ( 1.000000000000000000, 0.000000000000000000, 0.000000000000000000 ) ) ;
#13962=ORIENTED_EDGE ( 'NONE', *, *, #21002, .T. ) ;
#13969=CARTESIAN_POINT ( 'NONE',  ( 283.0000000000000568, -32.94999999999885176, 7.700000000000000178 ) ) ;
#13970=LINE ( 'NONE', #68423, #51116 ) ;
#13981=DIRECTION ( 'NONE',  ( -1.000000000000000000, 0.000000000000000000, 0.000000000000000000 ) ) ;
#13983=ADVANCED_FACE ( 'NONE', ( #58337 ), #36767, .F. ) ;
#14001=ORIENTED_EDGE ( 'NONE', *, *, #17234, .F. ) ;
#14010=ORIENTED_EDGE ( 'NONE', *, *, #37707, .F. ) ;
#14011=ORIENTED_EDGE ( 'NONE', *, *, #26442, .T. ) ;
#14020=CARTESIAN_POINT ( 'NONE',  ( 7.000000000000000000, -26.42999999999999972, 5.874955318979029784 ) ) ;
#14037=DIRECTION ( 'NONE',  ( -0.5773502691896273964, -0.5773502691896268413, 0.5773502691896232886 ) ) ;
#14046=CARTESIAN_POINT ( 'NONE',  ( 289.5000000000000000, -0.5000000000000000000, 27.00000000000000000 ) ) ;
#14062=AXIS2_PLACEMENT_3D ( 'NONE', #51879, #41966, #63888 ) ;
#14064=CARTESIAN_POINT ( 'NONE',  ( 283.0000000000000568, -21.00000000000000000, -12.50000000000000000 ) ) ;
#14068=CARTESIAN_POINT ( 'NONE',  ( 7.000000000000000000, -41.99999999999906208, 14.49999999999903899 ) ) ;
#14080=CARTESIAN_POINT ( 'NONE',  ( 275.0000000000000000, -32.95000000000000284, -13.19999999999999929 ) ) ;
#14113=CARTESIAN_POINT ( 'NONE',  ( 275.0000000000000000, -42.00000000000000000, -15.10000000000000142 ) ) ;
#14122=VECTOR ( 'NONE', #22251, 1000.000000000000000 ) ;
#14137=ORIENTED_EDGE ( 'NONE', *, *, #57426, .T. ) ;
#14142=LINE ( 'NONE', #68948, #1598 ) ;
#14156=DIRECTION ( 'NONE',  ( 0.000000000000000000, 1.000000000000000000, 0.000000000000000000 ) ) ;
#14169=AXIS2_PLACEMENT_3D ( 'NONE', #50118, #44805, #12618 ) ;
#14176=CARTESIAN_POINT ( 'NONE',  ( 283.0000000000000568, -25.60000000000000142, 17.60000000000000142 ) ) ;
#14177=DIRECTION ( 'NONE',  ( 0.000000000000000000, 0.000000000000000000, -1.000000000000000000 ) ) ;
#14179=ORIENTED_EDGE ( 'NONE', *, *, #58140, .F. ) ;
#14202=ADVANCED_FACE ( 'NONE', ( #1353 ), #38497, .F. ) ;
#14212=AXIS2_PLACEMENT_3D ( 'NONE', #14676, #68422, #58532 ) ;
#14214=CARTESIAN_POINT ( 'NONE',  ( 7.000000000000000000, -23.70411739045900390, 12.50000000000000000 ) ) ;
#14218=FACE_OUTER_BOUND ( 'NONE', #9985, .T. ) ;
#14223=FACE_OUTER_BOUND ( 'NONE', #40104, .T. ) ;
#14235=CARTESIAN_POINT ( 'NONE',  ( 7.000000000000000000, -20.40000000000000213, 12.40000000000000213 ) ) ;
#14240=CARTESIAN_POINT ( 'NONE',  ( 7.000000000000000000, -25.93000000000544958, -9.412893218815410634 ) ) ;
#14262=CARTESIAN_POINT ( 'NONE',  ( 7.000000000000000000, -20.40000000000000213, -17.60000000000000142 ) ) ;
#14268=VERTEX_POINT ( 'NONE', #24660 ) ;
#14282=CARTESIAN_POINT ( 'NONE',  ( 7.000000000000000000, -20.40000000000000213, 12.40000000000000213 ) ) ;
#14303=CARTESIAN_POINT ( 'NONE',  ( 275.0000000000000000, -20.40000000000000213, -17.60000000000000142 ) ) ;
#14304=DIRECTION ( 'NONE',  ( 1.000000000000000000, 0.000000000000000000, 0.000000000000000000 ) ) ;
#14306=CARTESIAN_POINT ( 'NONE',  ( 283.0000000000000568, -20.40000000000000213, -12.40000000000000213 ) ) ;
#14307=EDGE_CURVE ( 'NONE', #44568, #44075, #57877, .T. ) ;
#14327=EDGE_CURVE ( 'NONE', #59333, #1005, #13346, .T. ) ;
#14331=DIRECTION ( 'NONE',  ( 0.000000000000000000, 0.7071067811865474617, 0.7071067811865474617 ) ) ;
#14348=EDGE_CURVE ( 'NONE', #10806, #34214, #41259, .T. ) ;
#14353=VECTOR ( 'NONE', #68375, 1000.000000000000114 ) ;
#14362=ORIENTED_EDGE ( 'NONE', *, *, #67780, .T. ) ;
#14368=ORIENTED_EDGE ( 'NONE', *, *, #64536, .F. ) ;
#14369=ORIENTED_EDGE ( 'NONE', *, *, #53600, .F. ) ;
#14388=EDGE_CURVE ( 'NONE', #21817, #44081, #48328, .T. ) ;
#14391=ORIENTED_EDGE ( 'NONE', *, *, #32593, .T. ) ;
#14400=CARTESIAN_POINT ( 'NONE',  ( 15.00000000000000000, -42.00000000000000000, 26.50000000000000000 ) ) ;
#14404=PLANE ( 'NONE',  #14062 ) ;
#14405=CARTESIAN_POINT ( 'NONE',  ( 283.0000000000000568, -23.29603921945599865, 12.50000000000000000 ) ) ;
#14413=ORIENTED_EDGE ( 'NONE', *, *, #5875, .T. ) ;
#14434=CARTESIAN_POINT ( 'NONE',  ( 275.0000000000000000, -21.00000000000000000, -12.50000000000000000 ) ) ;
#14441=VECTOR ( 'NONE', #64959, 1000.000000000000000 ) ;
#14442=FACE_OUTER_BOUND ( 'NONE', #66496, .T. ) ;
#14449=DIRECTION ( 'NONE',  ( 1.000000000000000000, -0.000000000000000000, -0.000000000000000000 ) ) ;
#14475=ORIENTED_EDGE ( 'NONE', *, *, #30616, .T. ) ;
#14477=EDGE_CURVE ( 'NONE', #596, #63351, #15462, .T. ) ;
#14481=DIRECTION ( 'NONE',  ( 0.000000000000000000, 0.000000000000000000, 1.000000000000000000 ) ) ;
#14492=CARTESIAN_POINT ( 'NONE',  ( 15.00000000000000000, -25.60000000000000142, 17.60000000000000142 ) ) ;
#14513=VERTEX_POINT ( 'NONE', #15105 ) ;
#14514=CARTESIAN_POINT ( 'NONE',  ( 283.0000000000000568, -20.50000000000000000, 17.00000000000000000 ) ) ;
#14535=CARTESIAN_POINT ( 'NONE',  ( 7.000000000000000000, -26.50000000000000000, -9.080000000000000071 ) ) ;
#14571=DIRECTION ( 'NONE',  ( 1.000000000000000000, 0.000000000000000000, 0.000000000000000000 ) ) ;
#14575=ORIENTED_EDGE ( 'NONE', *, *, #3486, .T. ) ;
#14587=ORIENTED_EDGE ( 'NONE', *, *, #48476, .T. ) ;
#14588=CIRCLE ( 'NONE', #63143, 4.000000000000000000 ) ;
#14593=ADVANCED_FACE ( 'NONE', ( #17875 ), #581, .F. ) ;
#14606=CARTESIAN_POINT ( 'NONE',  ( 7.000000000000000000, -32.44999999999905071, -14.49999999999906031 ) ) ;
#14608=EDGE_LOOP ( 'NONE', ( #6347, #59142, #12155 ) ) ;
#14609=ORIENTED_EDGE ( 'NONE', *, *, #8713, .T. ) ;
#14620=ORIENTED_EDGE ( 'NONE', *, *, #33890, .T. ) ;
#14631=VECTOR ( 'NONE', #31186, 1000.000000000000000 ) ;
#14656=ORIENTED_EDGE ( 'NONE', *, *, #47569, .F. ) ;
#14657=VECTOR ( 'NONE', #67741, 1000.000000000000000 ) ;
#14659=LINE ( 'NONE', #30571, #46761 ) ;
#14671=CARTESIAN_POINT ( 'NONE',  ( 283.0000000000000568, -37.15000000000001279, 7.700000000000000178 ) ) ;
#14672=ORIENTED_EDGE ( 'NONE', *, *, #11345, .T. ) ;
#14675=FACE_OUTER_BOUND ( 'NONE', #20236, .T. ) ;
#14676=CARTESIAN_POINT ( 'NONE',  ( 283.0000000000000568, -38.65000000000095781, 14.49999999999903899 ) ) ;
#14681=CARTESIAN_POINT ( 'NONE',  ( 280.0000000000000000, -20.40000000000000213, -16.00000000000000711 ) ) ;
#14685=EDGE_CURVE ( 'NONE', #40434, #56856, #29525, .T. ) ;
#14750=CARTESIAN_POINT ( 'NONE',  ( 275.5000000000001137, -42.00000000000004263, -26.99999999999991829 ) ) ;
#14766=ORIENTED_EDGE ( 'NONE', *, *, #58383, .T. ) ;
#14773=ORIENTED_EDGE ( 'NONE', *, *, #36236, .F. ) ;
#14803=ORIENTED_EDGE ( 'NONE', *, *, #64572, .T. ) ;
#14824=DIRECTION ( 'NONE',  ( 0.000000000000000000, 0.000000000000000000, -1.000000000000000000 ) ) ;
#14835=VECTOR ( 'NONE', #60044, 1000.000000000000000 ) ;
#14851=CARTESIAN_POINT ( 'NONE',  ( 277.3542486889354564, -25.50000000000000355, 17.00000000000000000 ) ) ;
#14889=ORIENTED_EDGE ( 'NONE', *, *, #62178, .T. ) ;
#14903=AXIS2_PLACEMENT_3D ( 'NONE', #59095, #63714, #47784 ) ;
#14910=VERTEX_POINT ( 'NONE', #59202 ) ;
#14911=CARTESIAN_POINT ( 'NONE',  ( 275.0000000000000000, -23.65000000000000568, 12.40000000000000213 ) ) ;
#14940=CARTESIAN_POINT ( 'NONE',  ( 7.000000000000000000, -38.15000000000000568, -14.50000000000000000 ) ) ;
#14945=ORIENTED_EDGE ( 'NONE', *, *, #50298, .T. ) ;
#14949=AXIS2_PLACEMENT_3D ( 'NONE', #13698, #35246, #62845 ) ;
#14952=AXIS2_PLACEMENT_3D ( 'NONE', #18727, #24738, #62919 ) ;
#14962=EDGE_CURVE ( 'NONE', #27615, #16092, #65545, .T. ) ;
#14972=ORIENTED_EDGE ( 'NONE', *, *, #24124, .T. ) ;
#14984=EDGE_CURVE ( 'NONE', #24256, #10988, #18748, .T. ) ;
#14986=DIRECTION ( 'NONE',  ( 0.000000000000000000, 1.000000000000000000, 0.000000000000000000 ) ) ;
#15002=CARTESIAN_POINT ( 'NONE',  ( 276.8775010008008053, -25.00000000000000000, 17.50000000000000000 ) ) ;
#15011=FACE_OUTER_BOUND ( 'NONE', #16900, .T. ) ;
#15012=CARTESIAN_POINT ( 'NONE',  ( 283.0000000000000568, -20.40000000000000213, -17.35424868893542438 ) ) ;
#15065=PLANE ( 'NONE',  #3070 ) ;
#15069=ADVANCED_FACE ( 'NONE', ( #48128 ), #32207, .F. ) ;
#15075=DIRECTION ( 'NONE',  ( -1.000000000000000000, 0.000000000000000000, 0.000000000000000000 ) ) ;
#15077=ORIENTED_EDGE ( 'NONE', *, *, #49300, .F. ) ;
#15078=VECTOR ( 'NONE', #44721, 1000.000000000000114 ) ;
#15081=FACE_OUTER_BOUND ( 'NONE', #760, .T. ) ;
#15097=VECTOR ( 'NONE', #49793, 1000.000000000000000 ) ;
#15104=CARTESIAN_POINT ( 'NONE',  ( 14.75000000000000000, -0.2500000000000020539, 26.75000000000000355 ) ) ;
#15105=CARTESIAN_POINT ( 'NONE',  ( 283.0000000000000568, -30.80000000000000071, 8.900000000000000355 ) ) ;
#15108=CYLINDRICAL_SURFACE ( 'NONE', #6015, 4.000000000000000000 ) ;
#15109=AXIS2_PLACEMENT_3D ( 'NONE', #18075, #18782, #67221 ) ;
#15121=EDGE_LOOP ( 'NONE', ( #42761, #46711, #21669, #62223 ) ) ;
#15132=DIRECTION ( 'NONE',  ( 0.000000000000000000, -1.000000000000000000, 3.819861094142539476E-12 ) ) ;
#15136=CARTESIAN_POINT ( 'NONE',  ( 7.000000000000000000, -27.13000000000000611, 15.49999999999930012 ) ) ;
#15154=AXIS2_PLACEMENT_3D ( 'NONE', #14240, #23792, #67979 ) ;
#15194=EDGE_LOOP ( 'NONE', ( #63831, #1330, #56010, #61899, #1416, #31452, #31672, #2602, #43534, #13587 ) ) ;
#15205=VERTEX_POINT ( 'NONE', #22635 ) ;
#15212=AXIS2_PLACEMENT_3D ( 'NONE', #57906, #63210, #15132 ) ;
#15221=DIRECTION ( 'NONE',  ( 0.000000000000000000, 1.000000000000000000, 0.000000000000000000 ) ) ;
#15222=ORIENTED_EDGE ( 'NONE', *, *, #26281, .T. ) ;
#15225=CARTESIAN_POINT ( 'NONE',  ( 7.000000000000000000, -26.50000000000000000, -9.080000000000000071 ) ) ;
#15244=LINE ( 'NONE', #26201, #4591 ) ;
#15247=AXIS2_PLACEMENT_3D ( 'NONE', #14080, #29995, #25051 ) ;
#15288=LINE ( 'NONE', #46399, #25212 ) ;
#15300=LINE ( 'NONE', #36881, #60263 ) ;
#15313=DIRECTION ( 'NONE',  ( -1.000000000000000000, 0.000000000000000000, 0.000000000000000000 ) ) ;
#15327=CARTESIAN_POINT ( 'NONE',  ( 290.0000000000000000, -42.00000000000000000, 26.50000000000000000 ) ) ;
#15339=LINE ( 'NONE', #63075, #23843 ) ;
#15356=CARTESIAN_POINT ( 'NONE',  ( 15.00000000000000000, -21.00000000000000000, 0.000000000000000000 ) ) ;
#15364=ADVANCED_FACE ( 'NONE', ( #56209 ), #66116, .F. ) ;
#15370=LINE ( 'NONE', #15716, #28603 ) ;
#15373=ORIENTED_EDGE ( 'NONE', *, *, #41471, .F. ) ;
#15407=ORIENTED_EDGE ( 'NONE', *, *, #44659, .F. ) ;
#15408=EDGE_LOOP ( 'NONE', ( #46697, #25665, #57490, #42571 ) ) ;
#15425=EDGE_CURVE ( 'NONE', #49993, #16188, #30028, .T. ) ;
#15440=EDGE_LOOP ( 'NONE', ( #58573, #30053, #54179, #63054 ) ) ;
#15451=LINE ( 'NONE', #41610, #10059 ) ;
#15453=DIRECTION ( 'NONE',  ( -0.5773502691896270633, -0.5773502691896270633, 0.5773502691896230665 ) ) ;
#15462=LINE ( 'NONE', #16496, #42440 ) ;
#15470=VECTOR ( 'NONE', #53098, 1000.000000000000000 ) ;
#15476=CARTESIAN_POINT ( 'NONE',  ( 10.62249899919925866, -21.00000000000000000, -17.50000000000000000 ) ) ;
#15492=CARTESIAN_POINT ( 'NONE',  ( 15.00000000000000000, -26.42999999999999972, 9.412893218813501051 ) ) ;
#15493=CARTESIAN_POINT ( 'NONE',  ( 7.000000000000000000, -53.81370849898476649, -16.03137303340311348 ) ) ;
#15496=EDGE_CURVE ( 'NONE', #38093, #69064, #3168, .T. ) ;
#15503=EDGE_CURVE ( 'NONE', #10975, #49352, #46287, .T. ) ;
#15516=CARTESIAN_POINT ( 'NONE',  ( 14.50000000000000711, -42.00000000000000000, 27.00000000000000355 ) ) ;
#15527=ORIENTED_EDGE ( 'NONE', *, *, #66179, .F. ) ;
#15534=EDGE_CURVE ( 'NONE', #187, #20252, #10217, .T. ) ;
#15550=CARTESIAN_POINT ( 'NONE',  ( 283.0000000000000568, -30.80000000000000071, 8.900000000000000355 ) ) ;
#15555=DIRECTION ( 'NONE',  ( 0.000000000000000000, 1.000000000000000000, 0.000000000000000000 ) ) ;
#15559=ADVANCED_FACE ( 'NONE', ( #53362 ), #54398, .F. ) ;
#15582=CARTESIAN_POINT ( 'NONE',  ( 283.0000000000000568, -30.45000000000000639, 15.00000000000000000 ) ) ;
#15590=ORIENTED_EDGE ( 'NONE', *, *, #63017, .T. ) ;
#15617=CARTESIAN_POINT ( 'NONE',  ( 280.0000000000000000, -20.40000000000000213, -20.00000000000000000 ) ) ;
#15624=EDGE_LOOP ( 'NONE', ( #1791, #36698, #7118, #52714 ) ) ;
#15628=DIRECTION ( 'NONE',  ( 0.000000000000000000, 0.000000000000000000, -1.000000000000000000 ) ) ;
#15646=ORIENTED_EDGE ( 'NONE', *, *, #59666, .T. ) ;
#15647=VERTEX_POINT ( 'NONE', #69958 ) ;
#15660=ORIENTED_EDGE ( 'NONE', *, *, #59121, .F. ) ;
#15673=CARTESIAN_POINT ( 'NONE',  ( 7.000000000000000000, -31.99999999999889866, -7.899999999997660893 ) ) ;
#15688=CARTESIAN_POINT ( 'NONE',  ( 7.000000000000000000, -25.93000000000544958, 9.412893218815410634 ) ) ;
#15706=VECTOR ( 'NONE', #28037, 1000.000000000000000 ) ;
#15713=VERTEX_POINT ( 'NONE', #23583 ) ;
#15714=DIRECTION ( 'NONE',  ( 0.000000000000000000, 0.6801302850037830305, 0.7330912599538155217 ) ) ;
#15716=CARTESIAN_POINT ( 'NONE',  ( 7.000000000000000000, -53.81370849898476649, 16.03137303340311348 ) ) ;
#15728=CARTESIAN_POINT ( 'NONE',  ( 283.0000000000000568, -26.42999999999999972, -9.412893218813501051 ) ) ;
#15751=EDGE_LOOP ( 'NONE', ( #31310, #24369, #10588, #56697 ) ) ;
#15753=EDGE_LOOP ( 'NONE', ( #23271, #15870, #24233, #37132 ) ) ;
#15754=VERTEX_POINT ( 'NONE', #45851 ) ;
#15756=EDGE_CURVE ( 'NONE', #31741, #32653, #55771, .T. ) ;
#15766=CARTESIAN_POINT ( 'NONE',  ( 277.3542486889354564, -25.50000000000000355, -17.00000000000000000 ) ) ;
#15772=AXIS2_PLACEMENT_3D ( 'NONE', #20525, #63317, #31851 ) ;
#15776=CARTESIAN_POINT ( 'NONE',  ( 0.5000000000000000000, -42.50000000000000000, -26.50000000000000000 ) ) ;
#15787=LINE ( 'NONE', #4836, #42805 ) ;
#15789=ADVANCED_FACE ( 'NONE', ( #22898 ), #55095, .F. ) ;
#15818=ORIENTED_EDGE ( 'NONE', *, *, #50967, .F. ) ;
#15826=LINE ( 'NONE', #32092, #67219 ) ;
#15831=DIRECTION ( 'NONE',  ( 0.000000000000000000, -1.000000000000000000, 0.000000000000000000 ) ) ;
#15835=EDGE_CURVE ( 'NONE', #62476, #28935, #29228, .T. ) ;
#15854=VECTOR ( 'NONE', #33052, 1000.000000000000114 ) ;
#15855=ORIENTED_EDGE ( 'NONE', *, *, #21022, .F. ) ;
#15856=ADVANCED_FACE ( 'NONE', ( #30301 ), #3770, .F. ) ;
#15861=ORIENTED_EDGE ( 'NONE', *, *, #62189, .T. ) ;
#15864=VECTOR ( 'NONE', #65769, 1000.000000000000000 ) ;
#15865=VECTOR ( 'NONE', #58889, 1000.000000000000000 ) ;
#15870=ORIENTED_EDGE ( 'NONE', *, *, #6165, .T. ) ;
#15880=LINE ( 'NONE', #15550, #6264 ) ;
#15883=DIRECTION ( 'NONE',  ( 1.000000000000000000, -0.000000000000000000, -0.000000000000000000 ) ) ;
#15884=ORIENTED_EDGE ( 'NONE', *, *, #5165, .T. ) ;
#15899=CARTESIAN_POINT ( 'NONE',  ( 275.0000000000000000, -25.60000000000000142, -15.10000000000000142 ) ) ;
#15923=VERTEX_POINT ( 'NONE', #3085 ) ;
#15924=EDGE_CURVE ( 'NONE', #3096, #46362, #67468, .T. ) ;
#15936=DIRECTION ( 'NONE',  ( 0.000000000000000000, 0.000000000000000000, 1.000000000000000000 ) ) ;
#15954=DIRECTION ( 'NONE',  ( -1.000000000000000000, 0.000000000000000000, 0.000000000000000000 ) ) ;
#15963=DIRECTION ( 'NONE',  ( 0.000000000000000000, -1.000000000000000000, 0.000000000000000000 ) ) ;
#16026=ORIENTED_EDGE ( 'NONE', *, *, #46777, .F. ) ;
#16027=ORIENTED_EDGE ( 'NONE', *, *, #65262, .T. ) ;
#16034=DIRECTION ( 'NONE',  ( -1.000000000000000000, 0.000000000000000000, 0.000000000000000000 ) ) ;
#16036=ORIENTED_EDGE ( 'NONE', *, *, #59121, .T. ) ;
#16038=CARTESIAN_POINT ( 'NONE',  ( 7.500000000000000000, -25.50000000000000355, -20.00000000000000000 ) ) ;
#16057=CIRCLE ( 'NONE', #32854, 0.9999999999984570120 ) ;
#16077=DIRECTION ( 'NONE',  ( 1.000000000000000000, 0.000000000000000000, 0.000000000000000000 ) ) ;
#16091=CARTESIAN_POINT ( 'NONE',  ( 15.00000000000000000, -42.00000000000000000, 26.50000000000000000 ) ) ;
#16092=VERTEX_POINT ( 'NONE', #14214 ) ;
#16097=VERTEX_POINT ( 'NONE', #38727 ) ;
#16099=ORIENTED_EDGE ( 'NONE', *, *, #61832, .T. ) ;
#16120=DIRECTION ( 'NONE',  ( -1.000000000000000000, 0.000000000000000000, 0.000000000000000000 ) ) ;
#16147=ADVANCED_FACE ( 'NONE', ( #30130 ), #65937, .T. ) ;
#16165=VERTEX_POINT ( 'NONE', #56990 ) ;
#16173=EDGE_LOOP ( 'NONE', ( #16888, #18937, #14609, #23452, #53511, #38840 ) ) ;
#16188=VERTEX_POINT ( 'NONE', #17509 ) ;
#16197=ORIENTED_EDGE ( 'NONE', *, *, #22467, .T. ) ;
#16203=ORIENTED_EDGE ( 'NONE', *, *, #35561, .T. ) ;
#16240=LINE ( 'NONE', #21551, #10704 ) ;
#16242=ORIENTED_EDGE ( 'NONE', *, *, #32361, .F. ) ;
#16274=ORIENTED_EDGE ( 'NONE', *, *, #2947, .T. ) ;
#16293=CARTESIAN_POINT ( 'NONE',  ( 14.75000000000000178, -0.2500000000000059952, 26.75000000000000000 ) ) ;
#16306=FACE_OUTER_BOUND ( 'NONE', #15408, .T. ) ;
#16310=ORIENTED_EDGE ( 'NONE', *, *, #68248, .F. ) ;
#16311=CARTESIAN_POINT ( 'NONE',  ( 7.000000000000000000, -25.93000000000544958, -9.412893218815410634 ) ) ;
#16327=CARTESIAN_POINT ( 'NONE',  ( 283.0000000000000568, -27.13000000000000611, 15.49999999999930012 ) ) ;
#16331=EDGE_CURVE ( 'NONE', #68520, #33439, #36480, .T. ) ;
#16357=ORIENTED_EDGE ( 'NONE', *, *, #11207, .T. ) ;
#16360=CARTESIAN_POINT ( 'NONE',  ( 275.0000000000000000, -25.00000000000299849, -9.079999998829670460 ) ) ;
#16373=CYLINDRICAL_SURFACE ( 'NONE', #33983, 0.9999999999984552357 ) ;
#16392=DIRECTION ( 'NONE',  ( 0.000000000000000000, -1.000000000000000000, 1.540434446669787085E-12 ) ) ;
#16401=ADVANCED_FACE ( 'NONE', ( #12022 ), #39257, .T. ) ;
#16420=CARTESIAN_POINT ( 'NONE',  ( 7.000000000000000000, -26.50000000000000000, -5.530822723609929881 ) ) ;
#16459=DIRECTION ( 'NONE',  ( 1.000000000000000000, -0.000000000000000000, -0.000000000000000000 ) ) ;
#16460=CARTESIAN_POINT ( 'NONE',  ( 15.00000000000000000, -21.00000000000000000, 0.000000000000000000 ) ) ;
#16479=DIRECTION ( 'NONE',  ( 0.000000000000000000, -1.000000000000000000, 0.000000000000000000 ) ) ;
#16486=VERTEX_POINT ( 'NONE', #60474 ) ;
#16496=CARTESIAN_POINT ( 'NONE',  ( 290.0000000000000000, -0.5000000000000000000, 26.50000000000000000 ) ) ;
#16509=ORIENTED_EDGE ( 'NONE', *, *, #45677, .F. ) ;
#16527=DIRECTION ( 'NONE',  ( 0.000000000000000000, 0.000000000000000000, 1.000000000000000000 ) ) ;
#16566=CARTESIAN_POINT ( 'NONE',  ( 283.0000000000000568, -26.28355339059299922, 9.766446609406699508 ) ) ;
#16568=DIRECTION ( 'NONE',  ( 0.000000000000000000, 0.000000000000000000, -1.000000000000000000 ) ) ;
#16576=ORIENTED_EDGE ( 'NONE', *, *, #40898, .T. ) ;
#16591=CARTESIAN_POINT ( 'NONE',  ( 0.000000000000000000, -21.00000000000000000, 0.000000000000000000 ) ) ;
#16594=ORIENTED_EDGE ( 'NONE', *, *, #49192, .F. ) ;
#16619=PRODUCT_DEFINITION_FORMATION_WITH_SPECIFIED_SOURCE ( 'ANY', '', #67289, .NOT_KNOWN. ) ;
#16623=VECTOR ( 'NONE', #17968, 1000.000000000000000 ) ;
#16656=FACE_OUTER_BOUND ( 'NONE', #25776, .T. ) ;
#16693=ORIENTED_EDGE ( 'NONE', *, *, #42767, .T. ) ;
#16713=VECTOR ( 'NONE', #43240, 1000.000000000000000 ) ;
#16721=LINE ( 'NONE', #59840, #41084 ) ;
#16729=AXIS2_PLACEMENT_3D ( 'NONE', #1582, #39756, #67351 ) ;
#16773=CIRCLE ( 'NONE', #27015, 7.800000000000000711 ) ;
#16774=CARTESIAN_POINT ( 'NONE',  ( 7.000000000000000000, -24.99999999999915090, 9.080000000000110205 ) ) ;
#16786=LINE ( 'NONE', #64197, #26998 ) ;
#16805=VERTEX_POINT ( 'NONE', #59013 ) ;
#16806=EDGE_CURVE ( 'NONE', #10944, #21570, #11937, .T. ) ;
#16814=LINE ( 'NONE', #39401, #4103 ) ;
#16816=ORIENTED_EDGE ( 'NONE', *, *, #40814, .T. ) ;
#16820=CARTESIAN_POINT ( 'NONE',  ( 275.0000000000000000, -32.44999999999905071, -14.49999999999906031 ) ) ;
#16822=VERTEX_POINT ( 'NONE', #48409 ) ;
#16824=DIRECTION ( 'NONE',  ( 0.000000000000000000, 0.7071067811865470176, 0.7071067811865480168 ) ) ;
#16833=DIRECTION ( 'NONE',  ( -0.7071067811865474617, 0.000000000000000000, 0.7071067811865474617 ) ) ;
#16858=FACE_OUTER_BOUND ( 'NONE', #23020, .T. ) ;
#16859=ORIENTED_EDGE ( 'NONE', *, *, #32941, .F. ) ;
#16861=ORIENTED_EDGE ( 'NONE', *, *, #44466, .T. ) ;
#16865=AXIS2_PLACEMENT_3D ( 'NONE', #69808, #60219, #15714 ) ;
#16868=VERTEX_POINT ( 'NONE', #44461 ) ;
#16888=ORIENTED_EDGE ( 'NONE', *, *, #12538, .T. ) ;
#16891=CARTESIAN_POINT ( 'NONE',  ( 7.000000000000000000, -37.61196062927500350, -8.008708659369300875 ) ) ;
#16900=EDGE_LOOP ( 'NONE', ( #27648, #12667, #31752, #17094 ) ) ;
#16915=CARTESIAN_POINT ( 'NONE',  ( 15.00000000000000000, 0.000000000000000000, 26.50000000000000000 ) ) ;
#16940=CARTESIAN_POINT ( 'NONE',  ( 290.0000000000000000, 0.000000000000000000, -27.00000000000000000 ) ) ;
#16945=EDGE_CURVE ( 'NONE', #47930, #10503, #56473, .T. ) ;
#16952=CARTESIAN_POINT ( 'NONE',  ( 7.000000000000000000, -25.60000000000000142, 17.60000000000000142 ) ) ;
#16956=CIRCLE ( 'NONE', #66605, 0.5000000000009441337 ) ;
#16958=CARTESIAN_POINT ( 'NONE',  ( 283.0000000000000568, -25.50000000000000355, 17.00000000000000000 ) ) ;
#16971=ORIENTED_EDGE ( 'NONE', *, *, #29356, .F. ) ;
#16980=EDGE_CURVE ( 'NONE', #54503, #37771, #24299, .T. ) ;
#16985=ORIENTED_EDGE ( 'NONE', *, *, #53970, .F. ) ;
#16987=ORIENTED_EDGE ( 'NONE', *, *, #12445, .T. ) ;
#16996=ORIENTED_EDGE ( 'NONE', *, *, #57837, .T. ) ;
#17001=DIRECTION ( 'NONE',  ( 1.000000000000000000, 0.000000000000000000, 0.000000000000000000 ) ) ;
#17017=DIRECTION ( 'NONE',  ( -0.7071067811865474617, 0.7071067811865474617, 0.000000000000000000 ) ) ;
#17022=CARTESIAN_POINT ( 'NONE',  ( 283.0000000000000568, -20.50000000000000000, -17.00000000000000000 ) ) ;
#17035=VECTOR ( 'NONE', #62079, 1000.000000000000000 ) ;
#17042=ORIENTED_EDGE ( 'NONE', *, *, #39700, .F. ) ;
#17055=VERTEX_POINT ( 'NONE', #30658 ) ;
#17056=VECTOR ( 'NONE', #1523, 1000.000000000000000 ) ;
#17068=EDGE_CURVE ( 'NONE', #10448, #39282, #63545, .T. ) ;
#17072=DIRECTION ( 'NONE',  ( 1.000000000000000000, 0.000000000000000000, 0.000000000000000000 ) ) ;
#17094=ORIENTED_EDGE ( 'NONE', *, *, #53600, .T. ) ;
#17105=VERTEX_POINT ( 'NONE', #52947 ) ;
#17107=ADVANCED_FACE ( 'NONE', ( #10143, #26069 ), #14404, .T. ) ;
#17110=DIRECTION ( 'NONE',  ( 0.000000000000000000, -0.7071067811865475727, 0.7071067811865475727 ) ) ;
#17128=VECTOR ( 'NONE', #11481, 1000.000000000000000 ) ;
#17144=LINE ( 'NONE', #204, #5370 ) ;
#17150=CARTESIAN_POINT ( 'NONE',  ( 290.0000000000000000, -21.00000000000000000, -5.000000000000000000 ) ) ;
#17164=DIRECTION ( 'NONE',  ( 0.000000000000000000, -1.000000000000000000, 0.000000000000000000 ) ) ;
#17169=EDGE_CURVE ( 'NONE', #38450, #59333, #31008, .T. ) ;
#17185=EDGE_CURVE ( 'NONE', #9319, #1040, #4842, .T. ) ;
#17190=ORIENTED_EDGE ( 'NONE', *, *, #66183, .T. ) ;
#17205=DIRECTION ( 'NONE',  ( 0.000000000000000000, 1.000000000000000000, 0.000000000000000000 ) ) ;
#17234=EDGE_CURVE ( 'NONE', #44081, #992, #38077, .T. ) ;
#17241=CARTESIAN_POINT ( 'NONE',  ( 15.00000000000000000, -21.00000000000000000, 0.000000000000000000 ) ) ;
#17243=DIRECTION ( 'NONE',  ( 0.000000000000000000, 1.000000000000000000, 0.000000000000000000 ) ) ;
#17267=AXIS2_PLACEMENT_3D ( 'NONE', #10980, #54466, #726 ) ;
#17293=ORIENTED_EDGE ( 'NONE', *, *, #18680, .T. ) ;
#17296=VECTOR ( 'NONE', #35096, 1000.000000000000000 ) ;
#17302=VECTOR ( 'NONE', #15313, 1000.000000000000000 ) ;
#17306=DIRECTION ( 'NONE',  ( 0.000000000000000000, 0.000000000000000000, -1.000000000000000000 ) ) ;
#17319=DIRECTION ( 'NONE',  ( 0.000000000000000000, -1.000000000000000000, 0.000000000000000000 ) ) ;
#17325=CARTESIAN_POINT ( 'NONE',  ( 283.0000000000000568, -23.65000000000000568, -12.40000000000000213 ) ) ;
#17331=VERTEX_POINT ( 'NONE', #34460 ) ;
#17334=PRESENTATION_STYLE_ASSIGNMENT (( #26929 ) ) ;
#17335=CARTESIAN_POINT ( 'NONE',  ( 7.000000000000000000, -28.94999999999999929, 13.50000000000000000 ) ) ;
#17338=CARTESIAN_POINT ( 'NONE',  ( 15.00000000000000000, -20.40000000000000213, -17.60000000000000142 ) ) ;
#17339=ORIENTED_EDGE ( 'NONE', *, *, #31834, .F. ) ;
#17342=DIRECTION ( 'NONE',  ( 1.000000000000000000, -0.000000000000000000, -0.000000000000000000 ) ) ;
#17353=CIRCLE ( 'NONE', #10551, 7.800000000000000711 ) ;
#17404=CARTESIAN_POINT ( 'NONE',  ( 275.2499999999998295, -42.24999999999996447, 26.75000000000008527 ) ) ;
#17425=VERTEX_POINT ( 'NONE', #9000 ) ;
#17431=ORIENTED_EDGE ( 'NONE', *, *, #27621, .F. ) ;
#17438=CARTESIAN_POINT ( 'NONE',  ( 1.000000000000000000, -21.00000000000000000, 0.000000000000000000 ) ) ;
#17441=ORIENTED_EDGE ( 'NONE', *, *, #49220, .T. ) ;
#17446=VECTOR ( 'NONE', #61908, 1000.000000000000114 ) ;
#17448=DIRECTION ( 'NONE',  ( 0.000000000000000000, 0.000000000000000000, -1.000000000000000000 ) ) ;
#17501=FACE_OUTER_BOUND ( 'NONE', #39885, .T. ) ;
#17504=FACE_OUTER_BOUND ( 'NONE', #63465, .T. ) ;
#17509=CARTESIAN_POINT ( 'NONE',  ( 283.0000000000000568, -25.60000000000000142, 15.10000000000000142 ) ) ;
#17524=CARTESIAN_POINT ( 'NONE',  ( 15.00000000000000000, -21.00000000000000000, 0.000000000000000000 ) ) ;
#17588=DIRECTION ( 'NONE',  ( -1.000000000000000000, 0.000000000000000000, 0.000000000000000000 ) ) ;
#17596=DIRECTION ( 'NONE',  ( -1.000000000000000000, 0.000000000000000000, 0.000000000000000000 ) ) ;
#17601=VERTEX_POINT ( 'NONE', #47883 ) ;
#17604=VERTEX_POINT ( 'NONE', #59200 ) ;
#17605=CARTESIAN_POINT ( 'NONE',  ( 15.00000000000000000, -42.50000000000000000, -26.50000000000000000 ) ) ;
#17625=ORIENTED_EDGE ( 'NONE', *, *, #22120, .F. ) ;
#17647=VECTOR ( 'NONE', #43139, 1000.000000000000000 ) ;
#17652=EDGE_CURVE ( 'NONE', #41347, #20252, #21014, .T. ) ;
#17656=DIRECTION ( 'NONE',  ( -1.000000000000000000, 0.000000000000000000, 0.000000000000000000 ) ) ;
#17685=EDGE_CURVE ( 'NONE', #31223, #23962, #43634, .T. ) ;
#17686=CARTESIAN_POINT ( 'NONE',  ( 283.0000000000000568, -26.42999999999999972, -9.412893218813501051 ) ) ;
#17697=CARTESIAN_POINT ( 'NONE',  ( 275.0000000000000000, -25.60000000000000142, -17.60000000000000142 ) ) ;
#17715=CIRCLE ( 'NONE', #65188, 4.000000000000000000 ) ;
#17729=CARTESIAN_POINT ( 'NONE',  ( 290.0000000000000000, -21.00000000000000000, 0.000000000000000000 ) ) ;
#17738=DIRECTION ( 'NONE',  ( 1.000000000000000000, -0.000000000000000000, -0.000000000000000000 ) ) ;
#17745=ORIENTED_EDGE ( 'NONE', *, *, #13231, .T. ) ;
#17764=CYLINDRICAL_SURFACE ( 'NONE', #2162, 1.500000000000849543 ) ;
#17798=CARTESIAN_POINT ( 'NONE',  ( 283.0000000000000568, -32.00000000000000000, 8.400000000000000355 ) ) ;
#17804=CARTESIAN_POINT ( 'NONE',  ( 289.9999999999998295, -0.5000000000000426326, -26.49999999999991829 ) ) ;
#17828=EDGE_LOOP ( 'NONE', ( #61613, #39626, #25049, #56110 ) ) ;
#17834=LINE ( 'NONE', #6542, #15854 ) ;
#17843=DIRECTION ( 'NONE',  ( 0.000000000000000000, 0.000000000000000000, 1.000000000000000000 ) ) ;
#17844=LINE ( 'NONE', #39063, #42450 ) ;
#17875=FACE_OUTER_BOUND ( 'NONE', #25509, .T. ) ;
#17905=DIRECTION ( 'NONE',  ( 1.000000000000000000, -0.000000000000000000, -0.000000000000000000 ) ) ;
#17925=DIRECTION ( 'NONE',  ( -0.000000000000000000, -1.000000000000000000, -0.000000000000000000 ) ) ;
#17929=CARTESIAN_POINT ( 'NONE',  ( 289.7500000000000000, -0.2500000000000106581, -26.74999999999999645 ) ) ;
#17938=VECTOR ( 'NONE', #54921, 1000.000000000000000 ) ;
#17954=LINE ( 'NONE', #38502, #15097 ) ;
#17959=CIRCLE ( 'NONE', #13426, 3.999999999999993339 ) ;
#17962=ORIENTED_EDGE ( 'NONE', *, *, #31515, .T. ) ;
#17968=DIRECTION ( 'NONE',  ( 0.000000000000000000, -1.000000000000000000, 0.000000000000000000 ) ) ;
#17970=EDGE_CURVE ( 'NONE', #35311, #43920, #4346, .T. ) ;
#17974=PLANE ( 'NONE',  #32176 ) ;
#17984=DIRECTION ( 'NONE',  ( -0.7071067811865480168, 0.000000000000000000, 0.7071067811865470176 ) ) ;
#17985=AXIS2_PLACEMENT_3D ( 'NONE', #32072, #57885, #52601 ) ;
#17990=DIRECTION ( 'NONE',  ( 1.000000000000000000, -0.000000000000000000, -0.000000000000000000 ) ) ;
#17999=CARTESIAN_POINT ( 'NONE',  ( 289.7500000000000000, -42.25000000000000000, 26.75000000000000000 ) ) ;
#18003=CARTESIAN_POINT ( 'NONE',  ( 7.000000000000000000, -25.50000000000000355, -16.03137303340311348 ) ) ;
#18033=CIRCLE ( 'NONE', #50786, 1.500000000000850875 ) ;
#18046=PLANE ( 'NONE',  #47952 ) ;
#18048=ORIENTED_EDGE ( 'NONE', *, *, #37514, .T. ) ;
#18055=CARTESIAN_POINT ( 'NONE',  ( 275.0000000000000000, -42.00000000000000000, 7.000000000000000000 ) ) ;
#18057=DIRECTION ( 'NONE',  ( 0.000000000000000000, -1.000000000000000000, 0.000000000000000000 ) ) ;
#18060=AXIS2_PLACEMENT_3D ( 'NONE', #51476, #13639, #55736 ) ;
#18061=CARTESIAN_POINT ( 'NONE',  ( 283.0000000000000568, -30.45000000000094786, 14.49999999999906031 ) ) ;
#18072=CARTESIAN_POINT ( 'NONE',  ( 10.70000000000000107, -20.40000000000000213, -17.60000000000000142 ) ) ;
#18075=CARTESIAN_POINT ( 'NONE',  ( 7.000000000000000000, -21.00000000000000000, 0.000000000000000000 ) ) ;
#18078=VERTEX_POINT ( 'NONE', #681 ) ;
#18090=CARTESIAN_POINT ( 'NONE',  ( 283.0000000000000568, -23.70411739045900390, -12.50000000000000000 ) ) ;
#18094=VECTOR ( 'NONE', #19688, 1000.000000000000000 ) ;
#18116=EDGE_CURVE ( 'NONE', #67984, #2683, #10781, .T. ) ;
#18124=ORIENTED_EDGE ( 'NONE', *, *, #33711, .F. ) ;
#18128=EDGE_LOOP ( 'NONE', ( #67181, #42851, #66485, #36685 ) ) ;
#18136=LINE ( 'NONE', #17798, #66707 ) ;
#18144=CIRCLE ( 'NONE', #68989, 7.799999999999999822 ) ;
#18145=CARTESIAN_POINT ( 'NONE',  ( 277.1811023147819810, -20.65270074880750073, 17.15270074880750784 ) ) ;
#18154=CARTESIAN_POINT ( 'NONE',  ( 283.0000000000000568, -28.95000000000155183, -14.49999999999845990 ) ) ;
#18162=AXIS2_PLACEMENT_3D ( 'NONE', #65685, #27514, #16568 ) ;
#18174=CARTESIAN_POINT ( 'NONE',  ( 289.5000000000000000, -0.5000000000000000000, -27.00000000000000000 ) ) ;
#18187=DIRECTION ( 'NONE',  ( 0.000000000000000000, 0.000000000000000000, 1.000000000000000000 ) ) ;
#18198=ORIENTED_EDGE ( 'NONE', *, *, #20613, .T. ) ;
#18205=ORIENTED_EDGE ( 'NONE', *, *, #22531, .T. ) ;
#18217=DIRECTION ( 'NONE',  ( 0.000000000000000000, 0.000000000000000000, 1.000000000000000000 ) ) ;
#18220=ORIENTED_EDGE ( 'NONE', *, *, #68443, .F. ) ;
#18225=DIRECTION ( 'NONE',  ( -0.000000000000000000, -1.000000000000000000, -0.000000000000000000 ) ) ;
#18241=FACE_OUTER_BOUND ( 'NONE', #49656, .T. ) ;
#18244=ORIENTED_EDGE ( 'NONE', *, *, #45580, .F. ) ;
#18255=DIRECTION ( 'NONE',  ( 0.000000000000000000, 1.000000000000000000, 0.000000000000000000 ) ) ;
#18267=EDGE_CURVE ( 'NONE', #57192, #25545, #33401, .T. ) ;
#18286=ORIENTED_EDGE ( 'NONE', *, *, #61797, .T. ) ;
#18297=ORIENTED_EDGE ( 'NONE', *, *, #41991, .F. ) ;
#18298=DIRECTION ( 'NONE',  ( 1.000000000000000000, -0.000000000000000000, -0.000000000000000000 ) ) ;
#18299=VERTEX_POINT ( 'NONE', #26078 ) ;
#18306=DIRECTION ( 'NONE',  ( 1.000000000000000000, -0.000000000000000000, -0.000000000000000000 ) ) ;
#18318=ORIENTED_EDGE ( 'NONE', *, *, #29679, .F. ) ;
#18329=DIRECTION ( 'NONE',  ( 0.000000000000000000, -2.206568261432184716E-12, 1.000000000000000000 ) ) ;
#18365=EDGE_CURVE ( 'NONE', #57368, #47821, #57538, .T. ) ;
#18373=CARTESIAN_POINT ( 'NONE',  ( 15.00000000000000000, -42.00000000000000000, 27.00000000000000000 ) ) ;
#18377=CARTESIAN_POINT ( 'NONE',  ( 283.0000000000000568, -38.64999999999999858, 12.69999999999999929 ) ) ;
#18393=VECTOR ( 'NONE', #22684, 1000.000000000000000 ) ;
#18405=ORIENTED_EDGE ( 'NONE', *, *, #42787, .T. ) ;
#18439=CARTESIAN_POINT ( 'NONE',  ( 276.8775010008008053, -21.00000000000000000, -17.50000000000000000 ) ) ;
#18452=AXIS2_PLACEMENT_3D ( 'NONE', #1466, #17738, #12407 ) ;
#18462=CARTESIAN_POINT ( 'NONE',  ( 276.8000000000000682, -20.40000000000000213, -17.60000000000000142 ) ) ;
#18466=EDGE_LOOP ( 'NONE', ( #46785, #7341, #50584, #8667 ) ) ;
#18515=EDGE_LOOP ( 'NONE', ( #29477, #64620, #19098, #59311 ) ) ;
#18523=AXIS2_PLACEMENT_3D ( 'NONE', #37923, #26962, #65480 ) ;
#18535=CARTESIAN_POINT ( 'NONE',  ( 283.0000000000000568, -26.50000000000000000, -9.080000000000000071 ) ) ;
#18565=CARTESIAN_POINT ( 'NONE',  ( 283.0000000000000568, -26.79000000000000625, 0.000000000000000000 ) ) ;
#18582=EDGE_CURVE ( 'NONE', #51967, #21925, #43595, .T. ) ;
#18586=ORIENTED_EDGE ( 'NONE', *, *, #10090, .T. ) ;
#18590=ORIENTED_EDGE ( 'NONE', *, *, #41107, .T. ) ;
#18598=ORIENTED_EDGE ( 'NONE', *, *, #26782, .F. ) ;
#18609=CIRCLE ( 'NONE', #59261, 3.999999999999993339 ) ;
#18617=VERTEX_POINT ( 'NONE', #40129 ) ;
#18618=VECTOR ( 'NONE', #64225, 1000.000000000000000 ) ;
#18627=EDGE_CURVE ( 'NONE', #69122, #65979, #54915, .T. ) ;
#18644=ORIENTED_EDGE ( 'NONE', *, *, #63874, .T. ) ;
#18680=EDGE_CURVE ( 'NONE', #13213, #10975, #28878, .T. ) ;
#18727=CARTESIAN_POINT ( 'NONE',  ( 275.0000000000000000, -23.50007830495750127, 12.28007262201345995 ) ) ;
#18741=CARTESIAN_POINT ( 'NONE',  ( 283.0000000000000568, -27.13000000000000611, -15.49999999999930012 ) ) ;
#18748=CIRCLE ( 'NONE', #58292, 4.000000000000000000 ) ;
#18751=ORIENTED_EDGE ( 'NONE', *, *, #38413, .T. ) ;
#18752=VERTEX_POINT ( 'NONE', #13969 ) ;
#18755=AXIS2_PLACEMENT_3D ( 'NONE', #22721, #58829, #37609 ) ;
#18763=VERTEX_POINT ( 'NONE', #57106 ) ;
#18782=DIRECTION ( 'NONE',  ( 1.000000000000000000, 0.000000000000000000, 0.000000000000000000 ) ) ;
#18791=AXIS2_PLACEMENT_3D ( 'NONE', #41515, #41861, #4405 ) ;
#18813=EDGE_CURVE ( 'NONE', #42028, #13533, #4439, .T. ) ;
#18814=CARTESIAN_POINT ( 'NONE',  ( 275.0000000000000000, -23.65000000000000568, -12.40000000000000213 ) ) ;
#18836=ADVANCED_FACE ( 'NONE', ( #6157 ), #27384, .T. ) ;
#18854=VECTOR ( 'NONE', #14824, 1000.000000000000000 ) ;
#18857=DIRECTION ( 'NONE',  ( 0.000000000000000000, -1.000000000000000000, 0.000000000000000000 ) ) ;
#18862=DIRECTION ( 'NONE',  ( 1.000000000000000000, -0.000000000000000000, -0.000000000000000000 ) ) ;
#18868=ORIENTED_EDGE ( 'NONE', *, *, #45240, .T. ) ;
#18878=ORIENTED_EDGE ( 'NONE', *, *, #38889, .F. ) ;
#18895=DIRECTION ( 'NONE',  ( 0.000000000000000000, 0.7066873191085843997, 0.7075259945833241026 ) ) ;
#18908=AXIS2_PLACEMENT_3D ( 'NONE', #19670, #20387, #36298 ) ;
#18913=AXIS2_PLACEMENT_3D ( 'NONE', #28355, #16034, #466 ) ;
#18935=CARTESIAN_POINT ( 'NONE',  ( 6.884529946162100345, -21.00000000000000000, 0.000000000000000000 ) ) ;
#18937=ORIENTED_EDGE ( 'NONE', *, *, #22222, .T. ) ;
#18941=EDGE_CURVE ( 'NONE', #54968, #56561, #43650, .T. ) ;
#18944=VERTEX_POINT ( 'NONE', #48952 ) ;
#18961=EDGE_LOOP ( 'NONE', ( #20530, #3894, #59569, #16509, #18205, #37124 ) ) ;
#18976=EDGE_LOOP ( 'NONE', ( #23454, #67288, #66419, #69226, #28833, #37233 ) ) ;
#18985=CARTESIAN_POINT ( 'NONE',  ( 275.0000000000000000, -38.10000000000000142, 8.400000000000000355 ) ) ;
#19014=EDGE_CURVE ( 'NONE', #61781, #992, #7534, .T. ) ;
#19022=PLANE ( 'NONE',  #54311 ) ;
#19031=VERTEX_POINT ( 'NONE', #8228 ) ;
#19036=FACE_OUTER_BOUND ( 'NONE', #63739, .T. ) ;
#19038=VERTEX_POINT ( 'NONE', #49633 ) ;
#19043=ADVANCED_FACE ( 'NONE', ( #61262 ), #60925, .F. ) ;
#19044=CARTESIAN_POINT ( 'NONE',  ( 7.000000000000000000, -26.42999999999999972, 5.874955318979029784 ) ) ;
#19048=CARTESIAN_POINT ( 'NONE',  ( 7.000000000000000000, -28.95000000000155183, 14.49999999999845990 ) ) ;
#19057=CARTESIAN_POINT ( 'NONE',  ( 275.0000000000000000, -38.65000000000095781, 13.20000000000094253 ) ) ;
#19076=DIRECTION ( 'NONE',  ( 1.000000000000000000, -0.000000000000000000, -0.000000000000000000 ) ) ;
#19079=CARTESIAN_POINT ( 'NONE',  ( 283.0000000000000568, -32.45000000000000995, -15.00000000000000000 ) ) ;
#19098=ORIENTED_EDGE ( 'NONE', *, *, #69128, .F. ) ;
#19100=VECTOR ( 'NONE', #44211, 1000.000000000000000 ) ;
#19102=DIRECTION ( 'NONE',  ( 1.000000000000000000, 0.000000000000000000, 0.000000000000000000 ) ) ;
#19121=EDGE_LOOP ( 'NONE', ( #56648, #4108, #50102, #35789, #58111 ) ) ;
#19123=AXIS2_PLACEMENT_3D ( 'NONE', #66542, #42980, #39327 ) ;
#19127=DIRECTION ( 'NONE',  ( -1.000000000000000000, 0.000000000000000000, 0.000000000000000000 ) ) ;
#19128=EDGE_LOOP ( 'NONE', ( #24157, #62609, #41163, #33609, #54901, #19443 ) ) ;
#19137=DIRECTION ( 'NONE',  ( -1.000000000000000000, 0.000000000000000000, 0.000000000000000000 ) ) ;
#19188=ORIENTED_EDGE ( 'NONE', *, *, #38889, .T. ) ;
#19190=EDGE_LOOP ( 'NONE', ( #55050, #52740, #41487, #42977 ) ) ;
#19206=AXIS2_PLACEMENT_3D ( 'NONE', #37649, #1205, #17448 ) ;
#19219=ORIENTED_EDGE ( 'NONE', *, *, #7613, .F. ) ;
#19233=CARTESIAN_POINT ( 'NONE',  ( 283.0000000000000568, -26.50000000000000000, 0.5000000000000000000 ) ) ;
#19251=AXIS2_PLACEMENT_3D ( 'NONE', #37865, #5357, #4990 ) ;
#19259=DIRECTION ( 'NONE',  ( 0.000000000000000000, 0.000000000000000000, 1.000000000000000000 ) ) ;
#19262=LINE ( 'NONE', #7940, #31967 ) ;
#19263=CARTESIAN_POINT ( 'NONE',  ( 10.31889768521803319, -25.34729925119248861, -17.15270074880751494 ) ) ;
#19309=VECTOR ( 'NONE', #39015, 1000.000000000000000 ) ;
#19329=ORIENTED_EDGE ( 'NONE', *, *, #28658, .T. ) ;
#19335=PLANE ( 'NONE',  #22906 ) ;
#19342=DIRECTION ( 'NONE',  ( 0.5773502691896257311, -0.5773502691896257311, -0.5773502691896257311 ) ) ;
#19346=DIRECTION ( 'NONE',  ( -1.000000000000000000, 0.000000000000000000, 0.000000000000000000 ) ) ;
#19352=ORIENTED_EDGE ( 'NONE', *, *, #12452, .F. ) ;
#19372=CARTESIAN_POINT ( 'NONE',  ( 7.000000000000000000, -23.70411739045900390, -12.50000000000000000 ) ) ;
#19387=LINE ( 'NONE', #25055, #47468 ) ;
#19420=CARTESIAN_POINT ( 'NONE',  ( 7.000000000000000000, -37.15000000000001279, -7.700000000000000178 ) ) ;
#19421=EDGE_CURVE ( 'NONE', #43665, #18078, #12951, .T. ) ;
#19423=DIRECTION ( 'NONE',  ( 0.000000000000000000, -1.000000000000000000, -8.396061623720747815E-13 ) ) ;
#19443=ORIENTED_EDGE ( 'NONE', *, *, #46777, .T. ) ;
#19445=DIRECTION ( 'NONE',  ( 0.000000000000000000, 0.000000000000000000, -1.000000000000000000 ) ) ;
#19446=AXIS2_PLACEMENT_3D ( 'NONE', #1310, #43049, #60001 ) ;
#19447=DIRECTION ( 'NONE',  ( 1.000000000000000000, -0.000000000000000000, -0.000000000000000000 ) ) ;
#19462=CYLINDRICAL_SURFACE ( 'NONE', #40096, 0.4999999999979551912 ) ;
#19471=CIRCLE ( 'NONE', #57883, 8.000000000000000000 ) ;
#19484=CARTESIAN_POINT ( 'NONE',  ( 283.0000000000000568, -38.15000000000000568, 14.50000000000000000 ) ) ;
#19506=CARTESIAN_POINT ( 'NONE',  ( 0.5000000000000000000, 0.000000000000000000, -26.50000000000000000 ) ) ;
#19509=DIRECTION ( 'NONE',  ( 0.000000000000000000, -1.901256929667043247E-12, 1.000000000000000000 ) ) ;
#19574=VECTOR ( 'NONE', #6599, 1000.000000000000000 ) ;
#19582=LINE ( 'NONE', #3678, #67325 ) ;
#19589=VECTOR ( 'NONE', #28538, 1000.000000000000114 ) ;
#19602=CARTESIAN_POINT ( 'NONE',  ( 283.0000000000000568, -42.50000000000000000, 10.20000000000000107 ) ) ;
#19606=CARTESIAN_POINT ( 'NONE',  ( 275.0000000000000000, -39.80000000000000426, 12.69999999999999929 ) ) ;
#19626=ORIENTED_EDGE ( 'NONE', *, *, #66183, .F. ) ;
#19627=VECTOR ( 'NONE', #45986, 1000.000000000000000 ) ;
#19645=ADVANCED_FACE ( 'NONE', ( #28119 ), #22809, .T. ) ;
#19657=VECTOR ( 'NONE', #50124, 1000.000000000000000 ) ;
#19670=CARTESIAN_POINT ( 'NONE',  ( 7.000000000000000000, -25.69999999999924967, -14.52500000000000213 ) ) ;
#19681=CYLINDRICAL_SURFACE ( 'NONE', #23692, 0.5000000000009459100 ) ;
#19684=DIRECTION ( 'NONE',  ( 0.5773502691896257311, -0.5773502691896257311, 0.5773502691896257311 ) ) ;
#19688=DIRECTION ( 'NONE',  ( 1.000000000000000000, 0.000000000000000000, 0.000000000000000000 ) ) ;
#19703=EDGE_LOOP ( 'NONE', ( #25318, #20962, #15527, #18751 ) ) ;
#19710=VECTOR ( 'NONE', #30085, 1000.000000000000000 ) ;
#19714=CARTESIAN_POINT ( 'NONE',  ( 15.00000000000000000, -23.65000000000000568, -12.40000000000000213 ) ) ;
#19744=CARTESIAN_POINT ( 'NONE',  ( 283.0000000000000568, -25.50000000000000355, 17.00000000000000000 ) ) ;
#19748=CARTESIAN_POINT ( 'NONE',  ( 289.5000000000000000, -0.5000000000000000000, -27.00000000000000000 ) ) ;
#19752=VECTOR ( 'NONE', #54251, 1000.000000000000000 ) ;
#19756=EDGE_LOOP ( 'NONE', ( #45955, #24161, #32848, #25170 ) ) ;
#19765=EDGE_CURVE ( 'NONE', #10975, #10944, #13590, .T. ) ;
#19785=VERTEX_POINT ( 'NONE', #51069 ) ;
#19788=DIRECTION ( 'NONE',  ( 0.000000000000000000, 1.000000000000000000, 0.000000000000000000 ) ) ;
#19800=EDGE_CURVE ( 'NONE', #61959, #39543, #2284, .T. ) ;
#19803=FACE_OUTER_BOUND ( 'NONE', #40484, .T. ) ;
#19810=VECTOR ( 'NONE', #57712, 1000.000000000000000 ) ;
#19833=ADVANCED_FACE ( 'NONE', ( #35144 ), #7582, .F. ) ;
#19834=CARTESIAN_POINT ( 'NONE',  ( 7.000000000000000000, -26.06132420600899735, 10.13999572156699891 ) ) ;
#19863=ORIENTED_EDGE ( 'NONE', *, *, #26189, .F. ) ;
#19873=ORIENTED_EDGE ( 'NONE', *, *, #56847, .F. ) ;
#19875=EDGE_LOOP ( 'NONE', ( #45118, #49433, #18198, #55931 ) ) ;
#19880=DIRECTION ( 'NONE',  ( 0.000000000000000000, -1.000000000000000000, 0.000000000000000000 ) ) ;
#19884=ADVANCED_FACE ( 'NONE', ( #8982 ), #52125, .T. ) ;
#19885=AXIS2_PLACEMENT_3D ( 'NONE', #62353, #13920, #50699 ) ;
#19887=ADVANCED_FACE ( 'NONE', ( #48230 ), #57425, .F. ) ;
#19899=CARTESIAN_POINT ( 'NONE',  ( 283.0000000000000568, -26.50000000000000000, 0.5000000000000000000 ) ) ;
#19913=AXIS2_PLACEMENT_3D ( 'NONE', #38313, #43255, #12113 ) ;
#19916=ORIENTED_EDGE ( 'NONE', *, *, #11091, .F. ) ;
#19929=AXIS2_PLACEMENT_3D ( 'NONE', #66540, #55587, #39657 ) ;
#19935=ORIENTED_EDGE ( 'NONE', *, *, #52518, .T. ) ;
#19963=CARTESIAN_POINT ( 'NONE',  ( 275.0000000000000000, -23.50007830495750127, 12.28007262201345995 ) ) ;
#19983=EDGE_CURVE ( 'NONE', #13174, #54503, #33345, .T. ) ;
#20005=CARTESIAN_POINT ( 'NONE',  ( 7.000000000000000000, -38.10000000000000142, 8.400000000000000355 ) ) ;
#20008=ORIENTED_EDGE ( 'NONE', *, *, #35435, .F. ) ;
#20024=AXIS2_PLACEMENT_3D ( 'NONE', #52562, #9776, #16120 ) ;
#20025=CARTESIAN_POINT ( 'NONE',  ( 283.0000000000000568, -42.00000000000000000, 15.00000000000000000 ) ) ;
#20031=DIRECTION ( 'NONE',  ( 0.000000000000000000, 0.7071067811865875408, 0.7071067811865076047 ) ) ;
#20038=ORIENTED_EDGE ( 'NONE', *, *, #31685, .T. ) ;
#20043=AXIS2_PLACEMENT_3D ( 'NONE', #34176, #34875, #39831 ) ;
#20050=DIRECTION ( 'NONE',  ( -1.000000000000000000, 0.000000000000000000, 0.000000000000000000 ) ) ;
#20081=DIRECTION ( 'NONE',  ( 0.000000000000000000, 0.7071067811865076047, 0.7071067811865875408 ) ) ;
#20096=LINE ( 'NONE', #52989, #63588 ) ;
#20104=EDGE_CURVE ( 'NONE', #68268, #14910, #50389, .T. ) ;
#20114=DIRECTION ( 'NONE',  ( 0.000000000000000000, -1.000000000000000000, 0.000000000000000000 ) ) ;
#20120=ORIENTED_EDGE ( 'NONE', *, *, #53981, .T. ) ;
#20130=DIRECTION ( 'NONE',  ( 0.000000000000000000, 0.000000000000000000, -1.000000000000000000 ) ) ;
#20148=CARTESIAN_POINT ( 'NONE',  ( 275.0000000000000000, -20.50000000000000000, -13.00000000000000178 ) ) ;
#20185=LINE ( 'NONE', #53081, #22110 ) ;
#20189=LINE ( 'NONE', #14535, #30516 ) ;
#20203=ADVANCED_FACE ( 'NONE', ( #39669 ), #40238, .T. ) ;
#20236=EDGE_LOOP ( 'NONE', ( #30334, #37928, #18297, #63634 ) ) ;
#20252=VERTEX_POINT ( 'NONE', #19506 ) ;
#20269=ORIENTED_EDGE ( 'NONE', *, *, #2553, .F. ) ;
#20292=DIRECTION ( 'NONE',  ( -1.000000000000000000, 0.000000000000000000, 0.000000000000000000 ) ) ;
#20297=ADVANCED_FACE ( 'NONE', ( #36122 ), #46379, .T. ) ;
#20300=CARTESIAN_POINT ( 'NONE',  ( 7.000000000000000000, -21.00000000000000000, 4.000000000000000000 ) ) ;
#20307=DIRECTION ( 'NONE',  ( 1.000000000000000000, -0.000000000000000000, -0.000000000000000000 ) ) ;
#20310=ORIENTED_EDGE ( 'NONE', *, *, #67400, .T. ) ;
#20311=AXIS2_PLACEMENT_3D ( 'NONE', #43134, #17905, #50770 ) ;
#20340=VECTOR ( 'NONE', #65376, 1000.000000000000000 ) ;
#20341=ORIENTED_EDGE ( 'NONE', *, *, #3469, .F. ) ;
#20361=DIRECTION ( 'NONE',  ( -1.000000000000000000, 0.000000000000000000, 0.000000000000000000 ) ) ;
#20363=MANIFOLD_SOLID_BREP ( 'Boss-Extrude1', #48759 ) ;
#20374=AXIS2_PLACEMENT_3D ( 'NONE', #5885, #33447, #27449 ) ;
#20387=DIRECTION ( 'NONE',  ( 1.000000000000000000, -0.000000000000000000, -0.000000000000000000 ) ) ;
#20392=CARTESIAN_POINT ( 'NONE',  ( 7.000000000000000000, -21.00000000000000000, 0.000000000000000000 ) ) ;
#20424=DIRECTION ( 'NONE',  ( 1.000000000000000000, 0.000000000000000000, 0.000000000000000000 ) ) ;
#20434=VERTEX_POINT ( 'NONE', #21956 ) ;
#20446=PLANE ( 'NONE',  #54292 ) ;
#20462=VECTOR ( 'NONE', #8702, 1000.000000000000000 ) ;
#20468=CARTESIAN_POINT ( 'NONE',  ( 7.000000000000000000, -20.40000000000000213, 12.40000000000000213 ) ) ;
#20514=VECTOR ( 'NONE', #46105, 1000.000000000000000 ) ;
#20525=CARTESIAN_POINT ( 'NONE',  ( 0.000000000000000000, -21.00000000000000000, 0.000000000000000000 ) ) ;
#20530=ORIENTED_EDGE ( 'NONE', *, *, #44360, .T. ) ;
#20555=EDGE_CURVE ( 'NONE', #66065, #26683, #2461, .T. ) ;
#20564=DIRECTION ( 'NONE',  ( 0.000000000000000000, -1.901256929667036381E-12, 1.000000000000000000 ) ) ;
#20573=VECTOR ( 'NONE', #59341, 1000.000000000000000 ) ;
#20612=CIRCLE ( 'NONE', #28521, 3.999999999999993339 ) ;
#20613=EDGE_CURVE ( 'NONE', #44568, #57476, #25799, .T. ) ;
#20615=VERTEX_POINT ( 'NONE', #51611 ) ;
#20638=ORIENTED_EDGE ( 'NONE', *, *, #39692, .F. ) ;
#20674=ORIENTED_EDGE ( 'NONE', *, *, #18941, .T. ) ;
#20680=EDGE_LOOP ( 'NONE', ( #16099, #60018, #10336, #53703 ) ) ;
#20704=CARTESIAN_POINT ( 'NONE',  ( 7.000000000000000000, -42.50000000000000000, 7.500000000000000000 ) ) ;
#20717=CARTESIAN_POINT ( 'NONE',  ( 7.000000000000000000, -30.45000000000000639, 15.00000000000000000 ) ) ;
#20740=CARTESIAN_POINT ( 'NONE',  ( 289.5000000000000000, 50.00000000000000000, -27.00000000000000000 ) ) ;
#20743=EDGE_LOOP ( 'NONE', ( #21745, #34445, #52478, #41113 ) ) ;
#20750=DIRECTION ( 'NONE',  ( 0.000000000000000000, 0.000000000000000000, 1.000000000000000000 ) ) ;
#20754=ADVANCED_FACE ( 'NONE', ( #65361 ), #43787, .F. ) ;
#20778=LINE ( 'NONE', #30699, #5108 ) ;
#20794=AXIS2_PLACEMENT_3D ( 'NONE', #27004, #138, #11421 ) ;
#20853=LINE ( 'NONE', #26512, #65980 ) ;
#20854=VERTEX_POINT ( 'NONE', #40470 ) ;
#20864=DIRECTION ( 'NONE',  ( 0.000000000000000000, 0.000000000000000000, 1.000000000000000000 ) ) ;
#20868=LINE ( 'NONE', #14514, #7398 ) ;
#20879=DIRECTION ( 'NONE',  ( 1.000000000000000000, -0.000000000000000000, -0.000000000000000000 ) ) ;
#20887=ORIENTED_EDGE ( 'NONE', *, *, #61955, .T. ) ;
#20908=FACE_OUTER_BOUND ( 'NONE', #33812, .T. ) ;
#20924=ORIENTED_EDGE ( 'NONE', *, *, #33387, .F. ) ;
#20928=VECTOR ( 'NONE', #22419, 1000.000000000000000 ) ;
#20951=ORIENTED_EDGE ( 'NONE', *, *, #7372, .T. ) ;
#20962=ORIENTED_EDGE ( 'NONE', *, *, #57868, .F. ) ;
#20977=ADVANCED_FACE ( 'NONE', ( #36212 ), #63799, .T. ) ;
#20979=EDGE_LOOP ( 'NONE', ( #53671, #59541, #25739, #36487, #2905, #2616, #40499, #24922, #29490, #48119 ) ) ;
#20997=CARTESIAN_POINT ( 'NONE',  ( 7.000000000000000000, -25.93000000000544958, -9.412893218815410634 ) ) ;
#21002=EDGE_CURVE ( 'NONE', #40605, #37208, #64164, .T. ) ;
#21014=LINE ( 'NONE', #65211, #19752 ) ;
#21022=EDGE_CURVE ( 'NONE', #17604, #50924, #5096, .T. ) ;
#21056=VERTEX_POINT ( 'NONE', #49947 ) ;
#21060=UNCERTAINTY_MEASURE_WITH_UNIT (LENGTH_MEASURE( 1.000000000000000082E-05 ), #4006, 'distance_accuracy_value', 'NONE');
#21069=VERTEX_POINT ( 'NONE', #22406 ) ;
#21070=CARTESIAN_POINT ( 'NONE',  ( 276.8775010008008053, -25.00000000000000000, -17.50000000000000000 ) ) ;
#21092=AXIS2_PLACEMENT_3D ( 'NONE', #38073, #64243, #10484 ) ;
#21127=EDGE_CURVE ( 'NONE', #29091, #4296, #59876, .T. ) ;
#21134=VECTOR ( 'NONE', #36752, 1000.000000000000000 ) ;
#21152=VECTOR ( 'NONE', #61293, 1000.000000000000000 ) ;
#21174=CARTESIAN_POINT ( 'NONE',  ( 283.0000000000000568, -40.30000000000000426, 8.900000000000000355 ) ) ;
#21184=FACE_OUTER_BOUND ( 'NONE', #57197, .T. ) ;
#21194=ORIENTED_EDGE ( 'NONE', *, *, #23037, .T. ) ;
#21198=LINE ( 'NONE', #27196, #49239 ) ;
#21201=DIRECTION ( 'NONE',  ( 1.000000000000000000, 0.000000000000000000, 0.000000000000000000 ) ) ;
#21226=ORIENTED_EDGE ( 'NONE', *, *, #586, .F. ) ;
#21237=DIRECTION ( 'NONE',  ( 1.000000000000000000, -0.000000000000000000, -0.000000000000000000 ) ) ;
#21238=ORIENTED_EDGE ( 'NONE', *, *, #12091, .T. ) ;
#21244=DIRECTION ( 'NONE',  ( 0.000000000000000000, 0.6801302850037830305, 0.7330912599538155217 ) ) ;
#21267=EDGE_CURVE ( 'NONE', #65495, #11767, #47444, .T. ) ;
#21272=LINE ( 'NONE', #25874, #60863 ) ;
#21279=PLANE ( 'NONE',  #14903 ) ;
#21286=EDGE_LOOP ( 'NONE', ( #13318, #56426, #69847, #56659 ) ) ;
#21291=DIRECTION ( 'NONE',  ( 0.000000000000000000, 0.000000000000000000, 1.000000000000000000 ) ) ;
#21297=ORIENTED_EDGE ( 'NONE', *, *, #55328, .F. ) ;
#21300=ADVANCED_FACE ( 'NONE', ( #14218 ), #25541, .F. ) ;
#21302=CARTESIAN_POINT ( 'NONE',  ( 7.000000000000000000, -29.94999999999999929, 14.50000000000000000 ) ) ;
#21311=LINE ( 'NONE', #32263, #45392 ) ;
#21315=FACE_BOUND ( 'NONE', #61309, .T. ) ;
#21329=LINE ( 'NONE', #54211, #45810 ) ;
#21356=CIRCLE ( 'NONE', #47337, 0.4999999999979768961 ) ;
#21359=CIRCLE ( 'NONE', #8919, 0.5000000000023396840 ) ;
#21375=DIRECTION ( 'NONE',  ( 0.000000000000000000, 0.000000000000000000, 1.000000000000000000 ) ) ;
#21387=ORIENTED_EDGE ( 'NONE', *, *, #37069, .F. ) ;
#21426=DIRECTION ( 'NONE',  ( -1.000000000000000000, 0.000000000000000000, 0.000000000000000000 ) ) ;
#21435=LINE ( 'NONE', #27085, #36714 ) ;
#21436=ADVANCED_FACE ( 'NONE', ( #33276 ), #54844, .F. ) ;
#21444=DIRECTION ( 'NONE',  ( 0.000000000000000000, 0.000000000000000000, -1.000000000000000000 ) ) ;
#21495=CARTESIAN_POINT ( 'NONE',  ( 275.0000000000000000, -20.40000000000000213, -12.40000000000000213 ) ) ;
#21497=ORIENTED_EDGE ( 'NONE', *, *, #31630, .T. ) ;
#21519=DIRECTION ( 'NONE',  ( 0.000000000000000000, -1.000000000000000000, -1.880440247955360336E-12 ) ) ;
#21520=EDGE_CURVE ( 'NONE', #26683, #27626, #66479, .T. ) ;
#21532=EDGE_CURVE ( 'NONE', #29731, #53055, #35329, .T. ) ;
#21544=ORIENTED_EDGE ( 'NONE', *, *, #48476, .F. ) ;
#21545=EDGE_LOOP ( 'NONE', ( #66337, #47136, #66692, #6142 ) ) ;
#21549=CIRCLE ( 'NONE', #68994, 0.5000000000004272138 ) ;
#21551=CARTESIAN_POINT ( 'NONE',  ( 283.0000000000000568, -32.00000000000000000, -8.400000000000000355 ) ) ;
#21570=VERTEX_POINT ( 'NONE', #40996 ) ;
#21573=ORIENTED_EDGE ( 'NONE', *, *, #41787, .T. ) ;
#21576=DIRECTION ( 'NONE',  ( 0.000000000000000000, 0.000000000000000000, 1.000000000000000000 ) ) ;
#21584=LINE ( 'NONE', #54463, #17647 ) ;
#21614=VERTEX_POINT ( 'NONE', #14492 ) ;
#21615=CARTESIAN_POINT ( 'NONE',  ( 14.50000000000000000, -42.00000000000000000, 27.00000000000000000 ) ) ;
#21644=ORIENTED_EDGE ( 'NONE', *, *, #12294, .F. ) ;
#21649=DIRECTION ( 'NONE',  ( 0.000000000000000000, -0.7071067811865475727, 0.7071067811865475727 ) ) ;
#21667=VECTOR ( 'NONE', #24765, 1000.000000000000000 ) ;
#21669=ORIENTED_EDGE ( 'NONE', *, *, #29875, .F. ) ;
#21702=DIRECTION ( 'NONE',  ( 0.000000000000000000, 0.000000000000000000, 1.000000000000000000 ) ) ;
#21706=VERTEX_POINT ( 'NONE', #53381 ) ;
#21728=DIRECTION ( 'NONE',  ( 0.000000000000000000, 0.7071067811865074937, 0.7071067811865876518 ) ) ;
#21742=CARTESIAN_POINT ( 'NONE',  ( 280.0000000000000000, -25.50000000000000355, -16.00000000000000711 ) ) ;
#21745=ORIENTED_EDGE ( 'NONE', *, *, #15924, .F. ) ;
#21753=VERTEX_POINT ( 'NONE', #2388 ) ;
#21760=DIRECTION ( 'NONE',  ( 0.000000000000000000, 1.000000000000000000, 1.880440247955334083E-12 ) ) ;
#21761=DIRECTION ( 'NONE',  ( 0.000000000000000000, -0.5017180897718492849, 0.8650311892618014475 ) ) ;
#21769=CARTESIAN_POINT ( 'NONE',  ( 283.0000000000000568, -25.14575131106458272, -17.35424868893542083 ) ) ;
#21789=CARTESIAN_POINT ( 'NONE',  ( 283.0000000000000568, -31.30000000000000071, -8.400000000000000355 ) ) ;
#21797=DIRECTION ( 'NONE',  ( 1.000000000000000000, 0.000000000000000000, 0.000000000000000000 ) ) ;
#21811=DIRECTION ( 'NONE',  ( 0.000000000000000000, 0.000000000000000000, -1.000000000000000000 ) ) ;
#21817=VERTEX_POINT ( 'NONE', #62123 ) ;
#21826=CARTESIAN_POINT ( 'NONE',  ( 283.0000000000000568, -20.40000000000000213, 17.35424868893542438 ) ) ;
#21849=DIRECTION ( 'NONE',  ( 0.000000000000000000, 0.000000000000000000, -1.000000000000000000 ) ) ;
#21855=DIRECTION ( 'NONE',  ( -1.000000000000000000, 0.000000000000000000, 0.000000000000000000 ) ) ;
#21876=FACE_OUTER_BOUND ( 'NONE', #30532, .T. ) ;
#21889=ORIENTED_EDGE ( 'NONE', *, *, #65503, .F. ) ;
#21903=VECTOR ( 'NONE', #9745, 1000.000000000000114 ) ;
#21925=VERTEX_POINT ( 'NONE', #52950 ) ;
#21928=LINE ( 'NONE', #27578, #32357 ) ;
#21946=DIRECTION ( 'NONE',  ( -1.000000000000000000, 0.000000000000000000, 0.000000000000000000 ) ) ;
#21952=PLANE ( 'NONE',  #9588 ) ;
#21956=CARTESIAN_POINT ( 'NONE',  ( 7.000000000000000000, -25.60000000000000142, -16.03137303340311348 ) ) ;
#21971=CARTESIAN_POINT ( 'NONE',  ( 275.5000000000000000, -42.50000000000000000, 15.10000000000000142 ) ) ;
#21994=EDGE_CURVE ( 'NONE', #68084, #25376, #63549, .T. ) ;
#22006=DIRECTION ( 'NONE',  ( -1.000000000000000000, 0.000000000000000000, 0.000000000000000000 ) ) ;
#22056=VECTOR ( 'NONE', #17243, 1000.000000000000000 ) ;
#22086=CARTESIAN_POINT ( 'NONE',  ( 283.0000000000000568, -21.00000000000000000, 12.50000000000000000 ) ) ;
#22095=ORIENTED_EDGE ( 'NONE', *, *, #7206, .T. ) ;
#22096=VERTEX_POINT ( 'NONE', #43011 ) ;
#22100=VERTEX_POINT ( 'NONE', #59633 ) ;
#22110=VECTOR ( 'NONE', #14177, 1000.000000000000000 ) ;
#22112=CARTESIAN_POINT ( 'NONE',  ( 283.0000000000000568, -38.10000000000000142, 8.400000000000000355 ) ) ;
#22120=EDGE_CURVE ( 'NONE', #31022, #33386, #22151, .T. ) ;
#22129=LINE ( 'NONE', #32045, #59622 ) ;
#22150=DIRECTION ( 'NONE',  ( 1.000000000000000000, 0.000000000000000000, 0.000000000000000000 ) ) ;
#22151=LINE ( 'NONE', #32063, #49095 ) ;
#22154=CARTESIAN_POINT ( 'NONE',  ( 10.14575131106465378, -25.50000000000000355, 17.00000000000000000 ) ) ;
#22165=AXIS2_PLACEMENT_3D ( 'NONE', #26526, #41380, #26884 ) ;
#22179=ORIENTED_EDGE ( 'NONE', *, *, #36202, .T. ) ;
#22186=EDGE_CURVE ( 'NONE', #62668, #48333, #57059, .T. ) ;
#22191=VERTEX_POINT ( 'NONE', #31612 ) ;
#22193=CARTESIAN_POINT ( 'NONE',  ( 7.000000000000000000, -31.30000000000000071, 8.400000000000000355 ) ) ;
#22202=ORIENTED_EDGE ( 'NONE', *, *, #8341, .T. ) ;
#22222=EDGE_CURVE ( 'NONE', #9656, #3514, #19582, .T. ) ;
#22251=DIRECTION ( 'NONE',  ( -1.000000000000000000, 0.000000000000000000, 0.000000000000000000 ) ) ;
#22276=ORIENTED_EDGE ( 'NONE', *, *, #23913, .T. ) ;
#22316=FACE_OUTER_BOUND ( 'NONE', #54025, .T. ) ;
#22331=DIRECTION ( 'NONE',  ( -0.7071067811865475727, 0.000000000000000000, 0.7071067811865475727 ) ) ;
#22349=EDGE_LOOP ( 'NONE', ( #16594, #60782, #16576, #5986 ) ) ;
#22354=AXIS2_PLACEMENT_3D ( 'NONE', #57783, #69444, #9711 ) ;
#22365=CIRCLE ( 'NONE', #57322, 0.4999999999945534124 ) ;
#22370=VECTOR ( 'NONE', #21702, 1000.000000000000000 ) ;
#22379=CARTESIAN_POINT ( 'NONE',  ( 275.2500000000001137, -0.2500000000000497935, 26.75000000000004263 ) ) ;
#22381=VECTOR ( 'NONE', #62025, 1000.000000000000000 ) ;
#22392=DIRECTION ( 'NONE',  ( 0.000000000000000000, 0.000000000000000000, -1.000000000000000000 ) ) ;
#22406=CARTESIAN_POINT ( 'NONE',  ( 7.500000000000000000, -25.60000000000000142, -16.00000000000000000 ) ) ;
#22409=ADVANCED_FACE ( 'NONE', ( #1162 ), #54567, .F. ) ;
#22419=DIRECTION ( 'NONE',  ( 0.000000000000000000, 0.000000000000000000, -1.000000000000000000 ) ) ;
#22428=FACE_OUTER_BOUND ( 'NONE', #18466, .T. ) ;
#22458=ORIENTED_EDGE ( 'NONE', *, *, #63972, .F. ) ;
#22463=ADVANCED_FACE ( 'NONE', ( #66875 ), #12430, .F. ) ;
#22467=EDGE_CURVE ( 'NONE', #13174, #68300, #2189, .T. ) ;
#22478=DIRECTION ( 'NONE',  ( 0.000000000000000000, 1.000000000000000000, 0.000000000000000000 ) ) ;
#22531=EDGE_CURVE ( 'NONE', #41506, #57189, #8179, .T. ) ;
#22542=ORIENTED_EDGE ( 'NONE', *, *, #3536, .F. ) ;
#22543=EDGE_CURVE ( 'NONE', #3117, #51826, #50975, .T. ) ;
#22549=DIRECTION ( 'NONE',  ( 1.000000000000000000, 0.000000000000000000, 0.000000000000000000 ) ) ;
#22556=CARTESIAN_POINT ( 'NONE',  ( 7.000000000000000000, -25.56180396883900130, -14.25872597390799967 ) ) ;
#22558=VECTOR ( 'NONE', #44917, 1000.000000000000000 ) ;
#22560=VERTEX_POINT ( 'NONE', #35049 ) ;
#22575=CYLINDRICAL_SURFACE ( 'NONE', #12370, 3.999999999999993339 ) ;
#22582=CARTESIAN_POINT ( 'NONE',  ( 275.2500000000000000, -0.2500000000000000000, 26.75000000000000000 ) ) ;
#22584=VECTOR ( 'NONE', #42267, 1000.000000000000000 ) ;
#22590=ORIENTED_EDGE ( 'NONE', *, *, #42701, .T. ) ;
#22605=CARTESIAN_POINT ( 'NONE',  ( 10.62249899919920004, -25.00000000000000000, 17.50000000000000000 ) ) ;
#22606=CARTESIAN_POINT ( 'NONE',  ( 283.0000000000000568, -38.10000000000000142, 8.400000000000000355 ) ) ;
#22620=ADVANCED_FACE ( 'NONE', ( #23684 ), #66816, .F. ) ;
#22635=CARTESIAN_POINT ( 'NONE',  ( 283.0000000000000568, -42.50000000000000000, 7.500000000000000000 ) ) ;
#22636=VERTEX_POINT ( 'NONE', #56226 ) ;
#22640=CYLINDRICAL_SURFACE ( 'NONE', #31272, 0.5000000000004236611 ) ;
#22667=ORIENTED_EDGE ( 'NONE', *, *, #69729, .F. ) ;
#22684=DIRECTION ( 'NONE',  ( 0.000000000000000000, 0.000000000000000000, -1.000000000000000000 ) ) ;
#22691=ORIENTED_EDGE ( 'NONE', *, *, #23913, .F. ) ;
#22699=VECTOR ( 'NONE', #33581, 1000.000000000000000 ) ;
#22708=VECTOR ( 'NONE', #29097, 1000.000000000000000 ) ;
#22709=VECTOR ( 'NONE', #46237, 1000.000000000000000 ) ;
#22713=EDGE_CURVE ( 'NONE', #8058, #31208, #43660, .T. ) ;
#22721=CARTESIAN_POINT ( 'NONE',  ( 15.00000000000000000, -42.50000000000000000, -26.50000000000000000 ) ) ;
#22724=CARTESIAN_POINT ( 'NONE',  ( 283.0000000000000568, -42.50000000000000000, 15.10000000000000142 ) ) ;
#22755=EDGE_CURVE ( 'NONE', #8602, #2847, #69878, .T. ) ;
#22766=CARTESIAN_POINT ( 'NONE',  ( 276.8775010008008053, -21.00000000000000000, 17.50000000000000000 ) ) ;
#22775=CARTESIAN_POINT ( 'NONE',  ( 0.000000000000000000, 0.000000000000000000, 0.000000000000000000 ) ) ;
#22777=ADVANCED_FACE ( 'NONE', ( #32744 ), #69187, .T. ) ;
#22779=ORIENTED_EDGE ( 'NONE', *, *, #56994, .T. ) ;
#22805=ORIENTED_EDGE ( 'NONE', *, *, #18582, .T. ) ;
#22809=CYLINDRICAL_SURFACE ( 'NONE', #25532, 0.5000000000009302559 ) ;
#22811=EDGE_LOOP ( 'NONE', ( #16816, #18318, #42054, #35245 ) ) ;
#22817=CARTESIAN_POINT ( 'NONE',  ( 289.5000000000000000, 0.000000000000000000, 50.00000000000000000 ) ) ;
#22835=DIRECTION ( 'NONE',  ( 0.000000000000000000, -0.7071067811865474617, 0.7071067811865474617 ) ) ;
#22842=VECTOR ( 'NONE', #50940, 1000.000000000000000 ) ;
#22847=AXIS2_PLACEMENT_3D ( 'NONE', #9738, #30595, #52162 ) ;
#22851=ORIENTED_EDGE ( 'NONE', *, *, #52928, .F. ) ;
#22875=PLANE ( 'NONE',  #37930 ) ;
#22881=PLANE ( 'NONE',  #64270 ) ;
#22895=EDGE_CURVE ( 'NONE', #51826, #45978, #7221, .T. ) ;
#22898=FACE_OUTER_BOUND ( 'NONE', #68039, .T. ) ;
#22906=AXIS2_PLACEMENT_3D ( 'NONE', #35589, #8737, #51875 ) ;
#22914=DIRECTION ( 'NONE',  ( 0.000000000000000000, -1.000000000000000000, 0.000000000000000000 ) ) ;
#22918=CIRCLE ( 'NONE', #4863, 5.000000000000000000 ) ;
#22933=CARTESIAN_POINT ( 'NONE',  ( 283.0000000000000568, -42.00000000000000000, -7.000000000000000000 ) ) ;
#22934=ORIENTED_EDGE ( 'NONE', *, *, #18116, .T. ) ;
#22942=CARTESIAN_POINT ( 'NONE',  ( 283.0000000000000568, -25.93000000000544958, -9.412893218815410634 ) ) ;
#22968=DIRECTION ( 'NONE',  ( 0.000000000000000000, -0.8650311892618017806, 0.5017180897718488408 ) ) ;
#22972=ORIENTED_EDGE ( 'NONE', *, *, #59187, .T. ) ;
#22979=CARTESIAN_POINT ( 'NONE',  ( 7.000000000000000000, -26.50000000000000000, -5.530822723609929881 ) ) ;
#22989=ADVANCED_FACE ( 'NONE', ( #68409 ), #29166, .F. ) ;
#22992=ADVANCED_FACE ( 'NONE', ( #46828 ), #68055, .F. ) ;
#22998=DIRECTION ( 'NONE',  ( 0.000000000000000000, 0.000000000000000000, 1.000000000000000000 ) ) ;
#23001=DIRECTION ( 'NONE',  ( -0.5773502691896268413, 0.5773502691896275074, -0.5773502691896227335 ) ) ;
#23012=VECTOR ( 'NONE', #22478, 1000.000000000000000 ) ;
#23015=AXIS2_PLACEMENT_3D ( 'NONE', #22817, #28457, #11844 ) ;
#23020=EDGE_LOOP ( 'NONE', ( #11216, #6763, #51581, #18878 ) ) ;
#23037=EDGE_CURVE ( 'NONE', #19031, #48215, #48353, .T. ) ;
#23045=CARTESIAN_POINT ( 'NONE',  ( 283.0000000000000568, -39.79999999999905214, -12.69999999999999929 ) ) ;
#23051=CYLINDRICAL_SURFACE ( 'NONE', #8032, 4.000000000000000000 ) ;
#23053=ORIENTED_EDGE ( 'NONE', *, *, #10262, .F. ) ;
#23056=CIRCLE ( 'NONE', #53570, 4.000000000000000000 ) ;
#23058=DIRECTION ( 'NONE',  ( 0.5773502691896175154, 0.5773502691896339467, 0.5773502691896257311 ) ) ;
#23079=FACE_OUTER_BOUND ( 'NONE', #33701, .T. ) ;
#23122=ORIENTED_EDGE ( 'NONE', *, *, #27103, .F. ) ;
#23152=FACE_OUTER_BOUND ( 'NONE', #65974, .T. ) ;
#23163=ORIENTED_EDGE ( 'NONE', *, *, #8366, .F. ) ;
#23177=EDGE_CURVE ( 'NONE', #65336, #19785, #31298, .T. ) ;
#23213=DIRECTION ( 'NONE',  ( 1.000000000000000000, 0.000000000000000000, 0.000000000000000000 ) ) ;
#23214=VECTOR ( 'NONE', #15555, 1000.000000000000000 ) ;
#23233=VECTOR ( 'NONE', #36320, 1000.000000000000000 ) ;
#23234=LINE ( 'NONE', #8358, #35898 ) ;
#23242=CARTESIAN_POINT ( 'NONE',  ( 276.8775010008008053, -21.00000000000000000, 17.50000000000000000 ) ) ;
#23243=CARTESIAN_POINT ( 'NONE',  ( 283.0000000000000568, -20.50000000000000000, 13.00000000000000178 ) ) ;
#23258=CARTESIAN_POINT ( 'NONE',  ( 14.50000000000000000, -42.50000000000000000, 27.00000000000000000 ) ) ;
#23271=ORIENTED_EDGE ( 'NONE', *, *, #49989, .T. ) ;
#23282=CARTESIAN_POINT ( 'NONE',  ( 15.00000000000000000, -26.42999999999999972, -5.874955318979029784 ) ) ;
#23289=CARTESIAN_POINT ( 'NONE',  ( 7.000000000000000000, -23.65000000000000568, -12.40000000000000213 ) ) ;
#23292=EDGE_LOOP ( 'NONE', ( #38283, #43683, #26462, #9577 ) ) ;
#23296=FACE_OUTER_BOUND ( 'NONE', #3501, .T. ) ;
#23307=VECTOR ( 'NONE', #35629, 1000.000000000000114 ) ;
#23310=FACE_OUTER_BOUND ( 'NONE', #43006, .T. ) ;
#23314=ADVANCED_FACE ( 'NONE', ( #1876 ), #38329, .F. ) ;
#23318=CARTESIAN_POINT ( 'NONE',  ( 275.0000000000000000, -26.79000000000000625, 0.000000000000000000 ) ) ;
#23344=VECTOR ( 'NONE', #34520, 1000.000000000000000 ) ;
#23351=CIRCLE ( 'NONE', #59504, 5.000000000000000000 ) ;
#23362=EDGE_LOOP ( 'NONE', ( #7784, #51482, #64548, #35673 ) ) ;
#23367=DIRECTION ( 'NONE',  ( 0.000000000000000000, 0.000000000000000000, 1.000000000000000000 ) ) ;
#23383=ORIENTED_EDGE ( 'NONE', *, *, #24948, .F. ) ;
#23390=ORIENTED_EDGE ( 'NONE', *, *, #36008, .T. ) ;
#23400=VECTOR ( 'NONE', #64295, 1000.000000000000000 ) ;
#23404=ADVANCED_FACE ( 'NONE', ( #46398 ), #44998, .F. ) ;
#23413=ORIENTED_EDGE ( 'NONE', *, *, #59572, .F. ) ;
#23415=VECTOR ( 'NONE', #60639, 1000.000000000000000 ) ;
#23444=ORIENTED_EDGE ( 'NONE', *, *, #46795, .T. ) ;
#23446=DIRECTION ( 'NONE',  ( 0.000000000000000000, 1.000000000000000000, 0.000000000000000000 ) ) ;
#23452=ORIENTED_EDGE ( 'NONE', *, *, #27172, .F. ) ;
#23454=ORIENTED_EDGE ( 'NONE', *, *, #61880, .F. ) ;
#23455=CIRCLE ( 'NONE', #12141, 0.3000000000005412781 ) ;
#23457=DIRECTION ( 'NONE',  ( 1.000000000000000000, -0.000000000000000000, -0.000000000000000000 ) ) ;
#23481=ADVANCED_FACE ( 'NONE', ( #23787 ), #67974, .F. ) ;
#23482=ORIENTED_EDGE ( 'NONE', *, *, #49667, .T. ) ;
#23504=DIRECTION ( 'NONE',  ( -1.000000000000000000, 0.000000000000000000, 0.000000000000000000 ) ) ;
#23508=LINE ( 'NONE', #34802, #22381 ) ;
#23514=AXIS2_PLACEMENT_3D ( 'NONE', #39074, #13596, #7228 ) ;
#23518=CARTESIAN_POINT ( 'NONE',  ( 283.0000000000000568, -37.15000000000001279, -7.700000000000000178 ) ) ;
#23530=PLANE ( 'NONE',  #68947 ) ;
#23532=CARTESIAN_POINT ( 'NONE',  ( 0.5000000000000000000, 0.000000000000000000, 26.50000000000000000 ) ) ;
#23537=CARTESIAN_POINT ( 'NONE',  ( 283.0000000000000568, -32.45000000000000995, -12.69999999999999929 ) ) ;
#23547=( BOUNDED_CURVE ( )  B_SPLINE_CURVE ( 3, ( #22766, #12488, #18145, #1535 ),
 .UNSPECIFIED., .F., .F. ) 
 B_SPLINE_CURVE_WITH_KNOTS ( ( 4, 4 ),
 ( 5.387520513321721438, 5.560451059366169346 ),
 .UNSPECIFIED. ) 
 CURVE ( )  GEOMETRIC_REPRESENTATION_ITEM ( )  RATIONAL_B_SPLINE_CURVE ( ( 1.000000000000000000, 0.9975094710839674805, 0.9975094710839674805, 1.000000000000000000 ) ) 
 REPRESENTATION_ITEM ( '' )  );
#23583=CARTESIAN_POINT ( 'NONE',  ( 290.0000000000000000, -42.00000000000000000, 26.50000000000000000 ) ) ;
#23587=CYLINDRICAL_SURFACE ( 'NONE', #14169, 4.000000000000000000 ) ;
#23596=CARTESIAN_POINT ( 'NONE',  ( 7.000000000000000000, -26.42999999999999972, -9.412893218813501051 ) ) ;
#23617=CARTESIAN_POINT ( 'NONE',  ( 7.000000000000000000, -39.79999999999954952, -8.900000000000419575 ) ) ;
#23628=VERTEX_POINT ( 'NONE', #64093 ) ;
#23629=LINE ( 'NONE', #23289, #37653 ) ;
#23633=VECTOR ( 'NONE', #23909, 1000.000000000000000 ) ;
#23639=CYLINDRICAL_SURFACE ( 'NONE', #64170, 0.5000000000009302559 ) ;
#23642=ORIENTED_EDGE ( 'NONE', *, *, #45744, .F. ) ;
#23646=LINE ( 'NONE', #45211, #1856 ) ;
#23655=EDGE_CURVE ( 'NONE', #30525, #50924, #59807, .T. ) ;
#23661=VERTEX_POINT ( 'NONE', #59463 ) ;
#23682=EDGE_CURVE ( 'NONE', #10783, #5708, #8767, .T. ) ;
#23684=FACE_OUTER_BOUND ( 'NONE', #32543, .T. ) ;
#23685=DIRECTION ( 'NONE',  ( 0.000000000000000000, 1.000000000000000000, 0.000000000000000000 ) ) ;
#23692=AXIS2_PLACEMENT_3D ( 'NONE', #68138, #40557, #45868 ) ;
#23720=CARTESIAN_POINT ( 'NONE',  ( 7.000000000000000000, -39.80000000000000426, 8.400000000000000355 ) ) ;
#23728=EDGE_CURVE ( 'NONE', #21706, #62668, #22365, .T. ) ;
#23758=DIRECTION ( 'NONE',  ( -1.000000000000000000, 0.000000000000000000, 0.000000000000000000 ) ) ;
#23761=CARTESIAN_POINT ( 'NONE',  ( 283.0000000000000568, -42.50000000000000000, -14.49999999999904077 ) ) ;
#23775=ORIENTED_EDGE ( 'NONE', *, *, #63237, .F. ) ;
#23787=FACE_OUTER_BOUND ( 'NONE', #44501, .T. ) ;
#23792=DIRECTION ( 'NONE',  ( 1.000000000000000000, 0.000000000000000000, 0.000000000000000000 ) ) ;
#23807=ORIENTED_EDGE ( 'NONE', *, *, #11009, .T. ) ;
#23829=EDGE_CURVE ( 'NONE', #62902, #48603, #3197, .T. ) ;
#23843=VECTOR ( 'NONE', #57416, 1000.000000000000000 ) ;
#23850=CIRCLE ( 'NONE', #42892, 0.4999999999945519691 ) ;
#23861=EDGE_CURVE ( 'NONE', #68300, #36802, #23455, .T. ) ;
#23867=VECTOR ( 'NONE', #60558, 1000.000000000000000 ) ;
#23876=CARTESIAN_POINT ( 'NONE',  ( 283.0000000000000568, -25.69999999999924967, -14.52500000000000213 ) ) ;
#23877=EDGE_CURVE ( 'NONE', #6538, #23628, #51269, .T. ) ;
#23886=CARTESIAN_POINT ( 'NONE',  ( 283.0000000000000568, -32.44999999999905071, -13.20000000000091944 ) ) ;
#23902=CARTESIAN_POINT ( 'NONE',  ( 275.0000000000000000, -0.5000000000000000000, -26.50000000000000000 ) ) ;
#23909=DIRECTION ( 'NONE',  ( 0.000000000000000000, 0.000000000000000000, -1.000000000000000000 ) ) ;
#23913=EDGE_CURVE ( 'NONE', #13668, #60332, #30056, .T. ) ;
#23962=VERTEX_POINT ( 'NONE', #53045 ) ;
#23965=ORIENTED_EDGE ( 'NONE', *, *, #64569, .T. ) ;
#23972=ORIENTED_EDGE ( 'NONE', *, *, #6675, .T. ) ;
#24002=ORIENTED_EDGE ( 'NONE', *, *, #26576, .F. ) ;
#24019=VERTEX_POINT ( 'NONE', #25461 ) ;
#24040=ADVANCED_FACE ( 'NONE', ( #68601 ), #36057, .T. ) ;
#24050=FACE_OUTER_BOUND ( 'NONE', #62819, .T. ) ;
#24083=CIRCLE ( 'NONE', #32035, 0.5000000000009441337 ) ;
#24097=CARTESIAN_POINT ( 'NONE',  ( 275.0000000000001137, -0.5000000000000603961, 26.49999999999996092 ) ) ;
#24108=CARTESIAN_POINT ( 'NONE',  ( 277.3542486889354564, -20.50000000000000000, 17.00000000000000000 ) ) ;
#24119=AXIS2_PLACEMENT_3D ( 'NONE', #14606, #29470, #2597 ) ;
#24124=EDGE_CURVE ( 'NONE', #38982, #8022, #64165, .T. ) ;
#24136=VERTEX_POINT ( 'NONE', #15899 ) ;
#24137=EDGE_CURVE ( 'NONE', #62476, #38230, #58508, .T. ) ;
#24157=ORIENTED_EDGE ( 'NONE', *, *, #28561, .F. ) ;
#24161=ORIENTED_EDGE ( 'NONE', *, *, #44079, .F. ) ;
#24179=DIRECTION ( 'NONE',  ( 0.000000000000000000, 0.000000000000000000, -1.000000000000000000 ) ) ;
#24198=ORIENTED_EDGE ( 'NONE', *, *, #62341, .T. ) ;
#24219=CARTESIAN_POINT ( 'NONE',  ( 275.5000000000000000, -42.50000000000000000, -15.10000000000000142 ) ) ;
#24233=ORIENTED_EDGE ( 'NONE', *, *, #67595, .F. ) ;
#24235=VERTEX_POINT ( 'NONE', #34206 ) ;
#24240=CARTESIAN_POINT ( 'NONE',  ( 7.500000000000000000, -20.40000000000000213, -20.00000000000000000 ) ) ;
#24247=CYLINDRICAL_SURFACE ( 'NONE', #56303, 0.9999999999984570120 ) ;
#24248=CARTESIAN_POINT ( 'NONE',  ( 7.000000000000000000, -26.42999999999999972, 9.412893218813501051 ) ) ;
#24256=VERTEX_POINT ( 'NONE', #45521 ) ;
#24259=DIRECTION ( 'NONE',  ( -1.000000000000000000, 0.000000000000000000, 0.000000000000000000 ) ) ;
#24262=DIRECTION ( 'NONE',  ( -1.000000000000000000, 0.000000000000000000, 0.000000000000000000 ) ) ;
#24264=VECTOR ( 'NONE', #65743, 1000.000000000000000 ) ;
#24290=ORIENTED_EDGE ( 'NONE', *, *, #48380, .F. ) ;
#24299=LINE ( 'NONE', #67448, #19657 ) ;
#24300=FACE_OUTER_BOUND ( 'NONE', #15440, .T. ) ;
#24303=DIRECTION ( 'NONE',  ( 0.7071067811865490160, 0.000000000000000000, -0.7071067811865461294 ) ) ;
#24315=ORIENTED_EDGE ( 'NONE', *, *, #1750, .T. ) ;
#24330=VERTEX_POINT ( 'NONE', #46926 ) ;
#24338=FACE_OUTER_BOUND ( 'NONE', #26594, .T. ) ;
#24350=VERTEX_POINT ( 'NONE', #40921 ) ;
#24369=ORIENTED_EDGE ( 'NONE', *, *, #28658, .F. ) ;
#24405=DIRECTION ( 'NONE',  ( -1.000000000000000000, 0.000000000000000000, 0.000000000000000000 ) ) ;
#24426=VECTOR ( 'NONE', #35137, 1000.000000000000114 ) ;
#24430=FACE_OUTER_BOUND ( 'NONE', #57744, .T. ) ;
#24435=ORIENTED_EDGE ( 'NONE', *, *, #18267, .F. ) ;
#24436=VECTOR ( 'NONE', #55496, 1000.000000000000000 ) ;
#24439=DIRECTION ( 'NONE',  ( -1.000000000000000000, 0.000000000000000000, 0.000000000000000000 ) ) ;
#24445=ORIENTED_EDGE ( 'NONE', *, *, #61800, .F. ) ;
#24446=DIRECTION ( 'NONE',  ( 0.5773502691896175154, 0.5773502691896339467, 0.5773502691896257311 ) ) ;
#24458=DIRECTION ( 'NONE',  ( 1.000000000000000000, 0.000000000000000000, 0.000000000000000000 ) ) ;
#24479=DIRECTION ( 'NONE',  ( 1.000000000000000000, -0.000000000000000000, -0.000000000000000000 ) ) ;
#24494=ORIENTED_EDGE ( 'NONE', *, *, #17068, .T. ) ;
#24524=DIRECTION ( 'NONE',  ( 0.000000000000000000, -1.000000000000000000, -1.880440247955360336E-12 ) ) ;
#24544=CARTESIAN_POINT ( 'NONE',  ( 283.0000000000000568, -38.15000000000000568, -14.50000000000000000 ) ) ;
#24555=LINE ( 'NONE', #4042, #52958 ) ;
#24562=DIRECTION ( 'NONE',  ( 0.000000000000000000, -0.7071067811865474617, 0.7071067811865474617 ) ) ;
#24597=EDGE_CURVE ( 'NONE', #42376, #42028, #29188, .T. ) ;
#24607=CARTESIAN_POINT ( 'NONE',  ( 283.0000000000000568, -42.00000000000000000, -15.00000000000000000 ) ) ;
#24610=EDGE_CURVE ( 'NONE', #27121, #35722, #9998, .T. ) ;
#24625=AXIS2_PLACEMENT_3D ( 'NONE', #9549, #31126, #30765 ) ;
#24629=ORIENTED_EDGE ( 'NONE', *, *, #5875, .F. ) ;
#24641=EDGE_LOOP ( 'NONE', ( #51916, #67604, #57015, #50479 ) ) ;
#24644=DIRECTION ( 'NONE',  ( 1.000000000000000000, -0.000000000000000000, -0.000000000000000000 ) ) ;
#24650=CARTESIAN_POINT ( 'NONE',  ( 15.00000000000000000, -0.5000000000000000000, 30.00000000000000000 ) ) ;
#24660=CARTESIAN_POINT ( 'NONE',  ( 283.0000000000000568, -26.28355339059299922, -9.766446609406699508 ) ) ;
#24682=VERTEX_POINT ( 'NONE', #29448 ) ;
#24690=DIRECTION ( 'NONE',  ( -0.5773502691896257311, -0.5773502691896257311, 0.5773502691896257311 ) ) ;
#24693=DIRECTION ( 'NONE',  ( -0.7071067811865470176, 0.000000000000000000, 0.7071067811865480168 ) ) ;
#24724=DIRECTION ( 'NONE',  ( 0.000000000000000000, 0.7071067811865474617, 0.7071067811865474617 ) ) ;
#24738=DIRECTION ( 'NONE',  ( -1.000000000000000000, 0.000000000000000000, 0.000000000000000000 ) ) ;
#24750=ORIENTED_EDGE ( 'NONE', *, *, #51989, .T. ) ;
#24764=ADVANCED_FACE ( 'NONE', ( #58785 ), #63387, .F. ) ;
#24765=DIRECTION ( 'NONE',  ( 0.000000000000000000, 0.000000000000000000, -1.000000000000000000 ) ) ;
#24776=VECTOR ( 'NONE', #45581, 1000.000000000000000 ) ;
#24782=ORIENTED_EDGE ( 'NONE', *, *, #38296, .T. ) ;
#24787=AXIS2_PLACEMENT_3D ( 'NONE', #30922, #13950, #46823 ) ;
#24802=CARTESIAN_POINT ( 'NONE',  ( 283.0000000000000568, -37.15000000000001279, -7.700000000000000178 ) ) ;
#24810=DIRECTION ( 'NONE',  ( 0.000000000000000000, 0.000000000000000000, -1.000000000000000000 ) ) ;
#24824=VECTOR ( 'NONE', #62106, 1000.000000000000000 ) ;
#24827=DIRECTION ( 'NONE',  ( 0.000000000000000000, 0.000000000000000000, 1.000000000000000000 ) ) ;
#24835=ORIENTED_EDGE ( 'NONE', *, *, #49300, .T. ) ;
#24846=ORIENTED_EDGE ( 'NONE', *, *, #39473, .T. ) ;
#24849=ORIENTED_EDGE ( 'NONE', *, *, #4855, .F. ) ;
#24865=VECTOR ( 'NONE', #39365, 1000.000000000000114 ) ;
#24874=ORIENTED_EDGE ( 'NONE', *, *, #5256, .T. ) ;
#24890=VERTEX_POINT ( 'NONE', #42158 ) ;
#24891=CIRCLE ( 'NONE', #49716, 4.000000000000000000 ) ;
#24892=CARTESIAN_POINT ( 'NONE',  ( 7.000000000000000000, -26.28355339059299922, -9.766446609406699508 ) ) ;
#24920=DIRECTION ( 'NONE',  ( 0.000000000000000000, 0.000000000000000000, 1.000000000000000000 ) ) ;
#24922=ORIENTED_EDGE ( 'NONE', *, *, #43339, .F. ) ;
#24928=ORIENTED_EDGE ( 'NONE', *, *, #53082, .F. ) ;
#24933=EDGE_CURVE ( 'NONE', #42376, #36190, #43552, .T. ) ;
#24948=EDGE_CURVE ( 'NONE', #34171, #66149, #12393, .T. ) ;
#24995=PLANE ( 'NONE',  #25402 ) ;
#25015=VECTOR ( 'NONE', #43596, 1000.000000000000000 ) ;
#25049=ORIENTED_EDGE ( 'NONE', *, *, #57700, .F. ) ;
#25051=DIRECTION ( 'NONE',  ( 0.000000000000000000, 0.000000000000000000, 1.000000000000000000 ) ) ;
#25055=CARTESIAN_POINT ( 'NONE',  ( 276.8000000000000682, -53.81370849898476649, -17.60000000000000142 ) ) ;
#25068=CARTESIAN_POINT ( 'NONE',  ( 15.00000000000000000, -20.40000000000000213, 17.60000000000000142 ) ) ;
#25069=CARTESIAN_POINT ( 'NONE',  ( 15.00000000000000000, -25.93000000000544958, 9.412893218815410634 ) ) ;
#25083=LINE ( 'NONE', #10215, #63567 ) ;
#25091=DIRECTION ( 'NONE',  ( 0.000000000000000000, 0.000000000000000000, 1.000000000000000000 ) ) ;
#25123=ORIENTED_EDGE ( 'NONE', *, *, #45815, .T. ) ;
#25127=DIRECTION ( 'NONE',  ( 0.000000000000000000, 0.000000000000000000, 1.000000000000000000 ) ) ;
#25132=ORIENTED_EDGE ( 'NONE', *, *, #3486, .F. ) ;
#25135=CARTESIAN_POINT ( 'NONE',  ( 283.0000000000000568, -37.61196062927500350, -8.008708659369300875 ) ) ;
#25149=VERTEX_POINT ( 'NONE', #55893 ) ;
#25162=CARTESIAN_POINT ( 'NONE',  ( 14.50000000000000000, 0.000000000000000000, 26.50000000000000000 ) ) ;
#25169=VECTOR ( 'NONE', #10467, 1000.000000000000000 ) ;
#25170=ORIENTED_EDGE ( 'NONE', *, *, #47362, .T. ) ;
#25174=CARTESIAN_POINT ( 'NONE',  ( 275.0000000000000000, -21.00000000000000000, 0.000000000000000000 ) ) ;
#25191=DIRECTION ( 'NONE',  ( 0.000000000000000000, 0.000000000000000000, -1.000000000000000000 ) ) ;
#25195=VECTOR ( 'NONE', #67069, 1000.000000000000114 ) ;
#25212=VECTOR ( 'NONE', #58067, 1000.000000000000000 ) ;
#25272=LINE ( 'NONE', #10068, #35325 ) ;
#25273=ORIENTED_EDGE ( 'NONE', *, *, #69147, .F. ) ;
#25280=LINE ( 'NONE', #63113, #48663 ) ;
#25283=CIRCLE ( 'NONE', #44491, 0.9999999999984570120 ) ;
#25288=EDGE_CURVE ( 'NONE', #596, #15713, #47037, .T. ) ;
#25301=AXIS2_PLACEMENT_3D ( 'NONE', #46740, #58059, #8909 ) ;
#25303=DIRECTION ( 'NONE',  ( -1.000000000000000000, 0.000000000000000000, 0.000000000000000000 ) ) ;
#25313=ORIENTED_EDGE ( 'NONE', *, *, #29751, .T. ) ;
#25318=ORIENTED_EDGE ( 'NONE', *, *, #69182, .T. ) ;
#25350=CARTESIAN_POINT ( 'NONE',  ( 7.000000000000000000, -21.00000000000000000, 7.799999999999999822 ) ) ;
#25356=ORIENTED_EDGE ( 'NONE', *, *, #68248, .T. ) ;
#25376=VERTEX_POINT ( 'NONE', #5655 ) ;
#25387=DIRECTION ( 'NONE',  ( -1.000000000000000000, 0.000000000000000000, 0.000000000000000000 ) ) ;
#25395=ORIENTED_EDGE ( 'NONE', *, *, #60922, .T. ) ;
#25402=AXIS2_PLACEMENT_3D ( 'NONE', #24650, #30304, #46199 ) ;
#25410=ORIENTED_EDGE ( 'NONE', *, *, #3434, .T. ) ;
#25432=CARTESIAN_POINT ( 'NONE',  ( 15.00000000000000000, -20.40000000000000213, 12.40000000000000213 ) ) ;
#25434=CARTESIAN_POINT ( 'NONE',  ( 289.5000000000000000, -42.50000000000000000, 26.50000000000000000 ) ) ;
#25437=CIRCLE ( 'NONE', #62721, 0.5000000000004167777 ) ;
#25446=ORIENTED_EDGE ( 'NONE', *, *, #59572, .T. ) ;
#25456=ORIENTED_EDGE ( 'NONE', *, *, #62511, .F. ) ;
#25460=VECTOR ( 'NONE', #51244, 1000.000000000000114 ) ;
#25461=CARTESIAN_POINT ( 'NONE',  ( 7.000000000000000000, -39.80000000000000426, 12.69999999999999929 ) ) ;
#25468=ORIENTED_EDGE ( 'NONE', *, *, #29105, .F. ) ;
#25495=EDGE_CURVE ( 'NONE', #49302, #27615, #3121, .T. ) ;
#25509=EDGE_LOOP ( 'NONE', ( #8388, #25410, #11459, #46606, #14137, #40097, #16027, #62346, #40583, #51810 ) ) ;
#25511=AXIS2_PLACEMENT_3D ( 'NONE', #49948, #11769, #60567 ) ;
#25518=DIRECTION ( 'NONE',  ( 0.000000000000000000, 0.000000000000000000, -1.000000000000000000 ) ) ;
#25532=AXIS2_PLACEMENT_3D ( 'NONE', #16820, #64910, #59607 ) ;
#25540=VECTOR ( 'NONE', #33703, 1000.000000000000000 ) ;
#25541=CYLINDRICAL_SURFACE ( 'NONE', #29138, 0.5000000000009354739 ) ;
#25545=VERTEX_POINT ( 'NONE', #66421 ) ;
#25565=DIRECTION ( 'NONE',  ( 0.000000000000000000, -0.7071067811865474617, -0.7071067811865474617 ) ) ;
#25602=DIRECTION ( 'NONE',  ( -1.000000000000000000, 0.000000000000000000, 0.000000000000000000 ) ) ;
#25613=VECTOR ( 'NONE', #15936, 1000.000000000000000 ) ;
#25636=CARTESIAN_POINT ( 'NONE',  ( 283.0000000000000568, -26.42999999999999972, 9.412893218813501051 ) ) ;
#25641=VECTOR ( 'NONE', #41604, 1000.000000000000000 ) ;
#25650=CIRCLE ( 'NONE', #35821, 0.9999999999984534593 ) ;
#25665=ORIENTED_EDGE ( 'NONE', *, *, #47956, .F. ) ;
#25678=VERTEX_POINT ( 'NONE', #64271 ) ;
#25683=CARTESIAN_POINT ( 'NONE',  ( 283.0000000000000568, -32.44999999999905071, 13.20000000000091944 ) ) ;
#25701=DIRECTION ( 'NONE',  ( 0.000000000000000000, 1.000000000000000000, 1.883909694907254982E-12 ) ) ;
#25705=VECTOR ( 'NONE', #28495, 1000.000000000000000 ) ;
#25706=DIRECTION ( 'NONE',  ( 0.000000000000000000, -0.7071067811865470176, 0.7071067811865480168 ) ) ;
#25715=VECTOR ( 'NONE', #55013, 1000.000000000000000 ) ;
#25718=DIRECTION ( 'NONE',  ( -0.7071067811865474617, 0.000000000000000000, -0.7071067811865474617 ) ) ;
#25721=CARTESIAN_POINT ( 'NONE',  ( 283.0000000000000568, -40.30000000000000426, 8.900000000000000355 ) ) ;
#25729=ORIENTED_EDGE ( 'NONE', *, *, #67780, .F. ) ;
#25739=ORIENTED_EDGE ( 'NONE', *, *, #46531, .F. ) ;
#25742=VERTEX_POINT ( 'NONE', #4524 ) ;
#25743=ORIENTED_EDGE ( 'NONE', *, *, #1680, .F. ) ;
#25745=VECTOR ( 'NONE', #24405, 1000.000000000000000 ) ;
#25757=DIRECTION ( 'NONE',  ( 0.000000000000000000, 0.000000000000000000, -1.000000000000000000 ) ) ;
#25776=EDGE_LOOP ( 'NONE', ( #32739, #58167, #26115, #11066 ) ) ;
#25799=LINE ( 'NONE', #30741, #21134 ) ;
#25804=ORIENTED_EDGE ( 'NONE', *, *, #36236, .T. ) ;
#25836=DIRECTION ( 'NONE',  ( 1.000000000000000000, -0.000000000000000000, -0.000000000000000000 ) ) ;
#25844=CARTESIAN_POINT ( 'NONE',  ( 283.0000000000000568, -30.45000000000094786, -14.49999999999906031 ) ) ;
#25846=AXIS2_PLACEMENT_3D ( 'NONE', #42679, #47986, #12482 ) ;
#25859=ORIENTED_EDGE ( 'NONE', *, *, #31267, .T. ) ;
#25874=CARTESIAN_POINT ( 'NONE',  ( 283.0000000000000568, -26.50000000000000000, -0.5000000000000000000 ) ) ;
#25899=EDGE_LOOP ( 'NONE', ( #49471, #61500, #39763, #17625 ) ) ;
#25931=ADVANCED_FACE ( 'NONE', ( #61361 ), #24247, .F. ) ;
#25938=DIRECTION ( 'NONE',  ( 1.000000000000000000, -0.000000000000000000, -0.000000000000000000 ) ) ;
#25956=ORIENTED_EDGE ( 'NONE', *, *, #14327, .T. ) ;
#25957=VECTOR ( 'NONE', #30030, 1000.000000000000000 ) ;
#25961=VECTOR ( 'NONE', #23001, 1000.000000000000114 ) ;
#25964=CARTESIAN_POINT ( 'NONE',  ( 283.0000000000000568, -32.94999999999885176, 8.199999999997979572 ) ) ;
#25968=LINE ( 'NONE', #42213, #12148 ) ;
#26069=FACE_BOUND ( 'NONE', #36582, .T. ) ;
#26078=CARTESIAN_POINT ( 'NONE',  ( 7.000000000000000000, -21.00000000000000000, -12.50000000000000000 ) ) ;
#26094=ORIENTED_EDGE ( 'NONE', *, *, #54455, .T. ) ;
#26111=ORIENTED_EDGE ( 'NONE', *, *, #56932, .T. ) ;
#26115=ORIENTED_EDGE ( 'NONE', *, *, #22713, .F. ) ;
#26130=LINE ( 'NONE', #10206, #23012 ) ;
#26133=CARTESIAN_POINT ( 'NONE',  ( 275.0000000000000000, -38.64999999999999858, -12.69999999999999929 ) ) ;
#26150=ORIENTED_EDGE ( 'NONE', *, *, #54017, .F. ) ;
#26187=VERTEX_POINT ( 'NONE', #58884 ) ;
#26189=EDGE_CURVE ( 'NONE', #33919, #596, #16786, .T. ) ;
#26201=CARTESIAN_POINT ( 'NONE',  ( 283.0000000000000568, -25.50000000000000355, -14.74860679774999994 ) ) ;
#26212=DIRECTION ( 'NONE',  ( 0.000000000000000000, -1.000000000000000000, 0.000000000000000000 ) ) ;
#26216=EDGE_LOOP ( 'NONE', ( #38094, #5653, #35452, #26611 ) ) ;
#26217=LINE ( 'NONE', #11000, #4495 ) ;
#26243=ORIENTED_EDGE ( 'NONE', *, *, #16980, .F. ) ;
#26250=VERTEX_POINT ( 'NONE', #21742 ) ;
#26254=EDGE_LOOP ( 'NONE', ( #38868, #16971, #9924, #38461 ) ) ;
#26262=CARTESIAN_POINT ( 'NONE',  ( 7.000000000000000000, -32.95000000000000284, 14.50000000000000000 ) ) ;
#26270=LINE ( 'NONE', #41825, #17302 ) ;
#26281=EDGE_CURVE ( 'NONE', #29414, #39081, #28095, .T. ) ;
#26307=DIRECTION ( 'NONE',  ( 1.000000000000000000, -0.000000000000000000, -0.000000000000000000 ) ) ;
#26331=VECTOR ( 'NONE', #9974, 1000.000000000000000 ) ;
#26343=ORIENTED_EDGE ( 'NONE', *, *, #52442, .T. ) ;
#26346=LINE ( 'NONE', #3730, #55755 ) ;
#26366=CARTESIAN_POINT ( 'NONE',  ( 0.4999999999999964473, -0.4999999999999964473, 26.99999999999999645 ) ) ;
#26367=EDGE_LOOP ( 'NONE', ( #10190, #42276, #46999, #52330, #69294, #5229, #14001, #15660, #34242, #37708, #8516, #3646, #47354, #41369, #48272, #12147, #49715, #50862, #45440, #20341, #39812, #49862, #51836, #36562 ) ) ;
#26375=VECTOR ( 'NONE', #21291, 1000.000000000000000 ) ;
#26387=FACE_OUTER_BOUND ( 'NONE', #27032, .T. ) ;
#26400=ORIENTED_EDGE ( 'NONE', *, *, #60739, .T. ) ;
#26412=AXIS2_PLACEMENT_3D ( 'NONE', #5403, #54183, #59821 ) ;
#26442=EDGE_CURVE ( 'NONE', #49302, #9032, #58640, .T. ) ;
#26444=VERTEX_POINT ( 'NONE', #65453 ) ;
#26448=EDGE_CURVE ( 'NONE', #46983, #40696, #12027, .T. ) ;
#26454=VECTOR ( 'NONE', #60248, 1000.000000000000000 ) ;
#26457=VERTEX_POINT ( 'NONE', #1429 ) ;
#26462=ORIENTED_EDGE ( 'NONE', *, *, #14477, .F. ) ;
#26482=DIRECTION ( 'NONE',  ( 0.000000000000000000, 1.000000000000000000, 0.000000000000000000 ) ) ;
#26512=CARTESIAN_POINT ( 'NONE',  ( 7.000000000000000000, -20.40000000000000213, -17.60000000000000142 ) ) ;
#26518=ADVANCED_FACE ( 'NONE', ( #38916 ), #27618, .T. ) ;
#26525=AXIS2_PLACEMENT_3D ( 'NONE', #35727, #25836, #47738 ) ;
#26526=CARTESIAN_POINT ( 'NONE',  ( 283.0000000000000568, -23.65000000000000568, 12.40000000000000213 ) ) ;
#26536=CARTESIAN_POINT ( 'NONE',  ( 14.75000000000000178, -42.25000000000000000, -26.75000000000000000 ) ) ;
#26538=ORIENTED_EDGE ( 'NONE', *, *, #26774, .F. ) ;
#26544=ORIENTED_EDGE ( 'NONE', *, *, #69100, .T. ) ;
#26550=AXIS2_PLACEMENT_3D ( 'NONE', #25844, #40692, #67918 ) ;
#26567=CARTESIAN_POINT ( 'NONE',  ( 275.0000000000000000, -38.65000000000095781, -13.20000000000094253 ) ) ;
#26576=EDGE_CURVE ( 'NONE', #66290, #14513, #12934, .T. ) ;
#26577=ORIENTED_EDGE ( 'NONE', *, *, #32361, .T. ) ;
#26583=DIRECTION ( 'NONE',  ( 0.000000000000000000, 0.000000000000000000, 1.000000000000000000 ) ) ;
#26589=DIRECTION ( 'NONE',  ( 1.000000000000000000, -0.000000000000000000, -0.000000000000000000 ) ) ;
#26594=EDGE_LOOP ( 'NONE', ( #46152, #5536, #3917, #63252 ) ) ;
#26596=CARTESIAN_POINT ( 'NONE',  ( 275.0000000000000000, -21.00000000000000000, -17.50000000000000000 ) ) ;
#26611=ORIENTED_EDGE ( 'NONE', *, *, #47923, .T. ) ;
#26634=LINE ( 'NONE', #47836, #48615 ) ;
#26659=FACE_OUTER_BOUND ( 'NONE', #37873, .T. ) ;
#26667=CARTESIAN_POINT ( 'NONE',  ( 7.000000000000000000, -42.50000000000000000, 7.500000000000000000 ) ) ;
#26675=CARTESIAN_POINT ( 'NONE',  ( 14.50000000000000000, -42.50000000000000000, 26.50000000000000000 ) ) ;
#26683=VERTEX_POINT ( 'NONE', #28855 ) ;
#26692=VECTOR ( 'NONE', #1531, 1000.000000000000000 ) ;
#26695=ADVANCED_FACE ( 'NONE', ( #29558 ), #2686, .F. ) ;
#26696=AXIS2_PLACEMENT_3D ( 'NONE', #9594, #36458, #4988 ) ;
#26704=AXIS2_PLACEMENT_3D ( 'NONE', #50866, #34945, #39222 ) ;
#26706=VERTEX_POINT ( 'NONE', #8698 ) ;
#26713=VERTEX_POINT ( 'NONE', #57484 ) ;
#26716=LINE ( 'NONE', #64549, #22584 ) ;
#26721=EDGE_CURVE ( 'NONE', #67348, #16165, #60443, .T. ) ;
#26726=DIRECTION ( 'NONE',  ( 0.000000000000000000, -1.000000000000000000, 1.540434446669787085E-12 ) ) ;
#26736=EDGE_LOOP ( 'NONE', ( #67587, #21226, #34828, #8410 ) ) ;
#26738=CARTESIAN_POINT ( 'NONE',  ( 14.74999999999998934, -0.2500000000000142109, 26.75000000000000711 ) ) ;
#26774=EDGE_CURVE ( 'NONE', #24256, #56561, #42270, .T. ) ;
#26777=EDGE_CURVE ( 'NONE', #17604, #31415, #9764, .T. ) ;
#26782=EDGE_CURVE ( 'NONE', #28379, #55647, #31343, .T. ) ;
#26783=DIRECTION ( 'NONE',  ( 1.000000000000000000, 0.000000000000000000, 0.000000000000000000 ) ) ;
#26789=EDGE_CURVE ( 'NONE', #59688, #41721, #52542, .T. ) ;
#26798=DIRECTION ( 'NONE',  ( 0.000000000000000000, 1.000000000000000000, 0.000000000000000000 ) ) ;
#26816=EDGE_LOOP ( 'NONE', ( #27667, #39223 ) ) ;
#26818=VECTOR ( 'NONE', #27225, 1000.000000000000114 ) ;
#26819=FACE_OUTER_BOUND ( 'NONE', #46767, .T. ) ;
#26830=ORIENTED_EDGE ( 'NONE', *, *, #57426, .F. ) ;
#26841=DIRECTION ( 'NONE',  ( 0.000000000000000000, 1.000000000000000000, 0.000000000000000000 ) ) ;
#26843=VECTOR ( 'NONE', #48236, 1000.000000000000000 ) ;
#26850=ADVANCED_FACE ( 'NONE', ( #65584 ), #59236, .F. ) ;
#26874=ORIENTED_EDGE ( 'NONE', *, *, #19983, .T. ) ;
#26881=CARTESIAN_POINT ( 'NONE',  ( 283.0000000000000568, -42.00000000000000000, -7.000000000000000000 ) ) ;
#26884=DIRECTION ( 'NONE',  ( 1.000000000000000000, 0.000000000000000000, 0.000000000000000000 ) ) ;
#26927=DIRECTION ( 'NONE',  ( 1.000000000000000000, -0.000000000000000000, -0.000000000000000000 ) ) ;
#26928=ORIENTED_EDGE ( 'NONE', *, *, #12525, .F. ) ;
#26929=SURFACE_STYLE_USAGE ( .BOTH. , #65778 ) ;
#26935=CARTESIAN_POINT ( 'NONE',  ( 7.500000000000000000, -20.49999999999999645, -16.00000000000000000 ) ) ;
#26962=DIRECTION ( 'NONE',  ( 1.000000000000000000, -0.000000000000000000, -0.000000000000000000 ) ) ;
#26969=CARTESIAN_POINT ( 'NONE',  ( 0.5000000000000000000, -42.50000000000000000, 26.50000000000000000 ) ) ;
#26993=EDGE_LOOP ( 'NONE', ( #29361, #10263, #29383, #36174, #68074 ) ) ;
#26998=VECTOR ( 'NONE', #53580, 1000.000000000000000 ) ;
#26999=DIRECTION ( 'NONE',  ( -1.000000000000000000, 0.000000000000000000, 0.000000000000000000 ) ) ;
#27004=CARTESIAN_POINT ( 'NONE',  ( 7.000000000000000000, -25.00000000000299849, -9.079999998829670460 ) ) ;
#27015=AXIS2_PLACEMENT_3D ( 'NONE', #1344, #27188, #11586 ) ;
#27021=EDGE_LOOP ( 'NONE', ( #60468, #38687, #60463, #5547, #19863, #27311 ) ) ;
#27030=ORIENTED_EDGE ( 'NONE', *, *, #7066, .T. ) ;
#27032=EDGE_LOOP ( 'NONE', ( #53906, #60824, #59929, #37517 ) ) ;
#27036=CIRCLE ( 'NONE', #15772, 5.000000000000000000 ) ;
#27050=EDGE_LOOP ( 'NONE', ( #66528, #51516, #31492, #19626, #32690, #31736 ) ) ;
#27061=VERTEX_POINT ( 'NONE', #39730 ) ;
#27064=LINE ( 'NONE', #33744, #17128 ) ;
#27067=AXIS2_PLACEMENT_3D ( 'NONE', #57910, #41291, #35992 ) ;
#27073=CARTESIAN_POINT ( 'NONE',  ( 282.8893988437589542, -25.27116123426318239, -17.22883876573683182 ) ) ;
#27085=CARTESIAN_POINT ( 'NONE',  ( 275.5000000000000000, 0.000000000000000000, 26.50000000000000000 ) ) ;
#27097=PLANE ( 'NONE',  #42067 ) ;
#27103=EDGE_CURVE ( 'NONE', #1005, #56517, #29481, .T. ) ;
#27120=DIRECTION ( 'NONE',  ( 0.000000000000000000, 0.000000000000000000, 1.000000000000000000 ) ) ;
#27121=VERTEX_POINT ( 'NONE', #36534 ) ;
#27138=ORIENTED_EDGE ( 'NONE', *, *, #49220, .F. ) ;
#27152=DIRECTION ( 'NONE',  ( 0.000000000000000000, 1.000000000000000000, 0.000000000000000000 ) ) ;
#27172=EDGE_CURVE ( 'NONE', #15713, #17105, #36183, .T. ) ;
#27183=LINE ( 'NONE', #10220, #43492 ) ;
#27188=DIRECTION ( 'NONE',  ( 1.000000000000000000, -0.000000000000000000, -0.000000000000000000 ) ) ;
#27196=CARTESIAN_POINT ( 'NONE',  ( 7.000000000000000000, -25.50000000000000355, 17.00000000000000000 ) ) ;
#27216=PLANE ( 'NONE',  #6209 ) ;
#27220=DIRECTION ( 'NONE',  ( 0.000000000000000000, 1.550842787525658429E-12, 1.000000000000000000 ) ) ;
#27225=DIRECTION ( 'NONE',  ( 0.000000000000000000, -0.7071067811865474617, -0.7071067811865474617 ) ) ;
#27233=ORIENTED_EDGE ( 'NONE', *, *, #19800, .T. ) ;
#27256=CARTESIAN_POINT ( 'NONE',  ( 283.0000000000000568, -28.94999999999999929, 13.50000000000000000 ) ) ;
#27269=LINE ( 'NONE', #17325, #47508 ) ;
#27283=DIRECTION ( 'NONE',  ( 0.000000000000000000, 0.000000000000000000, -1.000000000000000000 ) ) ;
#27289=EDGE_CURVE ( 'NONE', #26187, #54496, #21329, .T. ) ;
#27290=EDGE_CURVE ( 'NONE', #57189, #53303, #53514, .T. ) ;
#27295=DIRECTION ( 'NONE',  ( 1.000000000000000000, 0.000000000000000000, 0.000000000000000000 ) ) ;
#27307=CARTESIAN_POINT ( 'NONE',  ( 275.0000000000000000, -26.42999999999999972, 9.412893218813501051 ) ) ;
#27311=ORIENTED_EDGE ( 'NONE', *, *, #52429, .T. ) ;
#27315=ORIENTED_EDGE ( 'NONE', *, *, #41991, .T. ) ;
#27328=CYLINDRICAL_SURFACE ( 'NONE', #2669, 1.499999999997026379 ) ;
#27341=CYLINDRICAL_SURFACE ( 'NONE', #18913, 0.2999999999994933941 ) ;
#27351=VECTOR ( 'NONE', #8811, 1000.000000000000000 ) ;
#27353=DIRECTION ( 'NONE',  ( 0.000000000000000000, 0.000000000000000000, -1.000000000000000000 ) ) ;
#27359=FACE_OUTER_BOUND ( 'NONE', #38784, .T. ) ;
#27365=VECTOR ( 'NONE', #5293, 1000.000000000000114 ) ;
#27384=PLANE ( 'NONE',  #31248 ) ;
#27392=ORIENTED_EDGE ( 'NONE', *, *, #66259, .F. ) ;
#27393=AXIS2_PLACEMENT_3D ( 'NONE', #66298, #65277, #16824 ) ;
#27413=DIRECTION ( 'NONE',  ( 0.000000000000000000, 0.000000000000000000, -1.000000000000000000 ) ) ;
#27449=DIRECTION ( 'NONE',  ( 0.7071067811865474617, -0.7071067811865474617, 0.000000000000000000 ) ) ;
#27454=PLANE ( 'NONE',  #1214 ) ;
#27460=ORIENTED_EDGE ( 'NONE', *, *, #62178, .F. ) ;
#27469=DIRECTION ( 'NONE',  ( 0.000000000000000000, -0.9239212585478300266, -0.3825826812643171038 ) ) ;
#27474=ORIENTED_EDGE ( 'NONE', *, *, #39095, .T. ) ;
#27479=AXIS2_PLACEMENT_3D ( 'NONE', #13874, #52789, #4345 ) ;
#27480=ORIENTED_EDGE ( 'NONE', *, *, #29222, .F. ) ;
#27493=AXIS2_PLACEMENT_3D ( 'NONE', #40942, #46951, #24693 ) ;
#27494=EDGE_CURVE ( 'NONE', #13213, #50319, #68281, .T. ) ;
#27514=DIRECTION ( 'NONE',  ( 0.000000000000000000, -1.000000000000000000, 0.000000000000000000 ) ) ;
#27518=DIRECTION ( 'NONE',  ( 0.000000000000000000, 0.000000000000000000, -1.000000000000000000 ) ) ;
#27521=DIRECTION ( 'NONE',  ( 0.000000000000000000, -0.7071067811865475727, -0.7071067811865475727 ) ) ;
#27522=VERTEX_POINT ( 'NONE', #46012 ) ;
#27542=DIRECTION ( 'NONE',  ( 1.000000000000000000, -0.000000000000000000, -0.000000000000000000 ) ) ;
#27545=EDGE_CURVE ( 'NONE', #20854, #53303, #57320, .T. ) ;
#27559=LINE ( 'NONE', #16958, #61665 ) ;
#27566=CARTESIAN_POINT ( 'NONE',  ( 1.000000000000000000, -21.00000000000000000, 5.000000000000000000 ) ) ;
#27578=CARTESIAN_POINT ( 'NONE',  ( 283.0000000000000568, -32.95000000000000284, 7.700000000000000178 ) ) ;
#27579=ORIENTED_EDGE ( 'NONE', *, *, #63756, .T. ) ;
#27603=ORIENTED_EDGE ( 'NONE', *, *, #28561, .T. ) ;
#27609=CARTESIAN_POINT ( 'NONE',  ( 7.000000000000000000, -32.95000000000000284, -14.50000000000000000 ) ) ;
#27615=VERTEX_POINT ( 'NONE', #19834 ) ;
#27618=PLANE ( 'NONE',  #48496 ) ;
#27621=EDGE_CURVE ( 'NONE', #53055, #22100, #20189, .T. ) ;
#27626=VERTEX_POINT ( 'NONE', #42803 ) ;
#27631=CARTESIAN_POINT ( 'NONE',  ( 7.000000000000000000, -25.50000000000000355, 16.03137303340311348 ) ) ;
#27648=ORIENTED_EDGE ( 'NONE', *, *, #38493, .F. ) ;
#27666=DIRECTION ( 'NONE',  ( 1.000000000000000000, 0.000000000000000000, 0.000000000000000000 ) ) ;
#27667=ORIENTED_EDGE ( 'NONE', *, *, #37514, .F. ) ;
#27702=EDGE_CURVE ( 'NONE', #17331, #3096, #15244, .T. ) ;
#27726=DIRECTION ( 'NONE',  ( 0.000000000000000000, -0.7075494706728322480, 0.7066638143775262337 ) ) ;
#27741=ORIENTED_EDGE ( 'NONE', *, *, #69128, .T. ) ;
#27754=DIRECTION ( 'NONE',  ( 0.000000000000000000, -0.7071067811865474617, -0.7071067811865474617 ) ) ;
#27758=AXIS2_PLACEMENT_3D ( 'NONE', #43919, #27666, #54899 ) ;
#27759=CARTESIAN_POINT ( 'NONE',  ( 14.50000000000000000, 0.000000000000000000, 26.50000000000000000 ) ) ;
#27775=ORIENTED_EDGE ( 'NONE', *, *, #45765, .F. ) ;
#27789=CARTESIAN_POINT ( 'NONE',  ( 282.6457513110646005, -20.49999999999999645, -17.00000000000000000 ) ) ;
#27791=VERTEX_POINT ( 'NONE', #17999 ) ;
#27801=CARTESIAN_POINT ( 'NONE',  ( 275.0000000000000000, -25.50000000000000355, -17.00000000000000000 ) ) ;
#27823=CARTESIAN_POINT ( 'NONE',  ( 283.0000000000000568, -42.50000000000000000, 9.700000000000002842 ) ) ;
#27826=CIRCLE ( 'NONE', #13116, 3.999999999999993339 ) ;
#27845=ORIENTED_EDGE ( 'NONE', *, *, #54995, .F. ) ;
#27846=EDGE_CURVE ( 'NONE', #31741, #45978, #61123, .T. ) ;
#27859=DIRECTION ( 'NONE',  ( -1.000000000000000000, 0.000000000000000000, 0.000000000000000000 ) ) ;
#27862=CARTESIAN_POINT ( 'NONE',  ( 7.000000000000000000, -23.29603921945599865, 12.50000000000000000 ) ) ;
#27886=ADVANCED_FACE ( 'NONE', ( #1068 ), #66447, .F. ) ;
#27894=ORIENTED_EDGE ( 'NONE', *, *, #68644, .T. ) ;
#27906=ORIENTED_EDGE ( 'NONE', *, *, #34233, .F. ) ;
#27911=DIRECTION ( 'NONE',  ( 0.000000000000000000, 0.000000000000000000, -1.000000000000000000 ) ) ;
#27912=ORIENTED_EDGE ( 'NONE', *, *, #7346, .T. ) ;
#27928=CYLINDRICAL_SURFACE ( 'NONE', #59458, 0.5000000000009459100 ) ;
#27981=CARTESIAN_POINT ( 'NONE',  ( 7.000000000000000000, -20.40000000000000213, -16.03137303340311348 ) ) ;
#28005=DIRECTION ( 'NONE',  ( 0.000000000000000000, -1.000000000000000000, 0.000000000000000000 ) ) ;
#28013=AXIS2_PLACEMENT_3D ( 'NONE', #39672, #24479, #12793 ) ;
#28034=LINE ( 'NONE', #22724, #47453 ) ;
#28037=DIRECTION ( 'NONE',  ( 1.000000000000000000, 0.000000000000000000, 0.000000000000000000 ) ) ;
#28076=DIRECTION ( 'NONE',  ( 1.000000000000000000, 0.000000000000000000, 0.000000000000000000 ) ) ;
#28080=DIRECTION ( 'NONE',  ( -1.000000000000000000, 0.000000000000000000, 0.000000000000000000 ) ) ;
#28095=CIRCLE ( 'NONE', #64294, 0.3000000000005387246 ) ;
#28096=ADVANCED_FACE ( 'NONE', ( #52648 ), #65591, .F. ) ;
#28099=CARTESIAN_POINT ( 'NONE',  ( 14.50000000000000000, -42.50000000000000000, 30.00000000000000000 ) ) ;
#28101=VECTOR ( 'NONE', #54182, 1000.000000000000000 ) ;
#28105=CYLINDRICAL_SURFACE ( 'NONE', #42596, 5.000000000000000000 ) ;
#28119=FACE_OUTER_BOUND ( 'NONE', #52797, .T. ) ;
#28135=DIRECTION ( 'NONE',  ( 0.000000000000000000, 1.000000000000000000, 1.880440247955334083E-12 ) ) ;
#28154=PLANE ( 'NONE',  #46928 ) ;
#28167=LINE ( 'NONE', #44758, #58199 ) ;
#28178=VECTOR ( 'NONE', #8866, 1000.000000000000000 ) ;
#28185=CARTESIAN_POINT ( 'NONE',  ( 7.000000000000000000, -30.45000000000094786, 14.49999999999906031 ) ) ;
#28189=CARTESIAN_POINT ( 'NONE',  ( 10.14575131106459160, -20.49999999999999645, -17.00000000000000000 ) ) ;
#28205=ORIENTED_EDGE ( 'NONE', *, *, #10262, .T. ) ;
#28219=DIRECTION ( 'NONE',  ( 0.7071067811865490160, 0.000000000000000000, 0.7071067811865461294 ) ) ;
#28220=DIRECTION ( 'NONE',  ( 0.000000000000000000, 0.000000000000000000, 1.000000000000000000 ) ) ;
#28223=LINE ( 'NONE', #5632, #20340 ) ;
#28233=PLANE ( 'NONE',  #32188 ) ;
#28255=CARTESIAN_POINT ( 'NONE',  ( 7.000000000000000000, -26.50000000000000000, 0.5000000000000000000 ) ) ;
#28257=VECTOR ( 'NONE', #69369, 1000.000000000000000 ) ;
#28259=CARTESIAN_POINT ( 'NONE',  ( 283.0000000000000568, -32.95000000000000284, 14.50000000000000000 ) ) ;
#28266=ORIENTED_EDGE ( 'NONE', *, *, #43767, .F. ) ;
#28280=LINE ( 'NONE', #49849, #29110 ) ;
#28281=PLANE ( 'NONE',  #55547 ) ;
#28290=CARTESIAN_POINT ( 'NONE',  ( 283.0000000000000568, -25.14575131106457917, 17.35424868893542438 ) ) ;
#28296=ORIENTED_EDGE ( 'NONE', *, *, #26789, .F. ) ;
#28315=EDGE_CURVE ( 'NONE', #41475, #55991, #15339, .T. ) ;
#28345=EDGE_LOOP ( 'NONE', ( #58390, #28732, #15861, #52990 ) ) ;
#28355=CARTESIAN_POINT ( 'NONE',  ( 275.0000000000000000, -25.69999999999924967, 14.52500000000000213 ) ) ;
#28370=CARTESIAN_POINT ( 'NONE',  ( 15.00000000000000000, -21.00000000000000000, -5.000000000000000000 ) ) ;
#28372=LINE ( 'NONE', #1174, #18618 ) ;
#28379=VERTEX_POINT ( 'NONE', #31275 ) ;
#28381=CARTESIAN_POINT ( 'NONE',  ( 283.0000000000000568, -23.65000000000000568, 12.40000000000000213 ) ) ;
#28395=CARTESIAN_POINT ( 'NONE',  ( 1.000000000000000000, -21.00000000000000000, 0.000000000000000000 ) ) ;
#28400=PLANE ( 'NONE',  #19206 ) ;
#28416=VECTOR ( 'NONE', #14986, 1000.000000000000000 ) ;
#28428=CARTESIAN_POINT ( 'NONE',  ( 283.0000000000000568, -42.50000000000000000, -15.10000000000000142 ) ) ;
#28429=CIRCLE ( 'NONE', #41973, 3.999999999999993339 ) ;
#28434=PLANE ( 'NONE',  #8068 ) ;
#28435=EDGE_CURVE ( 'NONE', #8968, #20434, #38304, .T. ) ;
#28453=CARTESIAN_POINT ( 'NONE',  ( 7.000000000000000000, -38.10000000000000142, -8.400000000000000355 ) ) ;
#28457=DIRECTION ( 'NONE',  ( 0.7071067811865470176, 0.7071067811865480168, 0.000000000000000000 ) ) ;
#28461=ORIENTED_EDGE ( 'NONE', *, *, #22755, .T. ) ;
#28495=DIRECTION ( 'NONE',  ( 0.000000000000000000, -1.000000000000000000, 0.000000000000000000 ) ) ;
#28496=( BOUNDED_CURVE ( )  B_SPLINE_CURVE ( 3, ( #22605, #5327, #54099, #69674 ),
 .UNSPECIFIED., .F., .F. ) 
 B_SPLINE_CURVE_WITH_KNOTS ( ( 4, 4 ),
 ( 2.245927859731928322, 2.418858405776365572 ),
 .UNSPECIFIED. ) 
 CURVE ( )  GEOMETRIC_REPRESENTATION_ITEM ( )  RATIONAL_B_SPLINE_CURVE ( ( 1.000000000000000000, 0.9975094710839678136, 0.9975094710839678136, 1.000000000000000000 ) ) 
 REPRESENTATION_ITEM ( '' )  );
#28498=ORIENTED_EDGE ( 'NONE', *, *, #48835, .T. ) ;
#28509=EDGE_CURVE ( 'NONE', #42130, #38006, #33336, .T. ) ;
#28510=VERTEX_POINT ( 'NONE', #11751 ) ;
#28517=DIRECTION ( 'NONE',  ( 1.000000000000000000, 0.000000000000000000, 0.000000000000000000 ) ) ;
#28521=AXIS2_PLACEMENT_3D ( 'NONE', #66319, #35163, #7243 ) ;
#28526=DIRECTION ( 'NONE',  ( 1.000000000000000000, -0.000000000000000000, -0.000000000000000000 ) ) ;
#28538=DIRECTION ( 'NONE',  ( -0.5773502691896257311, 0.5773502691896257311, 0.5773502691896257311 ) ) ;
#28540=DIRECTION ( 'NONE',  ( 0.000000000000000000, 0.000000000000000000, 1.000000000000000000 ) ) ;
#28543=PLANE ( 'NONE',  #31098 ) ;
#28550=EDGE_LOOP ( 'NONE', ( #14972, #29916, #40848, #4975 ) ) ;
#28552=CARTESIAN_POINT ( 'NONE',  ( 7.000000000000000000, -25.93000000000544958, -9.412893218815410634 ) ) ;
#28560=EDGE_LOOP ( 'NONE', ( #3925, #66336, #49180, #63566, #41516, #48804 ) ) ;
#28561=EDGE_CURVE ( 'NONE', #50939, #65427, #60542, .T. ) ;
#28564=EDGE_LOOP ( 'NONE', ( #14368, #68249, #27474, #5295 ) ) ;
#28574=ORIENTED_EDGE ( 'NONE', *, *, #15756, .T. ) ;
#28582=CARTESIAN_POINT ( 'NONE',  ( 283.0000000000000568, -26.06132420600899735, 10.13999572156699891 ) ) ;
#28595=LINE ( 'NONE', #28255, #24264 ) ;
#28603=VECTOR ( 'NONE', #37286, 1000.000000000000000 ) ;
#28609=FACE_OUTER_BOUND ( 'NONE', #63057, .T. ) ;
#28624=DIRECTION ( 'NONE',  ( 0.7071067811865474617, 0.7071067811865474617, 0.000000000000000000 ) ) ;
#28652=DIRECTION ( 'NONE',  ( 0.000000000000000000, -0.6801302850037772574, -0.7330912599538208507 ) ) ;
#28658=EDGE_CURVE ( 'NONE', #52522, #31415, #56281, .T. ) ;
#28667=EDGE_CURVE ( 'NONE', #38006, #60907, #40372, .T. ) ;
#28674=VECTOR ( 'NONE', #13192, 1000.000000000000000 ) ;
#28717=DIRECTION ( 'NONE',  ( 0.7071067811865474617, 0.7071067811865474617, 0.000000000000000000 ) ) ;
#28732=ORIENTED_EDGE ( 'NONE', *, *, #14307, .T. ) ;
#28741=CARTESIAN_POINT ( 'NONE',  ( 283.0000000000000568, -31.99999999999889866, -7.899999999997660893 ) ) ;
#28772=ORIENTED_EDGE ( 'NONE', *, *, #14307, .F. ) ;
#28801=VECTOR ( 'NONE', #65152, 1000.000000000000000 ) ;
#28807=ORIENTED_EDGE ( 'NONE', *, *, #49667, .F. ) ;
#28817=DIRECTION ( 'NONE',  ( 0.000000000000000000, 0.000000000000000000, -1.000000000000000000 ) ) ;
#28825=DIRECTION ( 'NONE',  ( 1.000000000000000000, -0.000000000000000000, -0.000000000000000000 ) ) ;
#28827=CARTESIAN_POINT ( 'NONE',  ( 276.8775010008008053, -53.81370849898476649, -17.50000000000000000 ) ) ;
#28833=ORIENTED_EDGE ( 'NONE', *, *, #8713, .F. ) ;
#28845=CARTESIAN_POINT ( 'NONE',  ( 283.0000000000000568, -20.40000000000000213, 12.40000000000000213 ) ) ;
#28849=VECTOR ( 'NONE', #49223, 1000.000000000000000 ) ;
#28855=CARTESIAN_POINT ( 'NONE',  ( 7.000000000000000000, -31.30000000000000071, -12.69999999999999929 ) ) ;
#28868=ADVANCED_FACE ( 'NONE', ( #60111 ), #69338, .T. ) ;
#28878=CIRCLE ( 'NONE', #14212, 0.5000000000009441337 ) ;
#28882=LINE ( 'NONE', #17929, #19589 ) ;
#28892=CARTESIAN_POINT ( 'NONE',  ( 15.00000000000000000, -20.40000000000000213, 17.60000000000000142 ) ) ;
#28904=EDGE_CURVE ( 'NONE', #26250, #40700, #28429, .T. ) ;
#28930=PRODUCT_DEFINITION_CONTEXT ( 'detailed design', #62502, 'design' ) ;
#28935=VERTEX_POINT ( 'NONE', #1411 ) ;
#28941=EDGE_LOOP ( 'NONE', ( #57676, #58520, #32169, #16861 ) ) ;
#28957=CYLINDRICAL_SURFACE ( 'NONE', #40256, 0.3000000000005393908 ) ;
#28959=ORIENTED_EDGE ( 'NONE', *, *, #10308, .T. ) ;
#28961=VECTOR ( 'NONE', #63241, 1000.000000000000000 ) ;
#28962=CARTESIAN_POINT ( 'NONE',  ( 1.000000000000000000, -21.00000000000000000, 0.000000000000000000 ) ) ;
#28977=DIRECTION ( 'NONE',  ( -1.000000000000000000, 0.000000000000000000, 0.000000000000000000 ) ) ;
#28978=ADVANCED_FACE ( 'NONE', ( #7051 ), #28281, .T. ) ;
#28984=LINE ( 'NONE', #25434, #11834 ) ;
#28993=ORIENTED_EDGE ( 'NONE', *, *, #22186, .T. ) ;
#29006=ORIENTED_EDGE ( 'NONE', *, *, #69006, .T. ) ;
#29024=LINE ( 'NONE', #55552, #19627 ) ;
#29028=DIRECTION ( 'NONE',  ( 0.000000000000000000, 1.000000000000000000, 1.880440247955360336E-12 ) ) ;
#29091=VERTEX_POINT ( 'NONE', #51601 ) ;
#29097=DIRECTION ( 'NONE',  ( 0.000000000000000000, 1.000000000000000000, 0.000000000000000000 ) ) ;
#29105=EDGE_CURVE ( 'NONE', #35311, #26457, #30022, .T. ) ;
#29110=VECTOR ( 'NONE', #59774, 1000.000000000000000 ) ;
#29112=EDGE_CURVE ( 'NONE', #520, #12942, #3163, .T. ) ;
#29119=VERTEX_POINT ( 'NONE', #45939 ) ;
#29123=CARTESIAN_POINT ( 'NONE',  ( 283.0000000000000568, -38.64999999999999858, 15.00000000000000000 ) ) ;
#29137=CARTESIAN_POINT ( 'NONE',  ( 7.000000000000000000, -42.50000000000000000, -14.50000000000000000 ) ) ;
#29138=AXIS2_PLACEMENT_3D ( 'NONE', #4335, #53463, #26583 ) ;
#29141=ORIENTED_EDGE ( 'NONE', *, *, #67550, .T. ) ;
#29144=LINE ( 'NONE', #55003, #10114 ) ;
#29146=ORIENTED_EDGE ( 'NONE', *, *, #42251, .F. ) ;
#29155=LINE ( 'NONE', #52771, #26331 ) ;
#29166=PLANE ( 'NONE',  #64018 ) ;
#29172=CARTESIAN_POINT ( 'NONE',  ( 283.0000000000000568, -40.30000000000000426, -12.20000000000000107 ) ) ;
#29176=DIRECTION ( 'NONE',  ( 0.000000000000000000, 1.000000000000000000, 0.000000000000000000 ) ) ;
#29188=CIRCLE ( 'NONE', #25846, 0.2999999999994933386 ) ;
#29200=EDGE_CURVE ( 'NONE', #44134, #29889, #31081, .T. ) ;
#29201=FACE_OUTER_BOUND ( 'NONE', #37591, .T. ) ;
#29220=CARTESIAN_POINT ( 'NONE',  ( 276.8000000000000682, -25.60000000000000142, 17.60000000000000142 ) ) ;
#29222=EDGE_CURVE ( 'NONE', #61067, #13213, #63615, .T. ) ;
#29228=LINE ( 'NONE', #50802, #25641 ) ;
#29232=VECTOR ( 'NONE', #44933, 1000.000000000000000 ) ;
#29237=CARTESIAN_POINT ( 'NONE',  ( 14.50000000000000000, -42.50000000000000000, 30.00000000000000000 ) ) ;
#29282=ORIENTED_EDGE ( 'NONE', *, *, #18582, .F. ) ;
#29294=EDGE_CURVE ( 'NONE', #24330, #10503, #32812, .T. ) ;
#29305=LINE ( 'NONE', #56879, #58517 ) ;
#29309=ADVANCED_FACE ( 'NONE', ( #31448 ), #48388, .F. ) ;
#29326=DIRECTION ( 'NONE',  ( 0.000000000000000000, 0.000000000000000000, 1.000000000000000000 ) ) ;
#29338=DIRECTION ( 'NONE',  ( 0.000000000000000000, 1.000000000000000000, 0.000000000000000000 ) ) ;
#29350=LINE ( 'NONE', #64344, #50185 ) ;
#29356=EDGE_CURVE ( 'NONE', #8058, #49494, #54049, .T. ) ;
#29361=ORIENTED_EDGE ( 'NONE', *, *, #12840, .F. ) ;
#29376=CARTESIAN_POINT ( 'NONE',  ( 275.0000000000000000, -42.00000000000000000, 26.50000000000000000 ) ) ;
#29382=CARTESIAN_POINT ( 'NONE',  ( 275.0000000000000000, -38.64999999999999858, 15.00000000000000000 ) ) ;
#29383=ORIENTED_EDGE ( 'NONE', *, *, #22895, .F. ) ;
#29395=LINE ( 'NONE', #13837, #52025 ) ;
#29397=ORIENTED_EDGE ( 'NONE', *, *, #68240, .F. ) ;
#29407=LINE ( 'NONE', #66882, #62927 ) ;
#29414=VERTEX_POINT ( 'NONE', #27862 ) ;
#29437=CARTESIAN_POINT ( 'NONE',  ( 7.500000000000000000, -53.81370849898476649, -16.00000000000000000 ) ) ;
#29448=CARTESIAN_POINT ( 'NONE',  ( 14.50000000000000000, -42.00000000000000000, 27.00000000000000000 ) ) ;
#29464=DIRECTION ( 'NONE',  ( 1.000000000000000000, -0.000000000000000000, -0.000000000000000000 ) ) ;
#29470=DIRECTION ( 'NONE',  ( 1.000000000000000000, -0.000000000000000000, -0.000000000000000000 ) ) ;
#29475=LINE ( 'NONE', #8245, #61006 ) ;
#29477=ORIENTED_EDGE ( 'NONE', *, *, #35031, .T. ) ;
#29481=LINE ( 'NONE', #12172, #31151 ) ;
#29483=ORIENTED_EDGE ( 'NONE', *, *, #51048, .F. ) ;
#29490=ORIENTED_EDGE ( 'NONE', *, *, #23037, .F. ) ;
#29493=PLANE ( 'NONE',  #68860 ) ;
#29500=CARTESIAN_POINT ( 'NONE',  ( 283.0000000000000568, -38.64999999999999858, 15.00000000000000000 ) ) ;
#29503=FACE_OUTER_BOUND ( 'NONE', #53642, .T. ) ;
#29514=CARTESIAN_POINT ( 'NONE',  ( 280.0000000000000000, -20.49999999999999645, -16.00000000000000711 ) ) ;
#29518=CARTESIAN_POINT ( 'NONE',  ( 7.000000000000000000, -21.00000000000000000, -4.000000000000000000 ) ) ;
#29525=LINE ( 'NONE', #41179, #67265 ) ;
#29542=EDGE_CURVE ( 'NONE', #61891, #15754, #62394, .T. ) ;
#29558=FACE_OUTER_BOUND ( 'NONE', #15121, .T. ) ;
#29567=CARTESIAN_POINT ( 'NONE',  ( 10.62249899919925866, -21.00000000000000000, -17.50000000000000000 ) ) ;
#29640=VECTOR ( 'NONE', #7227, 1000.000000000000000 ) ;
#29670=CARTESIAN_POINT ( 'NONE',  ( 275.0000000000000000, -37.14999999999894698, 8.200000000002349410 ) ) ;
#29671=LINE ( 'NONE', #19420, #24776 ) ;
#29672=CARTESIAN_POINT ( 'NONE',  ( 289.4999999999998863, -42.00000000000004263, 26.99999999999991829 ) ) ;
#29673=CARTESIAN_POINT ( 'NONE',  ( 7.000000000000000000, -39.79999999999954952, 8.900000000000419575 ) ) ;
#29679=EDGE_CURVE ( 'NONE', #22100, #64136, #32397, .T. ) ;
#29682=CARTESIAN_POINT ( 'NONE',  ( 7.000000000000000000, -21.00000000000000000, 0.000000000000000000 ) ) ;
#29686=DIRECTION ( 'NONE',  ( -1.000000000000000000, 0.000000000000000000, 0.000000000000000000 ) ) ;
#29694=EDGE_CURVE ( 'NONE', #38093, #20252, #69521, .T. ) ;
#29714=DIRECTION ( 'NONE',  ( 1.000000000000000000, 0.000000000000000000, 0.000000000000000000 ) ) ;
#29718=CIRCLE ( 'NONE', #24119, 0.5000000000009302559 ) ;
#29719=EDGE_LOOP ( 'NONE', ( #24629, #56613, #53750, #4329 ) ) ;
#29731=VERTEX_POINT ( 'NONE', #42647 ) ;
#29737=VERTEX_POINT ( 'NONE', #58916 ) ;
#29750=DIRECTION ( 'NONE',  ( 0.5773502691896216232, 0.5773502691896359451, 0.5773502691896197359 ) ) ;
#29751=EDGE_CURVE ( 'NONE', #37106, #47930, #64229, .T. ) ;
#29768=ADVANCED_FACE ( 'NONE', ( #15081 ), #48651, .T. ) ;
#29769=EDGE_LOOP ( 'NONE', ( #44464, #56290, #12024, #55207 ) ) ;
#29785=EDGE_LOOP ( 'NONE', ( #30680, #34360, #28296, #10702, #47180, #23482 ) ) ;
#29813=ADVANCED_FACE ( 'NONE', ( #23152 ), #44711, .T. ) ;
#29830=ORIENTED_EDGE ( 'NONE', *, *, #12216, .F. ) ;
#29839=ORIENTED_EDGE ( 'NONE', *, *, #57743, .F. ) ;
#29855=ADVANCED_FACE ( 'NONE', ( #17504 ), #39073, .F. ) ;
#29875=EDGE_CURVE ( 'NONE', #42019, #15647, #55683, .T. ) ;
#29889=VERTEX_POINT ( 'NONE', #28453 ) ;
#29891=CARTESIAN_POINT ( 'NONE',  ( 277.3542486889354564, -25.50000000000000355, -17.00000000000000000 ) ) ;
#29916=ORIENTED_EDGE ( 'NONE', *, *, #10705, .F. ) ;
#29930=CARTESIAN_POINT ( 'NONE',  ( 7.500000000000000000, -20.40000000000000213, -16.00000000000000000 ) ) ;
#29945=CARTESIAN_POINT ( 'NONE',  ( 283.0000000000000568, -38.15000000000000568, -14.50000000000000000 ) ) ;
#29952=CARTESIAN_POINT ( 'NONE',  ( 280.0000000000000000, -20.40000000000000213, -20.00000000000000000 ) ) ;
#29962=AXIS2_PLACEMENT_3D ( 'NONE', #51207, #14449, #35999 ) ;
#29975=CARTESIAN_POINT ( 'NONE',  ( 283.0000000000000568, -32.45000000000000995, -15.00000000000000000 ) ) ;
#29983=EDGE_CURVE ( 'NONE', #33386, #60663, #29155, .T. ) ;
#29993=EDGE_CURVE ( 'NONE', #28935, #39720, #68105, .T. ) ;
#29995=DIRECTION ( 'NONE',  ( 0.000000000000000000, 1.000000000000000000, 0.000000000000000000 ) ) ;
#29999=DIRECTION ( 'NONE',  ( -0.000000000000000000, -1.000000000000000000, -0.000000000000000000 ) ) ;
#30008=VECTOR ( 'NONE', #19684, 1000.000000000000114 ) ;
#30014=CARTESIAN_POINT ( 'NONE',  ( 282.8893988437589542, -20.72883876573682826, 17.22883876573683182 ) ) ;
#30022=LINE ( 'NONE', #20468, #47678 ) ;
#30028=LINE ( 'NONE', #13417, #12028 ) ;
#30030=DIRECTION ( 'NONE',  ( -1.000000000000000000, 0.000000000000000000, 0.000000000000000000 ) ) ;
#30039=CYLINDRICAL_SURFACE ( 'NONE', #13772, 0.2500000000000002220 ) ;
#30043=DIRECTION ( 'NONE',  ( 0.000000000000000000, -0.7051282051282045105, 0.7090798363602486276 ) ) ;
#30053=ORIENTED_EDGE ( 'NONE', *, *, #65116, .F. ) ;
#30056=LINE ( 'NONE', #51635, #61909 ) ;
#30084=CIRCLE ( 'NONE', #38030, 1.999999999999315436 ) ;
#30085=DIRECTION ( 'NONE',  ( -1.000000000000000000, 0.000000000000000000, 0.000000000000000000 ) ) ;
#30098=ORIENTED_EDGE ( 'NONE', *, *, #17234, .T. ) ;
#30100=CARTESIAN_POINT ( 'NONE',  ( 275.0000000000000000, -39.79999999999905214, -12.19999999999906315 ) ) ;
#30117=ORIENTED_EDGE ( 'NONE', *, *, #69497, .T. ) ;
#30118=AXIS2_PLACEMENT_3D ( 'NONE', #37422, #58979, #10193 ) ;
#30123=CARTESIAN_POINT ( 'NONE',  ( 14.50000000000000000, 0.000000000000000000, -26.50000000000000000 ) ) ;
#30129=ORIENTED_EDGE ( 'NONE', *, *, #69006, .F. ) ;
#30130=FACE_OUTER_BOUND ( 'NONE', #61812, .T. ) ;
#30138=CIRCLE ( 'NONE', #52729, 3.999999999999993339 ) ;
#30145=DIRECTION ( 'NONE',  ( -1.000000000000000000, 0.000000000000000000, 0.000000000000000000 ) ) ;
#30152=VERTEX_POINT ( 'NONE', #18072 ) ;
#30155=CARTESIAN_POINT ( 'NONE',  ( 283.0000000000000568, -23.29603921945599865, 12.50000000000000000 ) ) ;
#30171=LINE ( 'NONE', #67651, #56909 ) ;
#30187=EDGE_CURVE ( 'NONE', #31998, #21817, #43914, .T. ) ;
#30193=PLANE ( 'NONE',  #30712 ) ;
#30194=PLANE ( 'NONE',  #7643 ) ;
#30196=LINE ( 'NONE', #51766, #12057 ) ;
#30211=DIRECTION ( 'NONE',  ( 1.000000000000000000, 0.000000000000000000, 0.000000000000000000 ) ) ;
#30212=EDGE_CURVE ( 'NONE', #32551, #14268, #20096, .T. ) ;
#30229=PLANE ( 'NONE',  #46267 ) ;
#30235=CARTESIAN_POINT ( 'NONE',  ( 10.14575131106465378, -25.50000000000000355, -17.00000000000000000 ) ) ;
#30236=VECTOR ( 'NONE', #58959, 1000.000000000000000 ) ;
#30288=DIRECTION ( 'NONE',  ( 0.000000000000000000, -1.000000000000000000, 0.000000000000000000 ) ) ;
#30291=PLANE ( 'NONE',  #10997 ) ;
#30301=FACE_OUTER_BOUND ( 'NONE', #41410, .T. ) ;
#30303=EDGE_CURVE ( 'NONE', #21925, #24235, #37413, .T. ) ;
#30304=DIRECTION ( 'NONE',  ( -0.7071067811865485719, -0.7071067811865465735, 0.000000000000000000 ) ) ;
#30314=DIRECTION ( 'NONE',  ( 0.000000000000000000, -1.000000000000000000, 0.000000000000000000 ) ) ;
#30330=ORIENTED_EDGE ( 'NONE', *, *, #35433, .T. ) ;
#30334=ORIENTED_EDGE ( 'NONE', *, *, #53970, .T. ) ;
#30343=PLANE ( 'NONE',  #27067 ) ;
#30370=DIRECTION ( 'NONE',  ( 0.000000000000000000, -0.7071067811865474617, 0.7071067811865474617 ) ) ;
#30394=CARTESIAN_POINT ( 'NONE',  ( 275.0000000000000000, -37.14999999999894698, -8.200000000002349410 ) ) ;
#30410=ORIENTED_EDGE ( 'NONE', *, *, #56597, .F. ) ;
#30417=CARTESIAN_POINT ( 'NONE',  ( 283.0000000000000568, -25.50000000000000355, -14.74860679774999994 ) ) ;
#30422=ADVANCED_FACE ( 'NONE', ( #60338 ), #43750, .T. ) ;
#30424=CARTESIAN_POINT ( 'NONE',  ( 275.0000000000000000, -25.60000000000000142, -15.10000000000000142 ) ) ;
#30467=VECTOR ( 'NONE', #29176, 1000.000000000000000 ) ;
#30492=VECTOR ( 'NONE', #4455, 1000.000000000000000 ) ;
#30516=VECTOR ( 'NONE', #31169, 1000.000000000000000 ) ;
#30520=AXIS2_PLACEMENT_3D ( 'NONE', #37372, #5193, #37716 ) ;
#30525=VERTEX_POINT ( 'NONE', #6308 ) ;
#30532=EDGE_LOOP ( 'NONE', ( #1146, #17042, #22934, #14889 ) ) ;
#30534=PLANE ( 'NONE',  #32755 ) ;
#30557=DIRECTION ( 'NONE',  ( 0.000000000000000000, 0.000000000000000000, -1.000000000000000000 ) ) ;
#30571=CARTESIAN_POINT ( 'NONE',  ( 0.5000000000000000000, -42.50000000000000000, 26.50000000000000000 ) ) ;
#30595=DIRECTION ( 'NONE',  ( 1.000000000000000000, -0.000000000000000000, -0.000000000000000000 ) ) ;
#30607=ORIENTED_EDGE ( 'NONE', *, *, #18627, .T. ) ;
#30610=LINE ( 'NONE', #47572, #15865 ) ;
#30614=ORIENTED_EDGE ( 'NONE', *, *, #18267, .T. ) ;
#30616=EDGE_CURVE ( 'NONE', #67044, #56517, #37797, .T. ) ;
#30658=CARTESIAN_POINT ( 'NONE',  ( 7.000000000000000000, -23.65000000000000568, -12.40000000000000213 ) ) ;
#30661=VERTEX_POINT ( 'NONE', #2037 ) ;
#30670=DIRECTION ( 'NONE',  ( 0.000000000000000000, -0.6787500000000000755, 0.7343694148723789450 ) ) ;
#30674=CARTESIAN_POINT ( 'NONE',  ( 14.99999999999999822, -42.00000000000000000, -15.10000000000000142 ) ) ;
#30678=ADVANCED_FACE ( 'NONE', ( #7321 ), #46207, .F. ) ;
#30680=ORIENTED_EDGE ( 'NONE', *, *, #45695, .T. ) ;
#30690=VERTEX_POINT ( 'NONE', #67078 ) ;
#30699=CARTESIAN_POINT ( 'NONE',  ( 283.0000000000000568, -32.44999999999905071, 12.69999999999999929 ) ) ;
#30703=ORIENTED_EDGE ( 'NONE', *, *, #2086, .F. ) ;
#30710=LINE ( 'NONE', #19044, #39308 ) ;
#30712=AXIS2_PLACEMENT_3D ( 'NONE', #46447, #68022, #35130 ) ;
#30721=ORIENTED_EDGE ( 'NONE', *, *, #7562, .F. ) ;
#30732=LINE ( 'NONE', #52300, #43003 ) ;
#30733=DIRECTION ( 'NONE',  ( 0.000000000000000000, 1.000000000000000000, 0.000000000000000000 ) ) ;
#30741=CARTESIAN_POINT ( 'NONE',  ( 283.0000000000000568, -25.00000000000000000, 17.50000000000000000 ) ) ;
#30765=DIRECTION ( 'NONE',  ( 0.000000000000000000, 0.000000000000000000, 1.000000000000000000 ) ) ;
#30787=VECTOR ( 'NONE', #8586, 1000.000000000000114 ) ;
#30808=ORIENTED_EDGE ( 'NONE', *, *, #1680, .T. ) ;
#30825=VECTOR ( 'NONE', #59051, 1000.000000000000000 ) ;
#30845=DIRECTION ( 'NONE',  ( 0.000000000000000000, 0.000000000000000000, 1.000000000000000000 ) ) ;
#30862=CARTESIAN_POINT ( 'NONE',  ( 283.0000000000000568, -42.00000000000000000, 7.000000000000000000 ) ) ;
#30874=ORIENTED_EDGE ( 'NONE', *, *, #31873, .F. ) ;
#30890=ORIENTED_EDGE ( 'NONE', *, *, #20555, .F. ) ;
#30896=EDGE_LOOP ( 'NONE', ( #193, #30703, #22458, #63580 ) ) ;
#30920=DIRECTION ( 'NONE',  ( 0.000000000000000000, -0.7075259945834421194, -0.7066873191084661610 ) ) ;
#30922=CARTESIAN_POINT ( 'NONE',  ( 7.000000000000000000, -25.93000000000544958, 9.412893218815410634 ) ) ;
#30945=CARTESIAN_POINT ( 'NONE',  ( 283.0000000000000568, -38.09999999999885034, -8.400000000000000355 ) ) ;
#30963=ORIENTED_EDGE ( 'NONE', *, *, #16806, .T. ) ;
#30973=DIRECTION ( 'NONE',  ( 1.000000000000000000, 0.000000000000000000, 0.000000000000000000 ) ) ;
#30980=EDGE_CURVE ( 'NONE', #13668, #53236, #57856, .T. ) ;
#31008=LINE ( 'NONE', #14750, #54713 ) ;
#31011=CARTESIAN_POINT ( 'NONE',  ( 7.000000000000000000, -42.50000000000000000, -15.10000000000000142 ) ) ;
#31013=CARTESIAN_POINT ( 'NONE',  ( 14.75000000000000533, -42.25000000000000000, -26.74999999999999645 ) ) ;
#31015=ADVANCED_FACE ( 'NONE', ( #38075 ), #27097, .F. ) ;
#31022=VERTEX_POINT ( 'NONE', #231 ) ;
#31023=VECTOR ( 'NONE', #53394, 1000.000000000000000 ) ;
#31034=ORIENTED_EDGE ( 'NONE', *, *, #48808, .T. ) ;
#31068=EDGE_CURVE ( 'NONE', #2050, #26250, #20612, .T. ) ;
#31081=LINE ( 'NONE', #42033, #27351 ) ;
#31098=AXIS2_PLACEMENT_3D ( 'NONE', #5954, #27521, #6640 ) ;
#31105=AXIS2_PLACEMENT_3D ( 'NONE', #15136, #53668, #25757 ) ;
#31110=LINE ( 'NONE', #42052, #45289 ) ;
#31111=ORIENTED_EDGE ( 'NONE', *, *, #47362, .F. ) ;
#31114=AXIS2_PLACEMENT_3D ( 'NONE', #42167, #36890, #57387 ) ;
#31124=ORIENTED_EDGE ( 'NONE', *, *, #39473, .F. ) ;
#31126=DIRECTION ( 'NONE',  ( -1.000000000000000000, 0.000000000000000000, 0.000000000000000000 ) ) ;
#31128=CARTESIAN_POINT ( 'NONE',  ( 7.000000000000000000, -38.65000000000095781, 13.20000000000094253 ) ) ;
#31140=CARTESIAN_POINT ( 'NONE',  ( 283.0000000000000568, -32.46196062927499781, -8.091291340630698770 ) ) ;
#31142=DIRECTION ( 'NONE',  ( 0.000000000000000000, 0.000000000000000000, -1.000000000000000000 ) ) ;
#31146=AXIS2_PLACEMENT_3D ( 'NONE', #55456, #33187, #47456 ) ;
#31151=VECTOR ( 'NONE', #51049, 1000.000000000000000 ) ;
#31154=LINE ( 'NONE', #9576, #53042 ) ;
#31169=DIRECTION ( 'NONE',  ( 0.000000000000000000, 0.000000000000000000, 1.000000000000000000 ) ) ;
#31186=DIRECTION ( 'NONE',  ( -1.000000000000000000, 0.000000000000000000, 0.000000000000000000 ) ) ;
#31208=VERTEX_POINT ( 'NONE', #25636 ) ;
#31223=VERTEX_POINT ( 'NONE', #47200 ) ;
#31248=AXIS2_PLACEMENT_3D ( 'NONE', #65555, #17110, #53921 ) ;
#31254=ORIENTED_EDGE ( 'NONE', *, *, #38043, .T. ) ;
#31265=AXIS2_PLACEMENT_3D ( 'NONE', #5247, #27152, #42713 ) ;
#31266=CARTESIAN_POINT ( 'NONE',  ( 7.000000000000000000, -53.81370849898476649, 16.03137303340311348 ) ) ;
#31267=EDGE_CURVE ( 'NONE', #26713, #53236, #25272, .T. ) ;
#31269=DIRECTION ( 'NONE',  ( 0.5773502691896230665, -0.5773502691896230665, 0.5773502691896311712 ) ) ;
#31271=ORIENTED_EDGE ( 'NONE', *, *, #2333, .T. ) ;
#31272=AXIS2_PLACEMENT_3D ( 'NONE', #49171, #59435, #5360 ) ;
#31275=CARTESIAN_POINT ( 'NONE',  ( 7.000000000000000000, -27.13000000000000611, 13.50000000000000000 ) ) ;
#31298=LINE ( 'NONE', #52867, #48255 ) ;
#31308=DIRECTION ( 'NONE',  ( 0.000000000000000000, -0.6801302850037772574, -0.7330912599538208507 ) ) ;
#31310=ORIENTED_EDGE ( 'NONE', *, *, #26777, .T. ) ;
#31314=VECTOR ( 'NONE', #43322, 1000.000000000000000 ) ;
#31334=ORIENTED_EDGE ( 'NONE', *, *, #14962, .F. ) ;
#31343=LINE ( 'NONE', #57137, #57068 ) ;
#31347=EDGE_CURVE ( 'NONE', #43188, #61781, #6501, .T. ) ;
#31355=LINE ( 'NONE', #20717, #7802 ) ;
#31377=CARTESIAN_POINT ( 'NONE',  ( 283.0000000000000568, -32.45000000000000995, 12.69999999999999929 ) ) ;
#31396=FACE_OUTER_BOUND ( 'NONE', #35994, .T. ) ;
#31397=ORIENTED_EDGE ( 'NONE', *, *, #42251, .T. ) ;
#31407=DIRECTION ( 'NONE',  ( 0.000000000000000000, 0.7071067811865875408, -0.7071067811865076047 ) ) ;
#31415=VERTEX_POINT ( 'NONE', #44302 ) ;
#31435=CARTESIAN_POINT ( 'NONE',  ( 283.0000000000000568, -26.79000000000000625, 0.000000000000000000 ) ) ;
#31443=FACE_OUTER_BOUND ( 'NONE', #44338, .T. ) ;
#31448=FACE_OUTER_BOUND ( 'NONE', #38592, .T. ) ;
#31452=ORIENTED_EDGE ( 'NONE', *, *, #39135, .F. ) ;
#31477=ORIENTED_EDGE ( 'NONE', *, *, #33147, .T. ) ;
#31492=ORIENTED_EDGE ( 'NONE', *, *, #62654, .T. ) ;
#31495=LINE ( 'NONE', #58371, #62674 ) ;
#31501=ADVANCED_FACE ( 'NONE', ( #61248 ), #46055, .T. ) ;
#31515=EDGE_CURVE ( 'NONE', #29091, #23661, #39353, .T. ) ;
#31521=CARTESIAN_POINT ( 'NONE',  ( 283.0000000000000568, -25.50000000000000355, 14.74860679774999994 ) ) ;
#31535=PLANE ( 'NONE',  #47388 ) ;
#31541=ORIENTED_EDGE ( 'NONE', *, *, #36742, .T. ) ;
#31554=ORIENTED_EDGE ( 'NONE', *, *, #51989, .F. ) ;
#31573=ADVANCED_FACE ( 'NONE', ( #3270 ), #57363, .T. ) ;
#31612=CARTESIAN_POINT ( 'NONE',  ( 7.000000000000000000, -26.42999999999999972, -5.874955318979029784 ) ) ;
#31618=CARTESIAN_POINT ( 'NONE',  ( 275.0000000000000000, -26.42999999999999972, -9.412893218813501051 ) ) ;
#31630=EDGE_CURVE ( 'NONE', #31998, #11694, #13945, .T. ) ;
#31632=ORIENTED_EDGE ( 'NONE', *, *, #6499, .F. ) ;
#31644=ADVANCED_FACE ( 'NONE', ( #36493 ), #3628, .F. ) ;
#31648=EDGE_CURVE ( 'NONE', #37548, #62567, #15288, .T. ) ;
#31672=ORIENTED_EDGE ( 'NONE', *, *, #33890, .F. ) ;
#31676=ORIENTED_EDGE ( 'NONE', *, *, #25495, .F. ) ;
#31677=ORIENTED_EDGE ( 'NONE', *, *, #63584, .T. ) ;
#31682=DIRECTION ( 'NONE',  ( 1.000000000000000000, -0.000000000000000000, -0.000000000000000000 ) ) ;
#31685=EDGE_CURVE ( 'NONE', #41344, #17425, #48942, .T. ) ;
#31688=DIRECTION ( 'NONE',  ( 1.000000000000000000, -0.000000000000000000, -0.000000000000000000 ) ) ;
#31697=AXIS2_PLACEMENT_3D ( 'NONE', #30100, #51680, #57325 ) ;
#31705=CARTESIAN_POINT ( 'NONE',  ( 7.000000000000000000, -26.50000000000000000, -5.809475019311129529 ) ) ;
#31716=DIRECTION ( 'NONE',  ( 1.000000000000000000, 0.000000000000000000, 0.000000000000000000 ) ) ;
#31721=ORIENTED_EDGE ( 'NONE', *, *, #66181, .F. ) ;
#31734=VECTOR ( 'NONE', #4200, 1000.000000000000000 ) ;
#31736=ORIENTED_EDGE ( 'NONE', *, *, #14348, .F. ) ;
#31741=VERTEX_POINT ( 'NONE', #17022 ) ;
#31745=ORIENTED_EDGE ( 'NONE', *, *, #36428, .T. ) ;
#31752=ORIENTED_EDGE ( 'NONE', *, *, #62051, .T. ) ;
#31769=VERTEX_POINT ( 'NONE', #27981 ) ;
#31795=CARTESIAN_POINT ( 'NONE',  ( 7.000000000000000000, -39.79999999999905214, -12.19999999999906315 ) ) ;
#31797=PLANE ( 'NONE',  #51493 ) ;
#31817=CARTESIAN_POINT ( 'NONE',  ( 275.2500000000001137, -0.2499999999999431288, -26.74999999999993250 ) ) ;
#31827=EDGE_CURVE ( 'NONE', #23661, #32632, #54172, .T. ) ;
#31829=DIRECTION ( 'NONE',  ( 0.000000000000000000, -0.7071067811865077157, 0.7071067811865873187 ) ) ;
#31831=EDGE_CURVE ( 'NONE', #56310, #69782, #24083, .T. ) ;
#31834=EDGE_CURVE ( 'NONE', #32632, #12243, #65465, .T. ) ;
#31838=DIRECTION ( 'NONE',  ( 1.000000000000000000, 0.000000000000000000, 0.000000000000000000 ) ) ;
#31850=VECTOR ( 'NONE', #41060, 1000.000000000000114 ) ;
#31851=DIRECTION ( 'NONE',  ( 0.000000000000000000, 0.000000000000000000, -1.000000000000000000 ) ) ;
#31856=ORIENTED_EDGE ( 'NONE', *, *, #38043, .F. ) ;
#31861=LINE ( 'NONE', #37169, #25613 ) ;
#31873=EDGE_CURVE ( 'NONE', #42019, #42376, #51185, .T. ) ;
#31885=FILL_AREA_STYLE_COLOUR ( '', #12018 ) ;
#31889=FACE_OUTER_BOUND ( 'NONE', #27050, .T. ) ;
#31905=VECTOR ( 'NONE', #28080, 1000.000000000000000 ) ;
#31916=FACE_OUTER_BOUND ( 'NONE', #12385, .T. ) ;
#31924=ORIENTED_EDGE ( 'NONE', *, *, #586, .T. ) ;
#31967=VECTOR ( 'NONE', #40828, 1000.000000000000114 ) ;
#31975=DIRECTION ( 'NONE',  ( 0.000000000000000000, 1.000000000000000000, 0.000000000000000000 ) ) ;
#31976=VECTOR ( 'NONE', #33924, 1000.000000000000114 ) ;
#31977=EDGE_CURVE ( 'NONE', #46313, #38349, #50232, .T. ) ;
#31993=DIRECTION ( 'NONE',  ( 0.000000000000000000, 0.000000000000000000, 1.000000000000000000 ) ) ;
#31998=VERTEX_POINT ( 'NONE', #69199 ) ;
#32014=ORIENTED_EDGE ( 'NONE', *, *, #53981, .F. ) ;
#32021=VERTEX_POINT ( 'NONE', #52954 ) ;
#32033=ORIENTED_EDGE ( 'NONE', *, *, #35561, .F. ) ;
#32035=AXIS2_PLACEMENT_3D ( 'NONE', #64428, #26589, #10330 ) ;
#32037=EDGE_CURVE ( 'NONE', #6255, #32021, #63171, .T. ) ;
#32043=DIRECTION ( 'NONE',  ( 0.000000000000000000, -1.000000000000000000, 0.000000000000000000 ) ) ;
#32045=CARTESIAN_POINT ( 'NONE',  ( 283.0000000000000568, -42.00000000000000000, 7.000000000000000000 ) ) ;
#32052=ORIENTED_EDGE ( 'NONE', *, *, #6499, .T. ) ;
#32059=VECTOR ( 'NONE', #40460, 1000.000000000000000 ) ;
#32063=CARTESIAN_POINT ( 'NONE',  ( 0.000000000000000000, -42.00000000000000000, 26.50000000000000000 ) ) ;
#32065=CARTESIAN_POINT ( 'NONE',  ( 7.500000000000000000, -53.81370849898476649, -20.00000000000000000 ) ) ;
#32072=CARTESIAN_POINT ( 'NONE',  ( 7.000000000000000000, -32.94999999999885176, -8.199999999997979572 ) ) ;
#32083=ORIENTED_EDGE ( 'NONE', *, *, #38066, .F. ) ;
#32092=CARTESIAN_POINT ( 'NONE',  ( 275.2500000000001137, -42.24999999999992184, 26.75000000000003197 ) ) ;
#32093=VERTEX_POINT ( 'NONE', #64255 ) ;
#32095=ORIENTED_EDGE ( 'NONE', *, *, #12897, .T. ) ;
#32128=CARTESIAN_POINT ( 'NONE',  ( 275.5000000000000000, -0.5000000000000000000, -27.00000000000000000 ) ) ;
#32129=LINE ( 'NONE', #69621, #3695 ) ;
#32141=ORIENTED_EDGE ( 'NONE', *, *, #39388, .F. ) ;
#32158=DIRECTION ( 'NONE',  ( 0.000000000000000000, -1.000000000000000000, 3.819861094142539476E-12 ) ) ;
#32163=VECTOR ( 'NONE', #65896, 1000.000000000000000 ) ;
#32169=ORIENTED_EDGE ( 'NONE', *, *, #58976, .T. ) ;
#32176=AXIS2_PLACEMENT_3D ( 'NONE', #22942, #51201, #39539 ) ;
#32188=AXIS2_PLACEMENT_3D ( 'NONE', #65386, #59383, #65041 ) ;
#32199=VECTOR ( 'NONE', #15963, 1000.000000000000000 ) ;
#32207=PLANE ( 'NONE',  #26696 ) ;
#32247=CARTESIAN_POINT ( 'NONE',  ( 283.0000000000000568, -53.81370849898476649, 17.35424868893542438 ) ) ;
#32250=AXIS2_PLACEMENT_3D ( 'NONE', #25683, #31682, #53254 ) ;
#32254=CYLINDRICAL_SURFACE ( 'NONE', #26412, 0.5000000000009441337 ) ;
#32263=CARTESIAN_POINT ( 'NONE',  ( 283.0000000000000568, -38.15000000000000568, 13.19999999999999929 ) ) ;
#32277=CIRCLE ( 'NONE', #1768, 0.5000000000009441337 ) ;
#32302=DIRECTION ( 'NONE',  ( -0.000000000000000000, -1.000000000000000000, -0.000000000000000000 ) ) ;
#32305=VERTEX_POINT ( 'NONE', #57105 ) ;
#32316=AXIS2_PLACEMENT_3D ( 'NONE', #44938, #29714, #41024 ) ;
#32326=CARTESIAN_POINT ( 'NONE',  ( 283.0000000000000568, -41.99999999999906208, 14.49999999999903899 ) ) ;
#32355=DIRECTION ( 'NONE',  ( 1.000000000000000000, 0.000000000000000000, 0.000000000000000000 ) ) ;
#32357=VECTOR ( 'NONE', #69323, 1000.000000000000000 ) ;
#32358=ORIENTED_EDGE ( 'NONE', *, *, #31831, .T. ) ;
#32361=EDGE_CURVE ( 'NONE', #47818, #57661, #13620, .T. ) ;
#32383=LINE ( 'NONE', #22112, #12093 ) ;
#32388=CARTESIAN_POINT ( 'NONE',  ( 275.0000000000000000, -26.28355339059299922, 9.766446609406699508 ) ) ;
#32396=CARTESIAN_POINT ( 'NONE',  ( 275.5000000000000000, -0.5000000000000000000, 27.00000000000000000 ) ) ;
#32397=LINE ( 'NONE', #31705, #25169 ) ;
#32400=VECTOR ( 'NONE', #53004, 1000.000000000000000 ) ;
#32405=CARTESIAN_POINT ( 'NONE',  ( 7.000000000000000000, -23.65000000000000568, 12.40000000000000213 ) ) ;
#32433=CARTESIAN_POINT ( 'NONE',  ( 275.0000000000000000, -42.00000000000000000, -7.000000000000000000 ) ) ;
#32435=ORIENTED_EDGE ( 'NONE', *, *, #45677, .T. ) ;
#32468=VECTOR ( 'NONE', #32043, 1000.000000000000000 ) ;
#32472=DIRECTION ( 'NONE',  ( -1.000000000000000000, 0.000000000000000000, 0.000000000000000000 ) ) ;
#32487=DIRECTION ( 'NONE',  ( 1.000000000000000000, 0.000000000000000000, 0.000000000000000000 ) ) ;
#32507=AXIS2_PLACEMENT_3D ( 'NONE', #12042, #11362, #54515 ) ;
#32525=DIRECTION ( 'NONE',  ( -1.000000000000000000, 0.000000000000000000, 0.000000000000000000 ) ) ;
#32536=LINE ( 'NONE', #54781, #12898 ) ;
#32537=ADVANCED_FACE ( 'NONE', ( #14675 ), #37998, .F. ) ;
#32543=EDGE_LOOP ( 'NONE', ( #32550, #26544, #47248, #2677, #2143, #60706 ) ) ;
#32546=ORIENTED_EDGE ( 'NONE', *, *, #50132, .F. ) ;
#32550=ORIENTED_EDGE ( 'NONE', *, *, #69725, .F. ) ;
#32551=VERTEX_POINT ( 'NONE', #65887 ) ;
#32564=CARTESIAN_POINT ( 'NONE',  ( 7.000000000000000000, -21.00000000000000000, 12.50000000000000000 ) ) ;
#32577=DIRECTION ( 'NONE',  ( 0.000000000000000000, -1.000000000000000000, 0.000000000000000000 ) ) ;
#32582=CARTESIAN_POINT ( 'NONE',  ( 7.000000000000000000, -32.46196062927499781, 8.091291340630698770 ) ) ;
#32593=EDGE_CURVE ( 'NONE', #27615, #8637, #18033, .T. ) ;
#32599=CARTESIAN_POINT ( 'NONE',  ( 283.0000000000000568, -20.40000000000000213, 12.40000000000000213 ) ) ;
#32606=CARTESIAN_POINT ( 'NONE',  ( 275.0000000000000000, -25.00000000000000000, -17.50000000000000000 ) ) ;
#32623=LINE ( 'NONE', #59490, #28801 ) ;
#32632=VERTEX_POINT ( 'NONE', #54261 ) ;
#32639=ADVANCED_FACE ( 'NONE', ( #22428 ), #28400, .F. ) ;
#32653=VERTEX_POINT ( 'NONE', #6831 ) ;
#32657=DIRECTION ( 'NONE',  ( 0.000000000000000000, 0.000000000000000000, -1.000000000000000000 ) ) ;
#32661=CIRCLE ( 'NONE', #19123, 3.999999999999993339 ) ;
#32664=VECTOR ( 'NONE', #35567, 1000.000000000000000 ) ;
#32690=ORIENTED_EDGE ( 'NONE', *, *, #3138, .F. ) ;
#32695=EDGE_CURVE ( 'NONE', #63351, #61661, #44655, .T. ) ;
#32704=CARTESIAN_POINT ( 'NONE',  ( 283.0000000000000568, -20.50000000000000000, 17.00000000000000000 ) ) ;
#32706=EDGE_LOOP ( 'NONE', ( #30963, #2860, #51831, #46809 ) ) ;
#32708=VECTOR ( 'NONE', #48417, 1000.000000000000000 ) ;
#32712=EDGE_LOOP ( 'NONE', ( #64289, #15818, #45365, #53179, #54777, #65473, #49328 ) ) ;
#32739=ORIENTED_EDGE ( 'NONE', *, *, #41037, .T. ) ;
#32744=FACE_OUTER_BOUND ( 'NONE', #18976, .T. ) ;
#32751=VECTOR ( 'NONE', #19346, 1000.000000000000000 ) ;
#32755=AXIS2_PLACEMENT_3D ( 'NONE', #52104, #68369, #63062 ) ;
#32763=AXIS2_PLACEMENT_3D ( 'NONE', #33675, #7488, #49262 ) ;
#32780=CARTESIAN_POINT ( 'NONE',  ( 7.000000000000000000, -20.50000000000000000, 13.00000000000000178 ) ) ;
#32782=ORIENTED_EDGE ( 'NONE', *, *, #53853, .F. ) ;
#32812=LINE ( 'NONE', #4568, #20573 ) ;
#32813=EDGE_CURVE ( 'NONE', #41344, #29414, #8227, .T. ) ;
#32848=ORIENTED_EDGE ( 'NONE', *, *, #48918, .T. ) ;
#32854=AXIS2_PLACEMENT_3D ( 'NONE', #64685, #59039, #27220 ) ;
#32916=DIRECTION ( 'NONE',  ( 0.000000000000000000, 0.000000000000000000, -1.000000000000000000 ) ) ;
#32922=DIRECTION ( 'NONE',  ( -0.7071067811865470176, 0.7071067811865480168, 0.000000000000000000 ) ) ;
#32930=LINE ( 'NONE', #54167, #28257 ) ;
#32939=AXIS2_PLACEMENT_3D ( 'NONE', #65090, #69704, #48475 ) ;
#32940=DIRECTION ( 'NONE',  ( 0.000000000000000000, -0.7071067811865475727, 0.7071067811865475727 ) ) ;
#32941=EDGE_CURVE ( 'NONE', #8558, #57661, #15300, .T. ) ;
#32968=VECTOR ( 'NONE', #46380, 1000.000000000000000 ) ;
#32971=FACE_BOUND ( 'NONE', #42004, .T. ) ;
#32976=ORIENTED_EDGE ( 'NONE', *, *, #56602, .T. ) ;
#32977=ADVANCED_FACE ( 'NONE', ( #31916 ), #32254, .T. ) ;
#32981=ORIENTED_EDGE ( 'NONE', *, *, #2478, .F. ) ;
#32982=EDGE_LOOP ( 'NONE', ( #11193, #54583, #62073, #59867 ) ) ;
#33025=CARTESIAN_POINT ( 'NONE',  ( 275.0000000000000000, -39.80000000000000426, -8.400000000000000355 ) ) ;
#33049=ORIENTED_EDGE ( 'NONE', *, *, #52684, .T. ) ;
#33051=VERTEX_POINT ( 'NONE', #21302 ) ;
#33052=DIRECTION ( 'NONE',  ( -0.5773502691896257311, -0.5773502691896257311, -0.5773502691896257311 ) ) ;
#33077=DIRECTION ( 'NONE',  ( -1.000000000000000000, 0.000000000000000000, 0.000000000000000000 ) ) ;
#33092=CARTESIAN_POINT ( 'NONE',  ( 282.8893988437589542, -20.72883876573683182, -17.22883876573683182 ) ) ;
#33106=VECTOR ( 'NONE', #3704, 1000.000000000000000 ) ;
#33117=CARTESIAN_POINT ( 'NONE',  ( 283.0000000000000568, -25.50000000000000355, -17.00000000000000000 ) ) ;
#33126=AXIS2_PLACEMENT_3D ( 'NONE', #16327, #37903, #59465 ) ;
#33140=FACE_BOUND ( 'NONE', #46910, .T. ) ;
#33147=EDGE_CURVE ( 'NONE', #66290, #13668, #29024, .T. ) ;
#33151=AXIS2_PLACEMENT_3D ( 'NONE', #16591, #38166, #53383 ) ;
#33152=CARTESIAN_POINT ( 'NONE',  ( 283.0000000000000568, -26.28355339059299922, -9.766446609406699508 ) ) ;
#33153=AXIS2_PLACEMENT_3D ( 'NONE', #47549, #52874, #31308 ) ;
#33158=DIRECTION ( 'NONE',  ( 0.000000000000000000, 0.000000000000000000, 1.000000000000000000 ) ) ;
#33187=DIRECTION ( 'NONE',  ( 1.000000000000000000, -0.000000000000000000, -0.000000000000000000 ) ) ;
#33199=ADVANCED_FACE ( 'NONE', ( #12059 ), #66498, .F. ) ;
#33203=DIRECTION ( 'NONE',  ( 0.000000000000000000, 0.000000000000000000, -1.000000000000000000 ) ) ;
#33227=ADVANCED_FACE ( 'NONE', ( #47039 ), #58365, .T. ) ;
#33237=ORIENTED_EDGE ( 'NONE', *, *, #44466, .F. ) ;
#33276=FACE_OUTER_BOUND ( 'NONE', #5432, .T. ) ;
#33279=ORIENTED_EDGE ( 'NONE', *, *, #35976, .T. ) ;
#33317=CIRCLE ( 'NONE', #5109, 0.5000000000009406920 ) ;
#33336=LINE ( 'NONE', #58830, #3571 ) ;
#33345=LINE ( 'NONE', #54577, #753 ) ;
#33360=DIRECTION ( 'NONE',  ( 0.000000000000000000, -1.887379141859195671E-12, 1.000000000000000000 ) ) ;
#33386=VERTEX_POINT ( 'NONE', #5658 ) ;
#33387=EDGE_CURVE ( 'NONE', #31415, #24890, #32536, .T. ) ;
#33401=CIRCLE ( 'NONE', #39041, 0.5000000000009302559 ) ;
#33439=VERTEX_POINT ( 'NONE', #344 ) ;
#33447=DIRECTION ( 'NONE',  ( -0.7071067811865475727, -0.7071067811865475727, 0.000000000000000000 ) ) ;
#33454=EDGE_CURVE ( 'NONE', #29737, #46983, #11286, .T. ) ;
#33479=ORIENTED_EDGE ( 'NONE', *, *, #57126, .F. ) ;
#33492=DIRECTION ( 'NONE',  ( 0.000000000000000000, 0.000000000000000000, 1.000000000000000000 ) ) ;
#33496=VECTOR ( 'NONE', #67084, 1000.000000000000000 ) ;
#33503=EDGE_CURVE ( 'NONE', #30661, #53553, #65733, .T. ) ;
#33513=CARTESIAN_POINT ( 'NONE',  ( 283.0000000000000568, -20.50000000000000000, -17.00000000000000000 ) ) ;
#33575=PLANE ( 'NONE',  #17267 ) ;
#33581=DIRECTION ( 'NONE',  ( -1.000000000000000000, 0.000000000000000000, 0.000000000000000000 ) ) ;
#33586=EDGE_LOOP ( 'NONE', ( #20924, #51988, #35192, #63845 ) ) ;
#33598=DIRECTION ( 'NONE',  ( 0.000000000000000000, 0.000000000000000000, 1.000000000000000000 ) ) ;
#33609=ORIENTED_EDGE ( 'NONE', *, *, #8092, .F. ) ;
#33643=DIRECTION ( 'NONE',  ( 1.000000000000000000, 0.000000000000000000, 0.000000000000000000 ) ) ;
#33645=DIRECTION ( 'NONE',  ( -0.4999999999999170108, 1.060575238724965586E-16, -0.8660254037844865582 ) ) ;
#33670=DIRECTION ( 'NONE',  ( 0.5773502691896291728, 0.5773502691896271743, 0.5773502691896209571 ) ) ;
#33675=CARTESIAN_POINT ( 'NONE',  ( 283.0000000000000568, -38.09999999999885034, -7.900000000002049383 ) ) ;
#33683=ADVANCED_FACE ( 'NONE', ( #40934 ), #63574, .F. ) ;
#33695=EDGE_CURVE ( 'NONE', #9319, #48333, #7298, .T. ) ;
#33699=CARTESIAN_POINT ( 'NONE',  ( 275.0000000000000000, -26.50000000000000000, 0.5000000000000000000 ) ) ;
#33701=EDGE_LOOP ( 'NONE', ( #49952, #18644, #14620, #14413, #61829, #3507, #40243, #21297, #47343 ) ) ;
#33703=DIRECTION ( 'NONE',  ( 0.000000000000000000, 0.7066873191085843997, 0.7075259945833241026 ) ) ;
#33704=ADVANCED_FACE ( 'NONE', ( #40591 ), #8402, .F. ) ;
#33709=DIRECTION ( 'NONE',  ( -1.000000000000000000, 0.000000000000000000, 0.000000000000000000 ) ) ;
#33711=EDGE_CURVE ( 'NONE', #29119, #18299, #62491, .T. ) ;
#33731=ORIENTED_EDGE ( 'NONE', *, *, #27702, .T. ) ;
#33743=DIRECTION ( 'NONE',  ( 0.000000000000000000, 0.000000000000000000, 1.000000000000000000 ) ) ;
#33744=CARTESIAN_POINT ( 'NONE',  ( 7.000000000000000000, -25.60000000000000142, 17.60000000000000142 ) ) ;
#33785=DIRECTION ( 'NONE',  ( 1.000000000000000000, -0.000000000000000000, -0.000000000000000000 ) ) ;
#33791=DIRECTION ( 'NONE',  ( 1.000000000000000000, -0.000000000000000000, -0.000000000000000000 ) ) ;
#33799=ORIENTED_EDGE ( 'NONE', *, *, #62799, .F. ) ;
#33803=CARTESIAN_POINT ( 'NONE',  ( 275.0000000000000000, -28.95000000000155183, -14.49999999999845990 ) ) ;
#33807=ORIENTED_EDGE ( 'NONE', *, *, #17685, .F. ) ;
#33812=EDGE_LOOP ( 'NONE', ( #49552, #26094, #25468, #9946, #52220 ) ) ;
#33818=LINE ( 'NONE', #55405, #42407 ) ;
#33823=CARTESIAN_POINT ( 'NONE',  ( 1.000000000000000000, -16.00000000000000000, 0.000000000000000000 ) ) ;
#33831=CARTESIAN_POINT ( 'NONE',  ( 280.0000000000000000, -53.81370849898476649, -16.00000000000000711 ) ) ;
#33842=LINE ( 'NONE', #50800, #55673 ) ;
#33846=EDGE_CURVE ( 'NONE', #45355, #9032, #52973, .T. ) ;
#33861=DIRECTION ( 'NONE',  ( 0.7071067811865460184, 0.000000000000000000, -0.7071067811865489050 ) ) ;
#33864=LINE ( 'NONE', #44129, #34300 ) ;
#33876=ORIENTED_EDGE ( 'NONE', *, *, #18941, .F. ) ;
#33882=FACE_OUTER_BOUND ( 'NONE', #4656, .T. ) ;
#33890=EDGE_CURVE ( 'NONE', #13397, #25678, #18609, .T. ) ;
#33894=DIRECTION ( 'NONE',  ( -1.000000000000000000, 0.000000000000000000, 0.000000000000000000 ) ) ;
#33911=DIRECTION ( 'NONE',  ( -1.000000000000000000, 0.000000000000000000, 0.000000000000000000 ) ) ;
#33913=CARTESIAN_POINT ( 'NONE',  ( 1.000000000000000000, -21.00000000000000000, 0.000000000000000000 ) ) ;
#33919=VERTEX_POINT ( 'NONE', #8592 ) ;
#33921=CARTESIAN_POINT ( 'NONE',  ( 290.0000000000000000, -42.00000000000000000, 50.00000000000000000 ) ) ;
#33923=CARTESIAN_POINT ( 'NONE',  ( 275.0000000000000000, -25.60000000000000142, 15.10000000000000142 ) ) ;
#33924=DIRECTION ( 'NONE',  ( 0.000000000000000000, 0.7071067811865074937, 0.7071067811865876518 ) ) ;
#33930=DIRECTION ( 'NONE',  ( 0.000000000000000000, 1.000000000000000000, 1.883909694907254982E-12 ) ) ;
#33933=VECTOR ( 'NONE', #10985, 1000.000000000000000 ) ;
#33952=CARTESIAN_POINT ( 'NONE',  ( 275.2500000000000000, -0.2500000000000000000, -26.75000000000000000 ) ) ;
#33977=ORIENTED_EDGE ( 'NONE', *, *, #11516, .F. ) ;
#33982=LINE ( 'NONE', #55568, #58000 ) ;
#33983=AXIS2_PLACEMENT_3D ( 'NONE', #38636, #64476, #59159 ) ;
#33993=ORIENTED_EDGE ( 'NONE', *, *, #7613, .T. ) ;
#34013=CARTESIAN_POINT ( 'NONE',  ( 277.3542486889354564, -20.49999999999999645, -17.00000000000000000 ) ) ;
#34019=EDGE_CURVE ( 'NONE', #27626, #24235, #11843, .T. ) ;
#34032=CARTESIAN_POINT ( 'NONE',  ( 7.000000000000000000, -37.14999999999894698, 8.200000000002349410 ) ) ;
#34042=DIRECTION ( 'NONE',  ( 1.000000000000000000, 0.000000000000000000, 0.000000000000000000 ) ) ;
#34043=ORIENTED_EDGE ( 'NONE', *, *, #11687, .F. ) ;
#34049=CARTESIAN_POINT ( 'NONE',  ( 283.0000000000000568, -21.00000000000000000, -17.50000000000000000 ) ) ;
#34085=ADVANCED_FACE ( 'NONE', ( #21315, #52813 ), #69394, .T. ) ;
#34095=EDGE_CURVE ( 'NONE', #31769, #61959, #48187, .T. ) ;
#34120=AXIS2_PLACEMENT_3D ( 'NONE', #55363, #69879, #28135 ) ;
#34122=CARTESIAN_POINT ( 'NONE',  ( 6.884529946162100345, -21.00000000000000000, -8.000000000000000000 ) ) ;
#34126=ORIENTED_EDGE ( 'NONE', *, *, #24597, .T. ) ;
#34131=ORIENTED_EDGE ( 'NONE', *, *, #21267, .F. ) ;
#34134=EDGE_LOOP ( 'NONE', ( #60871, #30890, #3192, #64804 ) ) ;
#34149=AXIS2_PLACEMENT_3D ( 'NONE', #41444, #14571, #36485 ) ;
#34155=EDGE_CURVE ( 'NONE', #25545, #3194, #32623, .T. ) ;
#34171=VERTEX_POINT ( 'NONE', #49567 ) ;
#34176=CARTESIAN_POINT ( 'NONE',  ( 7.500000000000000000, -53.81370849898476649, -20.00000000000000000 ) ) ;
#34177=CYLINDRICAL_SURFACE ( 'NONE', #10313, 0.5000000000004254375 ) ;
#34179=ORIENTED_EDGE ( 'NONE', *, *, #15924, .T. ) ;
#34191=DIRECTION ( 'NONE',  ( -0.7071067811865460184, -0.7071067811865489050, 0.000000000000000000 ) ) ;
#34206=CARTESIAN_POINT ( 'NONE',  ( 7.000000000000000000, -32.95000000000000284, -13.19999999999999929 ) ) ;
#34212=AXIS2_PLACEMENT_3D ( 'NONE', #9617, #56036, #20564 ) ;
#34214=VERTEX_POINT ( 'NONE', #26969 ) ;
#34217=DIRECTION ( 'NONE',  ( -1.000000000000000000, 0.000000000000000000, 0.000000000000000000 ) ) ;
#34233=EDGE_CURVE ( 'NONE', #5501, #21753, #65823, .T. ) ;
#34242=ORIENTED_EDGE ( 'NONE', *, *, #62939, .F. ) ;
#34254=DIRECTION ( 'NONE',  ( 1.000000000000000000, 0.000000000000000000, 0.000000000000000000 ) ) ;
#34257=DIRECTION ( 'NONE',  ( 0.000000000000000000, -0.7071067811828075644, 0.7071067811902875810 ) ) ;
#34271=FACE_BOUND ( 'NONE', #10354, .T. ) ;
#34283=DIRECTION ( 'NONE',  ( 1.000000000000000000, -0.000000000000000000, -0.000000000000000000 ) ) ;
#34284=DIRECTION ( 'NONE',  ( 0.000000000000000000, 0.7071067811865475727, -0.7071067811865475727 ) ) ;
#34291=VERTEX_POINT ( 'NONE', #63271 ) ;
#34300=VECTOR ( 'NONE', #49101, 1000.000000000000000 ) ;
#34340=CARTESIAN_POINT ( 'NONE',  ( 283.0000000000000568, -25.50000000000000355, 17.00000000000000000 ) ) ;
#34356=CARTESIAN_POINT ( 'NONE',  ( 15.00000000000000000, -26.28355339059299922, 9.766446609406699508 ) ) ;
#34360=ORIENTED_EDGE ( 'NONE', *, *, #62511, .T. ) ;
#34389=LINE ( 'NONE', #61620, #60154 ) ;
#34397=CARTESIAN_POINT ( 'NONE',  ( 280.0000000000000000, -20.49999999999999645, -20.00000000000000000 ) ) ;
#34401=EDGE_CURVE ( 'NONE', #14513, #60332, #15880, .T. ) ;
#34445=ORIENTED_EDGE ( 'NONE', *, *, #27702, .F. ) ;
#34460=CARTESIAN_POINT ( 'NONE',  ( 283.0000000000000568, -25.50000000000000355, -14.74860679774999994 ) ) ;
#34475=CARTESIAN_POINT ( 'NONE',  ( 283.0000000000000568, -26.42999999999999972, 9.412893218813501051 ) ) ;
#34490=VECTOR ( 'NONE', #68017, 1000.000000000000000 ) ;
#34492=AXIS2_PLACEMENT_3D ( 'NONE', #37595, #60177, #11731 ) ;
#34519=DIRECTION ( 'NONE',  ( 0.000000000000000000, -1.000000000000000000, 0.000000000000000000 ) ) ;
#34520=DIRECTION ( 'NONE',  ( 0.000000000000000000, 0.000000000000000000, -1.000000000000000000 ) ) ;
#34522=VECTOR ( 'NONE', #23504, 1000.000000000000000 ) ;
#34531=DIRECTION ( 'NONE',  ( -1.000000000000000000, 0.000000000000000000, 0.000000000000000000 ) ) ;
#34534=LINE ( 'NONE', #13329, #24824 ) ;
#34540=LINE ( 'NONE', #34886, #2165 ) ;
#34591=CARTESIAN_POINT ( 'NONE',  ( 7.500000000000000000, -53.81370849898476649, -20.00000000000000000 ) ) ;
#34597=AXIS2_PLACEMENT_3D ( 'NONE', #53420, #20879, #21244 ) ;
#34624=ORIENTED_EDGE ( 'NONE', *, *, #34155, .F. ) ;
#34628=ADVANCED_FACE ( 'NONE', ( #273 ), #22875, .F. ) ;
#34629=CARTESIAN_POINT ( 'NONE',  ( 283.0000000000000568, -42.50000000000000000, 7.500000000000000000 ) ) ;
#34635=ORIENTED_EDGE ( 'NONE', *, *, #62189, .F. ) ;
#34643=AXIS2_PLACEMENT_3D ( 'NONE', #18985, #66022, #17588 ) ;
#34656=ORIENTED_EDGE ( 'NONE', *, *, #10874, .F. ) ;
#34665=CARTESIAN_POINT ( 'NONE',  ( 7.000000000000000000, -26.79000000000000625, 0.000000000000000000 ) ) ;
#34684=EDGE_CURVE ( 'NONE', #22096, #61056, #33818, .T. ) ;
#34754=VECTOR ( 'NONE', #50190, 1000.000000000000000 ) ;
#34773=ADVANCED_FACE ( 'NONE', ( #46177 ), #46523, .T. ) ;
#34779=ORIENTED_EDGE ( 'NONE', *, *, #68591, .F. ) ;
#34790=ORIENTED_EDGE ( 'NONE', *, *, #64436, .F. ) ;
#34802=CARTESIAN_POINT ( 'NONE',  ( 283.0000000000000568, -20.40000000000000213, 17.60000000000000142 ) ) ;
#34808=VECTOR ( 'NONE', #12451, 1000.000000000000000 ) ;
#34823=CARTESIAN_POINT ( 'NONE',  ( 7.000000000000000000, -38.64999999999999858, -15.00000000000000000 ) ) ;
#34828=ORIENTED_EDGE ( 'NONE', *, *, #37897, .F. ) ;
#34836=LINE ( 'NONE', #66675, #56021 ) ;
#34861=ADVANCED_FACE ( 'NONE', ( #47242 ), #36620, .F. ) ;
#34863=LINE ( 'NONE', #8710, #69680 ) ;
#34875=DIRECTION ( 'NONE',  ( 0.000000000000000000, 1.000000000000000000, 0.000000000000000000 ) ) ;
#34883=AXIS2_PLACEMENT_3D ( 'NONE', #58076, #21649, #25565 ) ;
#34884=LINE ( 'NONE', #35229, #7445 ) ;
#34886=CARTESIAN_POINT ( 'NONE',  ( 289.5000000000000000, -42.50000000000000000, 26.50000000000000000 ) ) ;
#34889=DIRECTION ( 'NONE',  ( -0.7071067811865490160, 0.7071067811865461294, 0.000000000000000000 ) ) ;
#34890=ORIENTED_EDGE ( 'NONE', *, *, #42731, .T. ) ;
#34904=CARTESIAN_POINT ( 'NONE',  ( 15.00000000000000000, -42.00000000000000000, -15.10000000000000142 ) ) ;
#34945=DIRECTION ( 'NONE',  ( 0.000000000000000000, 0.000000000000000000, 1.000000000000000000 ) ) ;
#34964=CARTESIAN_POINT ( 'NONE',  ( 283.0000000000000568, -38.15000000000000568, 13.19999999999999929 ) ) ;
#34970=LINE ( 'NONE', #50554, #59019 ) ;
#34972=DIRECTION ( 'NONE',  ( 0.000000000000000000, 0.000000000000000000, -1.000000000000000000 ) ) ;
#34992=ADVANCED_FACE ( 'NONE', ( #44342 ), #38374, .T. ) ;
#35006=AXIS2_PLACEMENT_3D ( 'NONE', #28428, #2265, #11817 ) ;
#35014=EDGE_LOOP ( 'NONE', ( #1060, #53601, #48900, #69484 ) ) ;
#35016=VECTOR ( 'NONE', #26999, 1000.000000000000000 ) ;
#35031=EDGE_CURVE ( 'NONE', #24890, #50924, #6545, .T. ) ;
#35049=CARTESIAN_POINT ( 'NONE',  ( 7.000000000000000000, -26.50000000000000000, 0.5000000000000000000 ) ) ;
#35074=DIRECTION ( 'NONE',  ( 0.000000000000000000, 0.000000000000000000, 1.000000000000000000 ) ) ;
#35096=DIRECTION ( 'NONE',  ( -1.000000000000000000, 0.000000000000000000, 0.000000000000000000 ) ) ;
#35106=LINE ( 'NONE', #56340, #63711 ) ;
#35124=ADVANCED_FACE ( 'NONE', ( #57052 ), #8613, .F. ) ;
#35130=DIRECTION ( 'NONE',  ( 0.000000000000000000, 0.000000000000000000, 1.000000000000000000 ) ) ;
#35137=DIRECTION ( 'NONE',  ( 0.000000000000000000, 0.7071067811865474617, 0.7071067811865474617 ) ) ;
#35144=FACE_OUTER_BOUND ( 'NONE', #29769, .T. ) ;
#35163=DIRECTION ( 'NONE',  ( 0.000000000000000000, 1.000000000000000000, 0.000000000000000000 ) ) ;
#35192=ORIENTED_EDGE ( 'NONE', *, *, #21022, .T. ) ;
#35210=CARTESIAN_POINT ( 'NONE',  ( 7.500000000000000000, -25.50000000000000355, 20.00000000000000000 ) ) ;
#35217=ORIENTED_EDGE ( 'NONE', *, *, #7310, .T. ) ;
#35229=CARTESIAN_POINT ( 'NONE',  ( 7.000000000000000000, -23.65000000000000568, 12.40000000000000213 ) ) ;
#35244=LINE ( 'NONE', #56826, #18094 ) ;
#35245=ORIENTED_EDGE ( 'NONE', *, *, #57837, .F. ) ;
#35246=DIRECTION ( 'NONE',  ( -1.000000000000000000, 0.000000000000000000, 0.000000000000000000 ) ) ;
#35250=DIRECTION ( 'NONE',  ( 0.000000000000000000, -1.901256929667043247E-12, 1.000000000000000000 ) ) ;
#35253=VECTOR ( 'NONE', #67076, 1000.000000000000000 ) ;
#35269=DIRECTION ( 'NONE',  ( 1.000000000000000000, 0.000000000000000000, 0.000000000000000000 ) ) ;
#35272=PLANE ( 'NONE',  #27493 ) ;
#35274=ORIENTED_EDGE ( 'NONE', *, *, #38629, .F. ) ;
#35278=EDGE_CURVE ( 'NONE', #12942, #66121, #31861, .T. ) ;
#35282=ORIENTED_EDGE ( 'NONE', *, *, #55303, .T. ) ;
#35285=AXIS2_PLACEMENT_3D ( 'NONE', #63674, #51656, #3918 ) ;
#35286=DIRECTION ( 'NONE',  ( 0.000000000000000000, 0.000000000000000000, 1.000000000000000000 ) ) ;
#35288=ADVANCED_FACE ( 'NONE', ( #68020 ), #48460, .F. ) ;
#35308=DIRECTION ( 'NONE',  ( 0.000000000000000000, 0.000000000000000000, 1.000000000000000000 ) ) ;
#35311=VERTEX_POINT ( 'NONE', #14282 ) ;
#35320=CYLINDRICAL_SURFACE ( 'NONE', #14952, 0.3000000000005393908 ) ;
#35324=DIRECTION ( 'NONE',  ( 1.000000000000000000, 0.000000000000000000, 0.000000000000000000 ) ) ;
#35325=VECTOR ( 'NONE', #46829, 1000.000000000000000 ) ;
#35329=LINE ( 'NONE', #56904, #54704 ) ;
#35342=FACE_OUTER_BOUND ( 'NONE', #19190, .T. ) ;
#35353=EDGE_CURVE ( 'NONE', #15205, #52522, #59066, .T. ) ;
#35372=CARTESIAN_POINT ( 'NONE',  ( 283.0000000000000568, -40.30000000000000426, -8.900000000000000355 ) ) ;
#35384=CARTESIAN_POINT ( 'NONE',  ( 7.000000000000000000, -26.50000000000000000, 9.080000000000000071 ) ) ;
#35388=EDGE_CURVE ( 'NONE', #18763, #3647, #65755, .T. ) ;
#35411=DIRECTION ( 'NONE',  ( -0.5773502691896257311, -0.5773502691896257311, 0.5773502691896257311 ) ) ;
#35417=CARTESIAN_POINT ( 'NONE',  ( 280.0000000000000000, -53.81370849898476649, -20.00000000000000000 ) ) ;
#35433=EDGE_CURVE ( 'NONE', #46362, #45646, #30084, .T. ) ;
#35435=EDGE_CURVE ( 'NONE', #10988, #24256, #62839, .T. ) ;
#35437=EDGE_LOOP ( 'NONE', ( #61715, #27906, #5647, #11622, #56949, #38259 ) ) ;
#35452=ORIENTED_EDGE ( 'NONE', *, *, #26774, .T. ) ;
#35457=VECTOR ( 'NONE', #54750, 1000.000000000000000 ) ;
#35513=AXIS2_PLACEMENT_3D ( 'NONE', #47950, #20031, #69519 ) ;
#35560=ORIENTED_EDGE ( 'NONE', *, *, #64536, .T. ) ;
#35561=EDGE_CURVE ( 'NONE', #23661, #5435, #67506, .T. ) ;
#35567=DIRECTION ( 'NONE',  ( -1.000000000000000000, 0.000000000000000000, 0.000000000000000000 ) ) ;
#35589=CARTESIAN_POINT ( 'NONE',  ( 275.0000000000000000, -40.30000000000000426, 8.900000000000000355 ) ) ;
#35603=CARTESIAN_POINT ( 'NONE',  ( 7.000000000000000000, -21.00000000000000000, 0.000000000000000000 ) ) ;
#35619=LINE ( 'NONE', #29975, #22709 ) ;
#35629=DIRECTION ( 'NONE',  ( 0.000000000000000000, -0.7071067811865474617, -0.7071067811865474617 ) ) ;
#35673=ORIENTED_EDGE ( 'NONE', *, *, #27494, .T. ) ;
#35674=CARTESIAN_POINT ( 'NONE',  ( 283.0000000000000568, -38.64999999999999858, 15.00000000000000000 ) ) ;
#35691=CARTESIAN_POINT ( 'NONE',  ( 6.884529946162100345, -21.00000000000000000, 0.000000000000000000 ) ) ;
#35695=VERTEX_POINT ( 'NONE', #31435 ) ;
#35722=VERTEX_POINT ( 'NONE', #9497 ) ;
#35727=CARTESIAN_POINT ( 'NONE',  ( 283.0000000000000568, -31.30000000000095284, -12.19999999999906315 ) ) ;
#35734=AXIS2_PLACEMENT_3D ( 'NONE', #28962, #1067, #17306 ) ;
#35736=( BOUNDED_CURVE ( )  B_SPLINE_CURVE ( 3, ( #42214, #62727, #58130, #15002 ),
 .UNSPECIFIED., .F., .F. ) 
 B_SPLINE_CURVE_WITH_KNOTS ( ( 4, 4 ),
 ( 3.864326901403208669, 4.037257447447657910 ),
 .UNSPECIFIED. ) 
 CURVE ( )  GEOMETRIC_REPRESENTATION_ITEM ( )  RATIONAL_B_SPLINE_CURVE ( ( 1.000000000000000000, 0.9975094710839674805, 0.9975094710839674805, 1.000000000000000000 ) ) 
 REPRESENTATION_ITEM ( '' )  );
#35743=VERTEX_POINT ( 'NONE', #52999 ) ;
#35784=VECTOR ( 'NONE', #24810, 1000.000000000000000 ) ;
#35785=PLANE ( 'NONE',  #34149 ) ;
#35788=LINE ( 'NONE', #52414, #67730 ) ;
#35789=ORIENTED_EDGE ( 'NONE', *, *, #23877, .T. ) ;
#35798=ORIENTED_EDGE ( 'NONE', *, *, #7310, .F. ) ;
#35810=ORIENTED_EDGE ( 'NONE', *, *, #2097, .T. ) ;
#35821=AXIS2_PLACEMENT_3D ( 'NONE', #19048, #31688, #26726 ) ;
#35840=ADVANCED_FACE ( 'NONE', ( #39478 ), #59680, .T. ) ;
#35841=CARTESIAN_POINT ( 'NONE',  ( 275.0000000000000000, -21.00000000000000000, 17.50000000000000000 ) ) ;
#35843=LINE ( 'NONE', #31266, #28416 ) ;
#35859=ORIENTED_EDGE ( 'NONE', *, *, #49192, .T. ) ;
#35898=VECTOR ( 'NONE', #17925, 1000.000000000000000 ) ;
#35903=CARTESIAN_POINT ( 'NONE',  ( 7.000000000000000000, -20.50000000000000000, -13.00000000000000178 ) ) ;
#35918=VERTEX_POINT ( 'NONE', #16891 ) ;
#35920=ORIENTED_EDGE ( 'NONE', *, *, #35278, .F. ) ;
#35923=UNCERTAINTY_MEASURE_WITH_UNIT (LENGTH_MEASURE( 1.000000000000000082E-05 ), #397, 'distance_accuracy_value', 'NONE');
#35955=CARTESIAN_POINT ( 'NONE',  ( 0.5000000000000000000, -42.00000000000000000, -27.00000000000000000 ) ) ;
#35968=ORIENTED_EDGE ( 'NONE', *, *, #36241, .T. ) ;
#35976=EDGE_CURVE ( 'NONE', #21925, #68361, #34863, .T. ) ;
#35980=ORIENTED_EDGE ( 'NONE', *, *, #916, .F. ) ;
#35981=LINE ( 'NONE', #47641, #66105 ) ;
#35984=CARTESIAN_POINT ( 'NONE',  ( 283.0000000000000568, -20.40000000000000213, -12.40000000000000213 ) ) ;
#35992=DIRECTION ( 'NONE',  ( 0.000000000000000000, 0.7071067811865474617, 0.7071067811865474617 ) ) ;
#35994=EDGE_LOOP ( 'NONE', ( #61594, #14656, #63774, #55053, #37476, #30607 ) ) ;
#35999=DIRECTION ( 'NONE',  ( 0.000000000000000000, -1.000000000000000000, -1.880440247955360336E-12 ) ) ;
#36008=EDGE_CURVE ( 'NONE', #50581, #66792, #17715, .T. ) ;
#36016=EDGE_CURVE ( 'NONE', #51904, #18299, #40174, .T. ) ;
#36032=DIRECTION ( 'NONE',  ( 0.5773502691896257311, -0.5773502691896258421, -0.5773502691896257311 ) ) ;
#36035=VECTOR ( 'NONE', #17596, 1000.000000000000000 ) ;
#36041=VECTOR ( 'NONE', #32577, 1000.000000000000000 ) ;
#36057=CYLINDRICAL_SURFACE ( 'NONE', #24625, 0.5000000000023371305 ) ;
#36122=FACE_OUTER_BOUND ( 'NONE', #52891, .T. ) ;
#36145=ORIENTED_EDGE ( 'NONE', *, *, #38437, .F. ) ;
#36174=ORIENTED_EDGE ( 'NONE', *, *, #22543, .F. ) ;
#36183=LINE ( 'NONE', #15327, #34490 ) ;
#36190=VERTEX_POINT ( 'NONE', #10115 ) ;
#36198=DIRECTION ( 'NONE',  ( -1.000000000000000000, 0.000000000000000000, 0.000000000000000000 ) ) ;
#36202=EDGE_CURVE ( 'NONE', #53301, #2050, #45633, .T. ) ;
#36212=FACE_OUTER_BOUND ( 'NONE', #38520, .T. ) ;
#36221=CARTESIAN_POINT ( 'NONE',  ( 15.00000000000000000, -20.40000000000000213, 12.40000000000000213 ) ) ;
#36236=EDGE_CURVE ( 'NONE', #8968, #13785, #17844, .T. ) ;
#36241=EDGE_CURVE ( 'NONE', #46689, #69904, #16814, .T. ) ;
#36270=CARTESIAN_POINT ( 'NONE',  ( 15.00000000000000000, -21.00000000000000000, -4.000000000000000000 ) ) ;
#36271=ORIENTED_EDGE ( 'NONE', *, *, #31648, .F. ) ;
#36281=AXIS2_PLACEMENT_3D ( 'NONE', #28741, #13529, #44649 ) ;
#36290=ORIENTED_EDGE ( 'NONE', *, *, #67542, .T. ) ;
#36298=DIRECTION ( 'NONE',  ( 0.000000000000000000, 0.6666666666652433237, -0.7453559925012029908 ) ) ;
#36303=LINE ( 'NONE', #31377, #8927 ) ;
#36308=CARTESIAN_POINT ( 'NONE',  ( 15.00000000000000000, -26.42999999999999972, -9.412893218813501051 ) ) ;
#36316=ORIENTED_EDGE ( 'NONE', *, *, #48808, .F. ) ;
#36320=DIRECTION ( 'NONE',  ( -0.7071067811865463515, -0.7071067811865487940, 0.000000000000000000 ) ) ;
#36324=DIRECTION ( 'NONE',  ( 1.000000000000000000, -0.000000000000000000, -0.000000000000000000 ) ) ;
#36368=FACE_OUTER_BOUND ( 'NONE', #42064, .T. ) ;
#36385=AXIS2_PLACEMENT_3D ( 'NONE', #23617, #18306, #45175 ) ;
#36428=EDGE_CURVE ( 'NONE', #51826, #31741, #8268, .T. ) ;
#36458=DIRECTION ( 'NONE',  ( 0.000000000000000000, -1.000000000000000000, 0.000000000000000000 ) ) ;
#36480=LINE ( 'NONE', #64416, #45551 ) ;
#36485=DIRECTION ( 'NONE',  ( 0.000000000000000000, 0.000000000000000000, -1.000000000000000000 ) ) ;
#36487=ORIENTED_EDGE ( 'NONE', *, *, #64040, .F. ) ;
#36493=FACE_OUTER_BOUND ( 'NONE', #63286, .T. ) ;
#36514=VERTEX_POINT ( 'NONE', #52117 ) ;
#36516=ORIENTED_EDGE ( 'NONE', *, *, #31267, .F. ) ;
#36519=CARTESIAN_POINT ( 'NONE',  ( 15.00000000000000000, -23.65000000000000568, 12.40000000000000213 ) ) ;
#36525=ORIENTED_EDGE ( 'NONE', *, *, #8424, .F. ) ;
#36529=ORIENTED_EDGE ( 'NONE', *, *, #46795, .F. ) ;
#36533=DIRECTION ( 'NONE',  ( 0.000000000000000000, 1.000000000000000000, 0.000000000000000000 ) ) ;
#36534=CARTESIAN_POINT ( 'NONE',  ( 7.000000000000000000, -37.61196062927500350, 8.008708659369300875 ) ) ;
#36535=EDGE_LOOP ( 'NONE', ( #54816, #50538, #34126, #39121 ) ) ;
#36538=AXIS2_PLACEMENT_3D ( 'NONE', #59653, #59985, #60682 ) ;
#36544=CIRCLE ( 'NONE', #33151, 5.000000000000000000 ) ;
#36553=CIRCLE ( 'NONE', #15109, 8.000000000000001776 ) ;
#36562=ORIENTED_EDGE ( 'NONE', *, *, #10308, .F. ) ;
#36582=EDGE_LOOP ( 'NONE', ( #69807, #34790 ) ) ;
#36592=CARTESIAN_POINT ( 'NONE',  ( 283.0000000000000568, -32.95000000000000284, 13.19999999999999929 ) ) ;
#36620=CYLINDRICAL_SURFACE ( 'NONE', #5218, 0.2999999999994933941 ) ;
#36650=CARTESIAN_POINT ( 'NONE',  ( 7.000000000000000000, -32.45000000000000995, -15.00000000000000000 ) ) ;
#36657=CARTESIAN_POINT ( 'NONE',  ( 283.0000000000000568, -42.50000000000000000, -14.49999999999903899 ) ) ;
#36673=ORIENTED_EDGE ( 'NONE', *, *, #61955, .F. ) ;
#36685=ORIENTED_EDGE ( 'NONE', *, *, #33503, .F. ) ;
#36686=DIRECTION ( 'NONE',  ( 1.000000000000000000, 0.000000000000000000, 0.000000000000000000 ) ) ;
#36694=CARTESIAN_POINT ( 'NONE',  ( 275.0000000000000000, -42.00000000000000000, -26.50000000000000000 ) ) ;
#36697=DIRECTION ( 'NONE',  ( 0.000000000000000000, 0.000000000000000000, -1.000000000000000000 ) ) ;
#36698=ORIENTED_EDGE ( 'NONE', *, *, #58301, .F. ) ;
#36714=VECTOR ( 'NONE', #49009, 1000.000000000000000 ) ;
#36729=LINE ( 'NONE', #19744, #32400 ) ;
#36742=EDGE_CURVE ( 'NONE', #10806, #26444, #51692, .T. ) ;
#36752=DIRECTION ( 'NONE',  ( -1.000000000000000000, 0.000000000000000000, 0.000000000000000000 ) ) ;
#36753=DIRECTION ( 'NONE',  ( 1.000000000000000000, -0.000000000000000000, -0.000000000000000000 ) ) ;
#36767=CYLINDRICAL_SURFACE ( 'NONE', #67209, 8.000000000000000000 ) ;
#36802=VERTEX_POINT ( 'NONE', #50280 ) ;
#36803=AXIS2_PLACEMENT_3D ( 'NONE', #17524, #22150, #28817 ) ;
#36813=CARTESIAN_POINT ( 'NONE',  ( 283.0000000000000568, -25.60000000000000142, 15.10000000000000142 ) ) ;
#36836=CARTESIAN_POINT ( 'NONE',  ( 283.0000000000000568, -30.80000000000000071, -12.20000000000000107 ) ) ;
#36849=LINE ( 'NONE', #64078, #5866 ) ;
#36862=ORIENTED_EDGE ( 'NONE', *, *, #34019, .T. ) ;
#36874=EDGE_LOOP ( 'NONE', ( #10187, #37334, #48568, #18405 ) ) ;
#36881=CARTESIAN_POINT ( 'NONE',  ( 14.50000000000000000, -0.5000000000000000000, -27.00000000000000000 ) ) ;
#36888=ORIENTED_EDGE ( 'NONE', *, *, #51576, .T. ) ;
#36890=DIRECTION ( 'NONE',  ( 1.000000000000000000, 0.000000000000000000, 0.000000000000000000 ) ) ;
#36892=( NAMED_UNIT ( * ) PLANE_ANGLE_UNIT ( ) SI_UNIT ( $, .RADIAN. ) );
#36941=LINE ( 'NONE', #489, #66122 ) ;
#36955=AXIS2_PLACEMENT_3D ( 'NONE', #23318, #22968, #44518 ) ;
#36965=DIRECTION ( 'NONE',  ( 0.000000000000000000, 1.000000000000000000, 0.000000000000000000 ) ) ;
#37004=CIRCLE ( 'NONE', #43754, 0.4999999999945519691 ) ;
#37014=CIRCLE ( 'NONE', #28013, 0.5000000000023371305 ) ;
#37016=DIRECTION ( 'NONE',  ( 0.000000000000000000, 0.7071067811865480168, 0.7071067811865470176 ) ) ;
#37030=CARTESIAN_POINT ( 'NONE',  ( 283.0000000000000568, -39.80000000000000426, -12.69999999999999929 ) ) ;
#37033=DIRECTION ( 'NONE',  ( -0.5773502691896257311, -0.5773502691896257311, 0.5773502691896257311 ) ) ;
#37069=EDGE_CURVE ( 'NONE', #27061, #40434, #46, .T. ) ;
#37077=ADVANCED_FACE ( 'NONE', ( #16656 ), #65434, .T. ) ;
#37088=ADVANCED_FACE ( 'NONE', ( #10636 ), #22640, .F. ) ;
#37106=VERTEX_POINT ( 'NONE', #16293 ) ;
#37112=ORIENTED_EDGE ( 'NONE', *, *, #52189, .F. ) ;
#37124=ORIENTED_EDGE ( 'NONE', *, *, #27290, .T. ) ;
#37132=ORIENTED_EDGE ( 'NONE', *, *, #39393, .F. ) ;
#37148=DIRECTION ( 'NONE',  ( 0.000000000000000000, 0.000000000000000000, 1.000000000000000000 ) ) ;
#37169=CARTESIAN_POINT ( 'NONE',  ( 283.0000000000000568, -20.50000000000000000, 13.00000000000000178 ) ) ;
#37182=DIRECTION ( 'NONE',  ( 0.000000000000000000, 1.000000000000000000, 0.000000000000000000 ) ) ;
#37183=DIRECTION ( 'NONE',  ( 0.000000000000000000, 1.000000000000000000, 8.604228440837611257E-13 ) ) ;
#37193=CARTESIAN_POINT ( 'NONE',  ( 275.0000000000000000, -32.95000000000000284, 14.50000000000000000 ) ) ;
#37196=ORIENTED_EDGE ( 'NONE', *, *, #10090, .F. ) ;
#37208=VERTEX_POINT ( 'NONE', #29930 ) ;
#37217=DIRECTION ( 'NONE',  ( 0.000000000000000000, 1.000000000000000000, 0.000000000000000000 ) ) ;
#37233=ORIENTED_EDGE ( 'NONE', *, *, #4202, .T. ) ;
#37240=ORIENTED_EDGE ( 'NONE', *, *, #43339, .T. ) ;
#37286=DIRECTION ( 'NONE',  ( 0.000000000000000000, 1.000000000000000000, 0.000000000000000000 ) ) ;
#37334=ORIENTED_EDGE ( 'NONE', *, *, #68431, .F. ) ;
#37343=VERTEX_POINT ( 'NONE', #63527 ) ;
#37351=LINE ( 'NONE', #32396, #32468 ) ;
#37372=CARTESIAN_POINT ( 'NONE',  ( 283.0000000000000568, -39.79999999999954952, 8.900000000000419575 ) ) ;
#37378=ORIENTED_EDGE ( 'NONE', *, *, #49912, .F. ) ;
#37383=DIRECTION ( 'NONE',  ( 0.000000000000000000, 0.9760787414516886029, 0.2174173187353931058 ) ) ;
#37391=AXIS2_PLACEMENT_3D ( 'NONE', #44349, #60628, #17843 ) ;
#37399=ORIENTED_EDGE ( 'NONE', *, *, #58860, .T. ) ;
#37413=LINE ( 'NONE', #58628, #10529 ) ;
#37418=DIRECTION ( 'NONE',  ( 0.000000000000000000, 0.000000000000000000, 1.000000000000000000 ) ) ;
#37421=AXIS2_PLACEMENT_3D ( 'NONE', #20997, #5456, #32657 ) ;
#37422=CARTESIAN_POINT ( 'NONE',  ( 7.000000000000000000, -38.65000000000095781, 14.49999999999903899 ) ) ;
#37424=CARTESIAN_POINT ( 'NONE',  ( 15.00000000000000000, -26.42999999999999972, -9.412893218813501051 ) ) ;
#37450=CARTESIAN_POINT ( 'NONE',  ( 7.000000000000000000, -39.79999999999905214, 12.19999999999906315 ) ) ;
#37456=DIRECTION ( 'NONE',  ( 0.000000000000000000, -0.7071067811828075644, 0.7071067811902875810 ) ) ;
#37466=VERTEX_POINT ( 'NONE', #15776 ) ;
#37473=CARTESIAN_POINT ( 'NONE',  ( 283.0000000000000568, -32.95000000000000284, 13.19999999999999929 ) ) ;
#37476=ORIENTED_EDGE ( 'NONE', *, *, #8366, .T. ) ;
#37480=EDGE_CURVE ( 'NONE', #55046, #65427, #37351, .T. ) ;
#37494=ORIENTED_EDGE ( 'NONE', *, *, #44886, .T. ) ;
#37506=VECTOR ( 'NONE', #60059, 1000.000000000000000 ) ;
#37514=EDGE_CURVE ( 'NONE', #3076, #30690, #49353, .T. ) ;
#37517=ORIENTED_EDGE ( 'NONE', *, *, #39218, .T. ) ;
#37545=VECTOR ( 'NONE', #24724, 1000.000000000000114 ) ;
#37548=VERTEX_POINT ( 'NONE', #926 ) ;
#37560=ORIENTED_EDGE ( 'NONE', *, *, #55165, .T. ) ;
#37569=ADVANCED_FACE ( 'NONE', ( #17501 ), #39072, .F. ) ;
#37587=ADVANCED_FACE ( 'NONE', ( #29503 ), #41159, .T. ) ;
#37591=EDGE_LOOP ( 'NONE', ( #47111, #15407, #7838, #48980 ) ) ;
#37595=CARTESIAN_POINT ( 'NONE',  ( 7.000000000000000000, -20.40000000000000213, -12.40000000000000213 ) ) ;
#37599=DIRECTION ( 'NONE',  ( 0.000000000000000000, 1.000000000000000000, 0.000000000000000000 ) ) ;
#37604=CIRCLE ( 'NONE', #35285, 3.999999999999993339 ) ;
#37608=DIRECTION ( 'NONE',  ( 0.000000000000000000, 1.000000000000000000, 0.000000000000000000 ) ) ;
#37609=DIRECTION ( 'NONE',  ( 0.000000000000000000, -0.7071067811865474617, 0.7071067811865474617 ) ) ;
#37644=LINE ( 'NONE', #16420, #19309 ) ;
#37649=CARTESIAN_POINT ( 'NONE',  ( 15.00000000000000000, 0.000000000000000000, -27.00000000000000000 ) ) ;
#37653=VECTOR ( 'NONE', #67121, 1000.000000000000114 ) ;
#37669=LINE ( 'NONE', #32704, #79 ) ;
#37672=ORIENTED_EDGE ( 'NONE', *, *, #31347, .F. ) ;
#37707=EDGE_CURVE ( 'NONE', #20854, #33919, #25968, .T. ) ;
#37708=ORIENTED_EDGE ( 'NONE', *, *, #56678, .F. ) ;
#37716=DIRECTION ( 'NONE',  ( 0.000000000000000000, -1.000000000000000000, -8.396061623720747815E-13 ) ) ;
#37717=CARTESIAN_POINT ( 'NONE',  ( 7.000000000000000000, -25.60000000000000142, 15.10000000000000142 ) ) ;
#37734=ORIENTED_EDGE ( 'NONE', *, *, #61062, .T. ) ;
#37755=CARTESIAN_POINT ( 'NONE',  ( 275.5000000000000000, -0.5000000000000000000, -27.00000000000000000 ) ) ;
#37771=VERTEX_POINT ( 'NONE', #47522 ) ;
#37784=ADVANCED_FACE ( 'NONE', ( #26659 ), #69089, .F. ) ;
#37797=LINE ( 'NONE', #1346, #51043 ) ;
#37814=ORIENTED_EDGE ( 'NONE', *, *, #53986, .T. ) ;
#37833=CARTESIAN_POINT ( 'NONE',  ( 283.0000000000000568, -23.29603921945599865, -12.50000000000000000 ) ) ;
#37859=DIRECTION ( 'NONE',  ( 0.000000000000000000, 1.000000000000000000, 0.000000000000000000 ) ) ;
#37865=CARTESIAN_POINT ( 'NONE',  ( 283.0000000000000568, -38.65000000000095781, -14.49999999999903899 ) ) ;
#37873=EDGE_LOOP ( 'NONE', ( #16693, #9709, #51994, #10022 ) ) ;
#37880=AXIS2_PLACEMENT_3D ( 'NONE', #8283, #20307, #47187 ) ;
#37886=EDGE_CURVE ( 'NONE', #62248, #51904, #65196, .T. ) ;
#37897=EDGE_CURVE ( 'NONE', #7638, #18944, #65527, .T. ) ;
#37903=DIRECTION ( 'NONE',  ( 1.000000000000000000, -0.000000000000000000, -0.000000000000000000 ) ) ;
#37909=ORIENTED_EDGE ( 'NONE', *, *, #51048, .T. ) ;
#37923=CARTESIAN_POINT ( 'NONE',  ( 7.000000000000000000, -31.30000000000095284, -12.19999999999906315 ) ) ;
#37928=ORIENTED_EDGE ( 'NONE', *, *, #49777, .F. ) ;
#37930=AXIS2_PLACEMENT_3D ( 'NONE', #65668, #28517, #44419 ) ;
#37941=PLANE ( 'NONE',  #27758 ) ;
#37966=VECTOR ( 'NONE', #60094, 1000.000000000000000 ) ;
#37998=PLANE ( 'NONE',  #46309 ) ;
#38006=VERTEX_POINT ( 'NONE', #34356 ) ;
#38012=CARTESIAN_POINT ( 'NONE',  ( 275.0000000000000000, -20.40000000000000213, 17.60000000000000142 ) ) ;
#38030=AXIS2_PLACEMENT_3D ( 'NONE', #44873, #39902, #66088 ) ;
#38038=CIRCLE ( 'NONE', #62846, 0.5000000000004272138 ) ;
#38043=EDGE_CURVE ( 'NONE', #47818, #41057, #66891, .T. ) ;
#38066=EDGE_CURVE ( 'NONE', #24350, #12410, #37014, .T. ) ;
#38068=CIRCLE ( 'NONE', #30118, 0.5000000000009441337 ) ;
#38071=CARTESIAN_POINT ( 'NONE',  ( 275.0000000000000000, 50.00000000000000000, -26.50000000000000000 ) ) ;
#38073=CARTESIAN_POINT ( 'NONE',  ( 283.0000000000000568, -25.93000000000544958, 9.412893218815410634 ) ) ;
#38075=FACE_OUTER_BOUND ( 'NONE', #65207, .T. ) ;
#38077=LINE ( 'NONE', #11861, #61438 ) ;
#38091=VERTEX_POINT ( 'NONE', #8543 ) ;
#38092=DIRECTION ( 'NONE',  ( 1.000000000000000000, -0.000000000000000000, -0.000000000000000000 ) ) ;
#38093=VERTEX_POINT ( 'NONE', #30123 ) ;
#38094=ORIENTED_EDGE ( 'NONE', *, *, #52518, .F. ) ;
#38097=PLANE ( 'NONE',  #36538 ) ;
#38111=EDGE_LOOP ( 'NONE', ( #28205, #34624, #13522, #24494 ) ) ;
#38130=DIRECTION ( 'NONE',  ( 1.000000000000000000, -0.000000000000000000, -0.000000000000000000 ) ) ;
#38135=CARTESIAN_POINT ( 'NONE',  ( 7.000000000000000000, -25.93000000000544958, -9.412893218815410634 ) ) ;
#38142=DIRECTION ( 'NONE',  ( 0.000000000000000000, 0.000000000000000000, -1.000000000000000000 ) ) ;
#38149=ADVANCED_FACE ( 'NONE', ( #11982 ), #23639, .T. ) ;
#38157=CARTESIAN_POINT ( 'NONE',  ( 7.000000000000000000, -38.64999999999999858, 15.00000000000000000 ) ) ;
#38166=DIRECTION ( 'NONE',  ( 1.000000000000000000, 0.000000000000000000, 0.000000000000000000 ) ) ;
#38178=CARTESIAN_POINT ( 'NONE',  ( 275.0000000000000000, -32.44999999999905071, 14.49999999999906031 ) ) ;
#38185=CIRCLE ( 'NONE', #16729, 0.5000000000004306555 ) ;
#38191=LINE ( 'NONE', #43824, #2979 ) ;
#38223=DIRECTION ( 'NONE',  ( 0.000000000000000000, 0.000000000000000000, -1.000000000000000000 ) ) ;
#38230=VERTEX_POINT ( 'NONE', #28259 ) ;
#38246=CARTESIAN_POINT ( 'NONE',  ( 15.00000000000000000, -25.60000000000000142, -17.60000000000000142 ) ) ;
#38259=ORIENTED_EDGE ( 'NONE', *, *, #17169, .T. ) ;
#38260=FACE_OUTER_BOUND ( 'NONE', #8002, .T. ) ;
#38278=CARTESIAN_POINT ( 'NONE',  ( 283.0000000000000568, -25.60000000000000142, -15.10000000000000142 ) ) ;
#38283=ORIENTED_EDGE ( 'NONE', *, *, #27172, .T. ) ;
#38287=LINE ( 'NONE', #11058, #64439 ) ;
#38296=EDGE_CURVE ( 'NONE', #46689, #56785, #30710, .T. ) ;
#38304=LINE ( 'NONE', #69790, #25015 ) ;
#38313=CARTESIAN_POINT ( 'NONE',  ( 283.0000000000000568, -38.09999999999885034, 7.900000000002049383 ) ) ;
#38329=PLANE ( 'NONE',  #50505 ) ;
#38334=CARTESIAN_POINT ( 'NONE',  ( 275.0000000000000000, -25.60000000000000142, 17.60000000000000142 ) ) ;
#38339=ORIENTED_EDGE ( 'NONE', *, *, #5179, .F. ) ;
#38342=DIRECTION ( 'NONE',  ( 1.000000000000000000, -0.000000000000000000, -0.000000000000000000 ) ) ;
#38349=VERTEX_POINT ( 'NONE', #40606 ) ;
#38374=CYLINDRICAL_SURFACE ( 'NONE', #45872, 0.4999999999945534124 ) ;
#38405=CARTESIAN_POINT ( 'NONE',  ( 283.0000000000000568, -20.85424868893542438, -17.35424868893542438 ) ) ;
#38413=EDGE_CURVE ( 'NONE', #35695, #1141, #29305, .T. ) ;
#38416=ORIENTED_EDGE ( 'NONE', *, *, #38961, .F. ) ;
#38428=ORIENTED_EDGE ( 'NONE', *, *, #34155, .T. ) ;
#38437=EDGE_CURVE ( 'NONE', #26706, #53994, #1869, .T. ) ;
#38439=LINE ( 'NONE', #605, #14441 ) ;
#38450=VERTEX_POINT ( 'NONE', #40275 ) ;
#38461=ORIENTED_EDGE ( 'NONE', *, *, #21127, .T. ) ;
#38493=EDGE_CURVE ( 'NONE', #38006, #53395, #55164, .T. ) ;
#38497=PLANE ( 'NONE',  #44630 ) ;
#38502=CARTESIAN_POINT ( 'NONE',  ( 283.0000000000000568, -32.00000000000000000, -8.400000000000000355 ) ) ;
#38520=EDGE_LOOP ( 'NONE', ( #36862, #2589, #29282, #54848 ) ) ;
#38551=CARTESIAN_POINT ( 'NONE',  ( 7.000000000000000000, -26.28355339059299922, -9.766446609406699508 ) ) ;
#38553=CARTESIAN_POINT ( 'NONE',  ( 10.31889768521804207, -20.65270074880752560, 17.15270074880752560 ) ) ;
#38570=CARTESIAN_POINT ( 'NONE',  ( 282.6457513110646005, -25.50000000000000355, 17.00000000000000000 ) ) ;
#38580=ORIENTED_EDGE ( 'NONE', *, *, #27289, .F. ) ;
#38592=EDGE_LOOP ( 'NONE', ( #6273, #12830, #56832, #13162 ) ) ;
#38620=LINE ( 'NONE', #50255, #56817 ) ;
#38621=DIRECTION ( 'NONE',  ( 0.000000000000000000, 0.000000000000000000, -1.000000000000000000 ) ) ;
#38628=FACE_OUTER_BOUND ( 'NONE', #69496, .T. ) ;
#38629=EDGE_CURVE ( 'NONE', #40700, #25742, #55567, .T. ) ;
#38634=ORIENTED_EDGE ( 'NONE', *, *, #65406, .T. ) ;
#38636=CARTESIAN_POINT ( 'NONE',  ( 275.0000000000000000, -28.95000000000155183, 14.49999999999845990 ) ) ;
#38639=CARTESIAN_POINT ( 'NONE',  ( 7.000000000000000000, -26.50000000000000000, -0.5000000000000000000 ) ) ;
#38649=ORIENTED_EDGE ( 'NONE', *, *, #12538, .F. ) ;
#38651=DIRECTION ( 'NONE',  ( 0.000000000000000000, 0.000000000000000000, -1.000000000000000000 ) ) ;
#38655=DIRECTION ( 'NONE',  ( 0.000000000000000000, 0.4606534372016282686, -0.8875800869748744493 ) ) ;
#38667=CARTESIAN_POINT ( 'NONE',  ( 7.000000000000000000, -40.30000000000000426, 12.20000000000000107 ) ) ;
#38672=ORIENTED_EDGE ( 'NONE', *, *, #9695, .T. ) ;
#38678=CARTESIAN_POINT ( 'NONE',  ( 283.0000000000000568, -21.00000000000000000, 12.50000000000000000 ) ) ;
#38687=ORIENTED_EDGE ( 'NONE', *, *, #43811, .T. ) ;
#38696=VECTOR ( 'NONE', #37148, 1000.000000000000000 ) ;
#38703=VERTEX_POINT ( 'NONE', #61310 ) ;
#38727=CARTESIAN_POINT ( 'NONE',  ( 7.000000000000000000, -26.50000000000000000, 5.530822723609939651 ) ) ;
#38728=DIRECTION ( 'NONE',  ( 0.000000000000000000, 0.000000000000000000, -1.000000000000000000 ) ) ;
#38784=EDGE_LOOP ( 'NONE', ( #63602, #32546, #5751, #28993 ) ) ;
#38806=CARTESIAN_POINT ( 'NONE',  ( 289.5000000000000000, -0.5000000000000000000, 27.00000000000000000 ) ) ;
#38813=DIRECTION ( 'NONE',  ( 1.000000000000000000, 0.000000000000000000, 0.000000000000000000 ) ) ;
#38822=CARTESIAN_POINT ( 'NONE',  ( 280.0000000000000000, -53.81370849898476649, 20.00000000000000000 ) ) ;
#38835=CIRCLE ( 'NONE', #47879, 0.5000000000009406920 ) ;
#38840=ORIENTED_EDGE ( 'NONE', *, *, #8092, .T. ) ;
#38850=CARTESIAN_POINT ( 'NONE',  ( 290.0000000000000000, -21.00000000000000000, -5.000000000000000000 ) ) ;
#38868=ORIENTED_EDGE ( 'NONE', *, *, #2947, .F. ) ;
#38871=AXIS2_PLACEMENT_3D ( 'NONE', #18061, #39964, #29028 ) ;
#38881=CARTESIAN_POINT ( 'NONE',  ( -1.110223024625156540E-16, -42.00000000000000000, -26.50000000000000000 ) ) ;
#38889=EDGE_CURVE ( 'NONE', #38703, #13736, #24555, .T. ) ;
#38894=CARTESIAN_POINT ( 'NONE',  ( 289.5000000000000000, 0.000000000000000000, -26.50000000000000000 ) ) ;
#38903=PLANE ( 'NONE',  #67162 ) ;
#38907=FILL_AREA_STYLE ('',( #31885 ) ) ;
#38916=FACE_OUTER_BOUND ( 'NONE', #1930, .T. ) ;
#38961=EDGE_CURVE ( 'NONE', #18752, #57384, #21356, .T. ) ;
#38982=VERTEX_POINT ( 'NONE', #31618 ) ;
#39005=ORIENTED_EDGE ( 'NONE', *, *, #69725, .T. ) ;
#39015=DIRECTION ( 'NONE',  ( 0.000000000000000000, 0.000000000000000000, 1.000000000000000000 ) ) ;
#39041=AXIS2_PLACEMENT_3D ( 'NONE', #2051, #18298, #35250 ) ;
#39063=CARTESIAN_POINT ( 'NONE',  ( 7.000000000000000000, -25.60000000000000142, -15.10000000000000142 ) ) ;
#39072=PLANE ( 'NONE',  #11010 ) ;
#39073=CYLINDRICAL_SURFACE ( 'NONE', #60135, 0.5000000000009302559 ) ;
#39074=CARTESIAN_POINT ( 'NONE',  ( 15.00000000000000000, -21.00000000000000000, 0.000000000000000000 ) ) ;
#39081=VERTEX_POINT ( 'NONE', #59529 ) ;
#39095=EDGE_CURVE ( 'NONE', #341, #11956, #6476, .T. ) ;
#39121=ORIENTED_EDGE ( 'NONE', *, *, #18813, .T. ) ;
#39135=EDGE_CURVE ( 'NONE', #25678, #27522, #69629, .T. ) ;
#39144=VECTOR ( 'NONE', #9590, 1000.000000000000114 ) ;
#39166=CARTESIAN_POINT ( 'NONE',  ( 7.000000000000000000, -39.80000000000000426, -8.400000000000000355 ) ) ;
#39191=VECTOR ( 'NONE', #55757, 1000.000000000000000 ) ;
#39200=VECTOR ( 'NONE', #62007, 1000.000000000000000 ) ;
#39218=EDGE_CURVE ( 'NONE', #17055, #53282, #61574, .T. ) ;
#39222=DIRECTION ( 'NONE',  ( 1.000000000000000000, 0.000000000000000000, 0.000000000000000000 ) ) ;
#39223=ORIENTED_EDGE ( 'NONE', *, *, #7066, .F. ) ;
#39250=CARTESIAN_POINT ( 'NONE',  ( 282.7711612342632179, -25.38939884375893286, 17.11060115624107425 ) ) ;
#39257=PLANE ( 'NONE',  #39890 ) ;
#39278=PLANE ( 'NONE',  #41983 ) ;
#39279=ORIENTED_EDGE ( 'NONE', *, *, #4748, .F. ) ;
#39282=VERTEX_POINT ( 'NONE', #57687 ) ;
#39288=CARTESIAN_POINT ( 'NONE',  ( 275.0000000000000000, -42.00000000000000000, -15.10000000000000142 ) ) ;
#39302=DIRECTION ( 'NONE',  ( -1.000000000000000000, 0.000000000000000000, 0.000000000000000000 ) ) ;
#39308=VECTOR ( 'NONE', #46604, 1000.000000000000000 ) ;
#39311=DIRECTION ( 'NONE',  ( 0.000000000000000000, 0.000000000000000000, -1.000000000000000000 ) ) ;
#39327=DIRECTION ( 'NONE',  ( 0.000000000000000000, 0.000000000000000000, -1.000000000000000000 ) ) ;
#39338=LINE ( 'NONE', #2206, #34808 ) ;
#39353=LINE ( 'NONE', #8212, #56787 ) ;
#39359=CARTESIAN_POINT ( 'NONE',  ( 10.70000000000000107, -53.81370849898476649, 17.60000000000000142 ) ) ;
#39365=DIRECTION ( 'NONE',  ( -0.5773502691896311712, 0.5773502691896230665, -0.5773502691896230665 ) ) ;
#39388=EDGE_CURVE ( 'NONE', #4296, #32632, #58036, .T. ) ;
#39393=EDGE_CURVE ( 'NONE', #24682, #26444, #59088, .T. ) ;
#39396=ADVANCED_FACE ( 'NONE', ( #20908 ), #31535, .F. ) ;
#39401=CARTESIAN_POINT ( 'NONE',  ( 7.000000000000000000, -26.42999999999999972, 5.874955318979029784 ) ) ;
#39413=CARTESIAN_POINT ( 'NONE',  ( 275.0000000000000000, -39.79999999999905214, 12.19999999999906315 ) ) ;
#39416=FACE_OUTER_BOUND ( 'NONE', #28560, .T. ) ;
#39473=EDGE_CURVE ( 'NONE', #61891, #8330, #26217, .T. ) ;
#39476=ADVANCED_FACE ( 'NONE', ( #58409 ), #4998, .T. ) ;
#39478=FACE_OUTER_BOUND ( 'NONE', #62591, .T. ) ;
#39534=PLANE ( 'NONE',  #66318 ) ;
#39539=DIRECTION ( 'NONE',  ( 0.000000000000000000, 0.000000000000000000, -1.000000000000000000 ) ) ;
#39543=VERTEX_POINT ( 'NONE', #747 ) ;
#39544=ORIENTED_EDGE ( 'NONE', *, *, #17970, .F. ) ;
#39579=DIRECTION ( 'NONE',  ( -1.000000000000000000, 0.000000000000000000, 0.000000000000000000 ) ) ;
#39583=DIRECTION ( 'NONE',  ( -1.000000000000000000, 0.000000000000000000, 0.000000000000000000 ) ) ;
#39584=VERTEX_POINT ( 'NONE', #54491 ) ;
#39601=PLANE ( 'NONE',  #63612 ) ;
#39608=CARTESIAN_POINT ( 'NONE',  ( 283.0000000000000568, -38.15000000000000568, -13.19999999999999929 ) ) ;
#39618=ADVANCED_FACE ( 'NONE', ( #55855 ), #44197, .F. ) ;
#39621=DIRECTION ( 'NONE',  ( 0.000000000000000000, 1.000000000000000000, 0.000000000000000000 ) ) ;
#39626=ORIENTED_EDGE ( 'NONE', *, *, #13100, .F. ) ;
#39649=AXIS2_PLACEMENT_3D ( 'NONE', #32606, #53833, #69743 ) ;
#39651=CARTESIAN_POINT ( 'NONE',  ( 289.5000000000001705, -0.5000000000000781597, -27.00000000000004263 ) ) ;
#39657=DIRECTION ( 'NONE',  ( 0.000000000000000000, 0.000000000000000000, 1.000000000000000000 ) ) ;
#39669=FACE_OUTER_BOUND ( 'NONE', #49564, .T. ) ;
#39672=CARTESIAN_POINT ( 'NONE',  ( 7.000000000000000000, -31.99999999999889866, 7.899999999997660893 ) ) ;
#39686=CARTESIAN_POINT ( 'NONE',  ( 15.00000000000000000, -20.40000000000000213, -12.40000000000000213 ) ) ;
#39692=EDGE_CURVE ( 'NONE', #65388, #32021, #29671, .T. ) ;
#39699=CARTESIAN_POINT ( 'NONE',  ( 7.000000000000000000, -38.09999999999885034, -7.900000000002049383 ) ) ;
#39700=EDGE_CURVE ( 'NONE', #67984, #6255, #9169, .T. ) ;
#39707=CARTESIAN_POINT ( 'NONE',  ( 14.50000000000000000, -42.50000000000000000, 15.10000000000000142 ) ) ;
#39716=DIRECTION ( 'NONE',  ( 0.000000000000000000, 1.550842787525658429E-12, 1.000000000000000000 ) ) ;
#39720=VERTEX_POINT ( 'NONE', #67158 ) ;
#39730=CARTESIAN_POINT ( 'NONE',  ( 289.5000000000000000, 0.000000000000000000, -26.50000000000000000 ) ) ;
#39731=VERTEX_POINT ( 'NONE', #14113 ) ;
#39756=DIRECTION ( 'NONE',  ( 1.000000000000000000, -0.000000000000000000, -0.000000000000000000 ) ) ;
#39762=EDGE_CURVE ( 'NONE', #65808, #2847, #45137, .T. ) ;
#39763=ORIENTED_EDGE ( 'NONE', *, *, #29983, .F. ) ;
#39766=LINE ( 'NONE', #23518, #10500 ) ;
#39812=ORIENTED_EDGE ( 'NONE', *, *, #65488, .F. ) ;
#39831=DIRECTION ( 'NONE',  ( 0.000000000000000000, 0.000000000000000000, 1.000000000000000000 ) ) ;
#39836=CARTESIAN_POINT ( 'NONE',  ( 15.00000000000000000, -25.60000000000000142, 15.10000000000000142 ) ) ;
#39848=FACE_OUTER_BOUND ( 'NONE', #65981, .T. ) ;
#39868=ORIENTED_EDGE ( 'NONE', *, *, #6724, .F. ) ;
#39871=DIRECTION ( 'NONE',  ( 1.000000000000000000, -0.000000000000000000, -0.000000000000000000 ) ) ;
#39884=ORIENTED_EDGE ( 'NONE', *, *, #36428, .F. ) ;
#39885=EDGE_LOOP ( 'NONE', ( #11816, #44922, #52702, #48202, #1578, #12853 ) ) ;
#39890=AXIS2_PLACEMENT_3D ( 'NONE', #16311, #5715, #27283 ) ;
#39894=ORIENTED_EDGE ( 'NONE', *, *, #26281, .F. ) ;
#39898=AXIS2_PLACEMENT_3D ( 'NONE', #45721, #18862, #24524 ) ;
#39902=DIRECTION ( 'NONE',  ( 1.000000000000000000, -0.000000000000000000, -0.000000000000000000 ) ) ;
#39918=DIRECTION ( 'NONE',  ( -1.000000000000000000, 0.000000000000000000, 0.000000000000000000 ) ) ;
#39932=DIRECTION ( 'NONE',  ( 0.000000000000000000, -9.159339953149780582E-13, 1.000000000000000000 ) ) ;
#39957=CARTESIAN_POINT ( 'NONE',  ( 15.00000000000000000, -26.42999999999999972, -5.874955318979029784 ) ) ;
#39964=DIRECTION ( 'NONE',  ( 1.000000000000000000, -0.000000000000000000, -0.000000000000000000 ) ) ;
#39967=LINE ( 'NONE', #61533, #22842 ) ;
#40003=EDGE_CURVE ( 'NONE', #60826, #11772, #65514, .T. ) ;
#40044=DIRECTION ( 'NONE',  ( -1.000000000000000000, 0.000000000000000000, 0.000000000000000000 ) ) ;
#40048=LINE ( 'NONE', #61623, #28674 ) ;
#40061=ORIENTED_EDGE ( 'NONE', *, *, #50132, .T. ) ;
#40081=ORIENTED_EDGE ( 'NONE', *, *, #7013, .T. ) ;
#40091=VECTOR ( 'NONE', #62423, 1000.000000000000114 ) ;
#40096=AXIS2_PLACEMENT_3D ( 'NONE', #41026, #62590, #25127 ) ;
#40097=ORIENTED_EDGE ( 'NONE', *, *, #67843, .T. ) ;
#40104=EDGE_LOOP ( 'NONE', ( #63979, #53582, #31745, #28574, #68624, #10171, #27392, #26874, #1379, #49119, #27579, #43102, #69126, #64410, #55713, #54434, #8246, #58725, #10337, #52494, #68463, #54837, #32033, #9855, #58952, #48580, #9440, #9173, #9918, #18244 ) ) ;
#40108=DIRECTION ( 'NONE',  ( 0.000000000000000000, 1.000000000000000000, 0.000000000000000000 ) ) ;
#40119=CARTESIAN_POINT ( 'NONE',  ( 0.2500000000000000000, -0.2499999999999970302, 26.75000000000000000 ) ) ;
#40122=DIRECTION ( 'NONE',  ( 0.000000000000000000, 0.6666666666652433237, -0.7453559925012029908 ) ) ;
#40129=CARTESIAN_POINT ( 'NONE',  ( 283.0000000000000568, -32.00000000000000000, -8.400000000000000355 ) ) ;
#40134=EDGE_CURVE ( 'NONE', #8330, #47821, #34534, .T. ) ;
#40158=EDGE_LOOP ( 'NONE', ( #7976, #57977, #51888, #40837, #34043, #60964 ) ) ;
#40174=LINE ( 'NONE', #46183, #8681 ) ;
#40194=DIRECTION ( 'NONE',  ( -1.000000000000000000, 0.000000000000000000, 0.000000000000000000 ) ) ;
#40210=CARTESIAN_POINT ( 'NONE',  ( 276.8775010008008053, -53.81370849898476649, 17.50000000000000000 ) ) ;
#40217=CYLINDRICAL_SURFACE ( 'NONE', #14949, 0.5000000000009441337 ) ;
#40238=CONICAL_SURFACE ( 'NONE', #9779, 7.799999999999999822, 1.047197551196693555 ) ;
#40241=CARTESIAN_POINT ( 'NONE',  ( 7.000000000000000000, -40.30000000000000426, -8.900000000000000355 ) ) ;
#40243=ORIENTED_EDGE ( 'NONE', *, *, #37886, .T. ) ;
#40253=VERTEX_POINT ( 'NONE', #36650 ) ;
#40256=AXIS2_PLACEMENT_3D ( 'NONE', #66777, #17656, #44171 ) ;
#40270=ADVANCED_FACE ( 'NONE', ( #58219 ), #53285, .T. ) ;
#40275=CARTESIAN_POINT ( 'NONE',  ( 275.5000000000000000, -42.00000000000000000, -27.00000000000000000 ) ) ;
#40311=DIRECTION ( 'NONE',  ( 1.000000000000000000, -0.000000000000000000, -0.000000000000000000 ) ) ;
#40320=AXIS2_PLACEMENT_3D ( 'NONE', #61039, #66705, #33492 ) ;
#40332=DIRECTION ( 'NONE',  ( 0.000000000000000000, 0.000000000000000000, 1.000000000000000000 ) ) ;
#40348=DIRECTION ( 'NONE',  ( 0.000000000000000000, 0.000000000000000000, 1.000000000000000000 ) ) ;
#40360=CARTESIAN_POINT ( 'NONE',  ( 289.7500000000000000, -42.25000000000000000, -26.75000000000000000 ) ) ;
#40368=FACE_OUTER_BOUND ( 'NONE', #22811, .T. ) ;
#40372=LINE ( 'NONE', #67598, #31850 ) ;
#40377=DIRECTION ( 'NONE',  ( 0.000000000000000000, 0.000000000000000000, -1.000000000000000000 ) ) ;
#40382=VECTOR ( 'NONE', #5945, 1000.000000000000000 ) ;
#40429=ADVANCED_FACE ( 'NONE', ( #64925 ), #49366, .T. ) ;
#40434=VERTEX_POINT ( 'NONE', #3965 ) ;
#40449=LINE ( 'NONE', #67671, #39200 ) ;
#40460=DIRECTION ( 'NONE',  ( 0.000000000000000000, 0.000000000000000000, 1.000000000000000000 ) ) ;
#40470=CARTESIAN_POINT ( 'NONE',  ( 289.5000000000000000, 0.000000000000000000, 26.50000000000000000 ) ) ;
#40474=LINE ( 'NONE', #60657, #15078 ) ;
#40484=EDGE_LOOP ( 'NONE', ( #32141, #9578, #17962, #9206 ) ) ;
#40497=FACE_OUTER_BOUND ( 'NONE', #40158, .T. ) ;
#40499=ORIENTED_EDGE ( 'NONE', *, *, #49172, .F. ) ;
#40525=CIRCLE ( 'NONE', #10067, 4.000000000000000000 ) ;
#40557=DIRECTION ( 'NONE',  ( -1.000000000000000000, 0.000000000000000000, 0.000000000000000000 ) ) ;
#40578=ADVANCED_FACE ( 'NONE', ( #31889 ), #53459, .F. ) ;
#40583=ORIENTED_EDGE ( 'NONE', *, *, #46973, .T. ) ;
#40591=FACE_OUTER_BOUND ( 'NONE', #30896, .T. ) ;
#40595=CARTESIAN_POINT ( 'NONE',  ( 275.0000000000000000, -23.29603921945599865, 12.50000000000000000 ) ) ;
#40605=VERTEX_POINT ( 'NONE', #26935 ) ;
#40606=CARTESIAN_POINT ( 'NONE',  ( 289.5000000000000000, -42.00000000000000000, 27.00000000000000000 ) ) ;
#40623=CARTESIAN_POINT ( 'NONE',  ( 282.6457513110646005, -20.50000000000000000, 17.00000000000000000 ) ) ;
#40639=CARTESIAN_POINT ( 'NONE',  ( 283.0000000000000568, -32.46196062927499781, -8.091291340630698770 ) ) ;
#40653=AXIS2_PLACEMENT_3D ( 'NONE', #40715, #24458, #25518 ) ;
#40654=LINE ( 'NONE', #18377, #10146 ) ;
#40662=ORIENTED_EDGE ( 'NONE', *, *, #66259, .T. ) ;
#40692=DIRECTION ( 'NONE',  ( 1.000000000000000000, -0.000000000000000000, -0.000000000000000000 ) ) ;
#40693=LINE ( 'NONE', #25135, #54148 ) ;
#40696=VERTEX_POINT ( 'NONE', #17338 ) ;
#40699=VERTEX_POINT ( 'NONE', #1096 ) ;
#40700=VERTEX_POINT ( 'NONE', #61502 ) ;
#40704=VECTOR ( 'NONE', #33911, 1000.000000000000000 ) ;
#40715=CARTESIAN_POINT ( 'NONE',  ( 7.000000000000000000, -25.69999999999924967, 14.52500000000000213 ) ) ;
#40720=CARTESIAN_POINT ( 'NONE',  ( 0.2499999999999831524, -42.25000000000000000, 26.75000000000000711 ) ) ;
#40735=CIRCLE ( 'NONE', #18162, 4.000000000000000000 ) ;
#40767=AXIS2_PLACEMENT_3D ( 'NONE', #43522, #5011, #32922 ) ;
#40791=ORIENTED_EDGE ( 'NONE', *, *, #65651, .F. ) ;
#40793=FACE_OUTER_BOUND ( 'NONE', #26254, .T. ) ;
#40814=EDGE_CURVE ( 'NONE', #16097, #64136, #18144, .T. ) ;
#40828=DIRECTION ( 'NONE',  ( -0.5773502691896285066, 0.5773502691896243988, -0.5773502691896243988 ) ) ;
#40829=DIRECTION ( 'NONE',  ( 1.000000000000000000, 0.000000000000000000, 0.000000000000000000 ) ) ;
#40837=ORIENTED_EDGE ( 'NONE', *, *, #2713, .F. ) ;
#40848=ORIENTED_EDGE ( 'NONE', *, *, #2626, .F. ) ;
#40860=ORIENTED_EDGE ( 'NONE', *, *, #34233, .T. ) ;
#40867=DIRECTION ( 'NONE',  ( 0.000000000000000000, 0.7071067811865474617, -0.7071067811865474617 ) ) ;
#40884=ORIENTED_EDGE ( 'NONE', *, *, #29542, .T. ) ;
#40889=ADVANCED_FACE ( 'NONE', ( #67170 ), #63274, .F. ) ;
#40898=EDGE_CURVE ( 'NONE', #42657, #17601, #44137, .T. ) ;
#40921=CARTESIAN_POINT ( 'NONE',  ( 7.000000000000000000, -32.00000000000000000, 8.400000000000000355 ) ) ;
#40934=FACE_OUTER_BOUND ( 'NONE', #17828, .T. ) ;
#40942=CARTESIAN_POINT ( 'NONE',  ( 0.5000000000000000000, -42.50000000000000000, -27.00000000000000000 ) ) ;
#40996=CARTESIAN_POINT ( 'NONE',  ( 7.000000000000000000, -42.00000000000000000, 15.00000000000000000 ) ) ;
#41011=ORIENTED_EDGE ( 'NONE', *, *, #32813, .F. ) ;
#41024=DIRECTION ( 'NONE',  ( 0.000000000000000000, -0.6874999999999994449, 0.7261843774138911911 ) ) ;
#41025=CARTESIAN_POINT ( 'NONE',  ( 283.0000000000000568, -23.29603921945599865, 12.50000000000000000 ) ) ;
#41026=CARTESIAN_POINT ( 'NONE',  ( 275.0000000000000000, -38.09999999999885034, -7.900000000002049383 ) ) ;
#41029=ORIENTED_EDGE ( 'NONE', *, *, #7372, .F. ) ;
#41035=AXIS2_PLACEMENT_3D ( 'NONE', #38135, #49070, #21849 ) ;
#41037=EDGE_CURVE ( 'NONE', #49494, #58107, #23850, .T. ) ;
#41043=EDGE_CURVE ( 'NONE', #1462, #50319, #31110, .T. ) ;
#41044=CARTESIAN_POINT ( 'NONE',  ( 283.0000000000000568, -30.45000000000094786, -15.00000000000000000 ) ) ;
#41048=ADVANCED_FACE ( 'NONE', ( #21876 ), #43433, .F. ) ;
#41052=ORIENTED_EDGE ( 'NONE', *, *, #46963, .F. ) ;
#41057=VERTEX_POINT ( 'NONE', #58334 ) ;
#41060=DIRECTION ( 'NONE',  ( 0.000000000000000000, 0.7071067811865074937, 0.7071067811865876518 ) ) ;
#41084=VECTOR ( 'NONE', #69774, 1000.000000000000000 ) ;
#41086=EDGE_LOOP ( 'NONE', ( #45701, #56393, #10375, #49677, #43879, #23972 ) ) ;
#41088=ORIENTED_EDGE ( 'NONE', *, *, #7653, .T. ) ;
#41091=CARTESIAN_POINT ( 'NONE',  ( 275.0000000000000000, -20.50000000000000000, 13.00000000000000178 ) ) ;
#41101=ADVANCED_FACE ( 'NONE', ( #5965 ), #22575, .T. ) ;
#41107=EDGE_CURVE ( 'NONE', #15205, #30525, #61069, .T. ) ;
#41108=DIRECTION ( 'NONE',  ( 0.000000000000000000, 1.000000000000000000, 0.000000000000000000 ) ) ;
#41113=ORIENTED_EDGE ( 'NONE', *, *, #44079, .T. ) ;
#41118=ADVANCED_FACE ( 'NONE', ( #1679 ), #55104, .T. ) ;
#41143=LINE ( 'NONE', #4727, #8634 ) ;
#41159=PLANE ( 'NONE',  #58419 ) ;
#41160=LINE ( 'NONE', #8985, #44159 ) ;
#41163=ORIENTED_EDGE ( 'NONE', *, *, #47759, .F. ) ;
#41179=CARTESIAN_POINT ( 'NONE',  ( 275.4999999999998863, 2.842170943040400743E-14, -26.49999999999993250 ) ) ;
#41201=CARTESIAN_POINT ( 'NONE',  ( 7.000000000000000000, -29.94999999999999929, -14.50000000000000000 ) ) ;
#41219=AXIS2_PLACEMENT_3D ( 'NONE', #66434, #17984, #61112 ) ;
#41259=LINE ( 'NONE', #13692, #55953 ) ;
#41266=VECTOR ( 'NONE', #40867, 1000.000000000000114 ) ;
#41282=ADVANCED_FACE ( 'NONE', ( #24300 ), #19681, .T. ) ;
#41291=DIRECTION ( 'NONE',  ( 0.000000000000000000, 0.7071067811865475727, -0.7071067811865475727 ) ) ;
#41293=ORIENTED_EDGE ( 'NONE', *, *, #34095, .T. ) ;
#41311=LINE ( 'NONE', #15516, #23400 ) ;
#41335=DIRECTION ( 'NONE',  ( 0.000000000000000000, -1.000000000000000000, 0.000000000000000000 ) ) ;
#41344=VERTEX_POINT ( 'NONE', #14405 ) ;
#41347=VERTEX_POINT ( 'NONE', #51531 ) ;
#41355=ORIENTED_EDGE ( 'NONE', *, *, #23829, .F. ) ;
#41357=AXIS2_PLACEMENT_3D ( 'NONE', #58500, #14304, #30557 ) ;
#41363=AXIS2_PLACEMENT_3D ( 'NONE', #29670, #39579, #2457 ) ;
#41364=CIRCLE ( 'NONE', #56054, 3.999999999999993339 ) ;
#41369=ORIENTED_EDGE ( 'NONE', *, *, #68210, .F. ) ;
#41371=VECTOR ( 'NONE', #44609, 1000.000000000000000 ) ;
#41380=DIRECTION ( 'NONE',  ( 0.000000000000000000, 0.000000000000000000, 1.000000000000000000 ) ) ;
#41410=EDGE_LOOP ( 'NONE', ( #20008, #19935, #20674, #26538 ) ) ;
#41420=AXIS2_PLACEMENT_3D ( 'NONE', #57240, #57935, #30370 ) ;
#41444=CARTESIAN_POINT ( 'NONE',  ( 283.0000000000000568, -25.93000000000544958, -9.412893218815410634 ) ) ;
#41471=EDGE_CURVE ( 'NONE', #10448, #10609, #51974, .T. ) ;
#41475=VERTEX_POINT ( 'NONE', #59276 ) ;
#41487=ORIENTED_EDGE ( 'NONE', *, *, #28315, .T. ) ;
#41505=ORIENTED_EDGE ( 'NONE', *, *, #18365, .F. ) ;
#41506=VERTEX_POINT ( 'NONE', #52588 ) ;
#41513=ADVANCED_FACE ( 'NONE', ( #68846 ), #7248, .T. ) ;
#41515=CARTESIAN_POINT ( 'NONE',  ( 283.0000000000000568, -20.40000000000000213, 17.60000000000000142 ) ) ;
#41516=ORIENTED_EDGE ( 'NONE', *, *, #37707, .T. ) ;
#41530=ORIENTED_EDGE ( 'NONE', *, *, #413, .T. ) ;
#41578=ORIENTED_EDGE ( 'NONE', *, *, #6724, .T. ) ;
#41600=ADVANCED_FACE ( 'NONE', ( #55033 ), #49705, .T. ) ;
#41604=DIRECTION ( 'NONE',  ( -1.000000000000000000, 0.000000000000000000, 0.000000000000000000 ) ) ;
#41610=CARTESIAN_POINT ( 'NONE',  ( 14.50000000000000000, 0.000000000000000000, 26.50000000000000000 ) ) ;
#41624=AXIS2_PLACEMENT_3D ( 'NONE', #1887, #23457, #37383 ) ;
#41643=CARTESIAN_POINT ( 'NONE',  ( 7.000000000000000000, -26.28355339059299922, 9.766446609406699508 ) ) ;
#41648=CARTESIAN_POINT ( 'NONE',  ( 275.5000000000000000, 0.000000000000000000, 26.50000000000000000 ) ) ;
#41671=CARTESIAN_POINT ( 'NONE',  ( 283.0000000000000568, -38.15000000000000568, -13.19999999999999929 ) ) ;
#41709=DIRECTION ( 'NONE',  ( 0.000000000000000000, -0.7071067811865475727, -0.7071067811865475727 ) ) ;
#41721=VERTEX_POINT ( 'NONE', #40119 ) ;
#41724=DIRECTION ( 'NONE',  ( 0.000000000000000000, -1.000000000000000000, 0.000000000000000000 ) ) ;
#41742=ORIENTED_EDGE ( 'NONE', *, *, #59029, .T. ) ;
#41787=EDGE_CURVE ( 'NONE', #16822, #54243, #67363, .T. ) ;
#41804=ORIENTED_EDGE ( 'NONE', *, *, #8341, .F. ) ;
#41820=EDGE_LOOP ( 'NONE', ( #15855, #19352, #18590, #53103 ) ) ;
#41825=CARTESIAN_POINT ( 'NONE',  ( 283.0000000000000568, -30.45000000000000639, 15.00000000000000000 ) ) ;
#41834=ORIENTED_EDGE ( 'NONE', *, *, #12216, .T. ) ;
#41856=DIRECTION ( 'NONE',  ( 0.000000000000000000, 0.000000000000000000, -1.000000000000000000 ) ) ;
#41861=DIRECTION ( 'NONE',  ( 0.000000000000000000, 0.000000000000000000, -1.000000000000000000 ) ) ;
#41926=CARTESIAN_POINT ( 'NONE',  ( 275.0000000000000000, -25.69999999999924967, -14.52500000000000213 ) ) ;
#41960=VECTOR ( 'NONE', #3322, 1000.000000000000000 ) ;
#41966=DIRECTION ( 'NONE',  ( 1.000000000000000000, 0.000000000000000000, 0.000000000000000000 ) ) ;
#41973=AXIS2_PLACEMENT_3D ( 'NONE', #48132, #37182, #58741 ) ;
#41983=AXIS2_PLACEMENT_3D ( 'NONE', #3803, #61173, #50587 ) ;
#41991=EDGE_CURVE ( 'NONE', #18752, #288, #29395, .T. ) ;
#41996=ADVANCED_FACE ( 'NONE', ( #8523 ), #50969, .F. ) ;
#42004=EDGE_LOOP ( 'NONE', ( #10429, #33993 ) ) ;
#42006=ORIENTED_EDGE ( 'NONE', *, *, #64279, .F. ) ;
#42014=VECTOR ( 'NONE', #19127, 1000.000000000000000 ) ;
#42019=VERTEX_POINT ( 'NONE', #68645 ) ;
#42028=VERTEX_POINT ( 'NONE', #31521 ) ;
#42033=CARTESIAN_POINT ( 'NONE',  ( 7.000000000000000000, -39.80000000000000426, -8.400000000000000355 ) ) ;
#42043=EDGE_CURVE ( 'NONE', #16486, #57476, #42808, .T. ) ;
#42052=CARTESIAN_POINT ( 'NONE',  ( 7.000000000000000000, -38.15000000000000568, 13.19999999999999929 ) ) ;
#42054=ORIENTED_EDGE ( 'NONE', *, *, #67843, .F. ) ;
#42064=EDGE_LOOP ( 'NONE', ( #24445, #22179, #20951, #21194 ) ) ;
#42067=AXIS2_PLACEMENT_3D ( 'NONE', #44376, #21444, #1268 ) ;
#42088=ORIENTED_EDGE ( 'NONE', *, *, #35976, .F. ) ;
#42097=VECTOR ( 'NONE', #52017, 1000.000000000000000 ) ;
#42117=DIRECTION ( 'NONE',  ( 0.000000000000000000, -1.000000000000000000, 0.000000000000000000 ) ) ;
#42130=VERTEX_POINT ( 'NONE', #64050 ) ;
#42136=DIRECTION ( 'NONE',  ( -1.000000000000000000, 0.000000000000000000, 0.000000000000000000 ) ) ;
#42155=CARTESIAN_POINT ( 'NONE',  ( 283.0000000000000568, -38.15000000000000568, -14.50000000000000000 ) ) ;
#42158=CARTESIAN_POINT ( 'NONE',  ( 7.000000000000000000, -42.00000000000000000, -7.000000000000000000 ) ) ;
#42167=CARTESIAN_POINT ( 'NONE',  ( 7.000000000000000000, -17.00000000000000000, 0.000000000000000000 ) ) ;
#42175=ORIENTED_EDGE ( 'NONE', *, *, #34401, .F. ) ;
#42177=VERTEX_POINT ( 'NONE', #18003 ) ;
#42192=CIRCLE ( 'NONE', #1500, 4.000000000000000000 ) ;
#42213=CARTESIAN_POINT ( 'NONE',  ( 289.5000000000001705, 6.039613253960851580E-14, 26.49999999999996092 ) ) ;
#42214=CARTESIAN_POINT ( 'NONE',  ( 277.3542486889354564, -25.50000000000000355, 17.00000000000000000 ) ) ;
#42251=EDGE_CURVE ( 'NONE', #3076, #69116, #65425, .T. ) ;
#42267=DIRECTION ( 'NONE',  ( -1.000000000000000000, 0.000000000000000000, 0.000000000000000000 ) ) ;
#42270=LINE ( 'NONE', #36270, #67211 ) ;
#42276=ORIENTED_EDGE ( 'NONE', *, *, #9444, .T. ) ;
#42289=PLANE ( 'NONE',  #35513 ) ;
#42291=CARTESIAN_POINT ( 'NONE',  ( 290.0000000000000000, -0.5000000000000000000, 27.00000000000000000 ) ) ;
#42310=VERTEX_POINT ( 'NONE', #48822 ) ;
#42327=ADVANCED_FACE ( 'NONE', ( #54563 ), #16373, .F. ) ;
#42328=DIRECTION ( 'NONE',  ( 0.000000000000000000, 0.7071067811865480168, 0.7071067811865470176 ) ) ;
#42362=DIRECTION ( 'NONE',  ( 0.000000000000000000, 1.000000000000000000, 0.000000000000000000 ) ) ;
#42367=ORIENTED_EDGE ( 'NONE', *, *, #49592, .F. ) ;
#42376=VERTEX_POINT ( 'NONE', #5774 ) ;
#42378=DIRECTION ( 'NONE',  ( 0.000000000000000000, 0.000000000000000000, -1.000000000000000000 ) ) ;
#42407=VECTOR ( 'NONE', #23213, 1000.000000000000000 ) ;
#42440=VECTOR ( 'NONE', #43009, 1000.000000000000000 ) ;
#42450=VECTOR ( 'NONE', #6196, 1000.000000000000000 ) ;
#42464=ADVANCED_FACE ( 'NONE', ( #44966 ), #23051, .T. ) ;
#42471=DIRECTION ( 'NONE',  ( 1.000000000000000000, -0.000000000000000000, -0.000000000000000000 ) ) ;
#42480=CARTESIAN_POINT ( 'NONE',  ( 7.000000000000000000, -31.30000000000045191, 8.900000000000430234 ) ) ;
#42484=VERTEX_POINT ( 'NONE', #46019 ) ;
#42560=LINE ( 'NONE', #64150, #13581 ) ;
#42571=ORIENTED_EDGE ( 'NONE', *, *, #67182, .T. ) ;
#42596=AXIS2_PLACEMENT_3D ( 'NONE', #16460, #11482, #50007 ) ;
#42610=CARTESIAN_POINT ( 'NONE',  ( 7.000000000000000000, -23.50007830495750127, 12.28007262201345995 ) ) ;
#42630=CARTESIAN_POINT ( 'NONE',  ( 277.0217896459287203, -25.18021646000301317, -17.31978353999699749 ) ) ;
#42635=DIRECTION ( 'NONE',  ( -1.000000000000000000, 0.000000000000000000, 0.000000000000000000 ) ) ;
#42647=CARTESIAN_POINT ( 'NONE',  ( 283.0000000000000568, -26.50000000000000000, -9.080000000000000071 ) ) ;
#42648=CARTESIAN_POINT ( 'NONE',  ( 275.0000000000000000, -38.15000000000000568, -14.50000000000000000 ) ) ;
#42657=VERTEX_POINT ( 'NONE', #24802 ) ;
#42674=ORIENTED_EDGE ( 'NONE', *, *, #32593, .F. ) ;
#42679=CARTESIAN_POINT ( 'NONE',  ( 283.0000000000000568, -25.69999999999924967, 14.52500000000000213 ) ) ;
#42687=CARTESIAN_POINT ( 'NONE',  ( 283.0000000000000568, -30.80000000000000071, -8.900000000000000355 ) ) ;
#42688=AXIS2_PLACEMENT_3D ( 'NONE', #6661, #27542, #44139 ) ;
#42701=EDGE_CURVE ( 'NONE', #15923, #56899, #1343, .T. ) ;
#42712=ORIENTED_EDGE ( 'NONE', *, *, #65503, .T. ) ;
#42713=DIRECTION ( 'NONE',  ( 0.000000000000000000, 0.000000000000000000, 1.000000000000000000 ) ) ;
#42723=ORIENTED_EDGE ( 'NONE', *, *, #29993, .T. ) ;
#42731=EDGE_CURVE ( 'NONE', #56899, #16486, #9524, .T. ) ;
#42735=CARTESIAN_POINT ( 'NONE',  ( 7.000000000000000000, -25.60000000000000142, -15.10000000000000142 ) ) ;
#42761=ORIENTED_EDGE ( 'NONE', *, *, #26782, .T. ) ;
#42767=EDGE_CURVE ( 'NONE', #22636, #32305, #10987, .T. ) ;
#42783=DIRECTION ( 'NONE',  ( 0.000000000000000000, -1.000000000000000000, 3.819861094142539476E-12 ) ) ;
#42787=EDGE_CURVE ( 'NONE', #15647, #55647, #59769, .T. ) ;
#42790=CARTESIAN_POINT ( 'NONE',  ( 283.0000000000000568, -31.30000000000045191, 8.400000000000000355 ) ) ;
#42798=ORIENTED_EDGE ( 'NONE', *, *, #29200, .T. ) ;
#42803=CARTESIAN_POINT ( 'NONE',  ( 7.000000000000000000, -32.45000000000000995, -12.69999999999999929 ) ) ;
#42805=VECTOR ( 'NONE', #63882, 1000.000000000000000 ) ;
#42808=LINE ( 'NONE', #58735, #33933 ) ;
#42810=ORIENTED_EDGE ( 'NONE', *, *, #7230, .T. ) ;
#42851=ORIENTED_EDGE ( 'NONE', *, *, #34684, .T. ) ;
#42856=VECTOR ( 'NONE', #65288, 1000.000000000000000 ) ;
#42892=AXIS2_PLACEMENT_3D ( 'NONE', #63632, #15883, #37456 ) ;
#42911=DIRECTION ( 'NONE',  ( 0.000000000000000000, -0.7071067811865475727, 0.7071067811865475727 ) ) ;
#42944=ORIENTED_EDGE ( 'NONE', *, *, #67182, .F. ) ;
#42966=CARTESIAN_POINT ( 'NONE',  ( 283.0000000000000568, -26.28355339059299922, 9.766446609406699508 ) ) ;
#42975=AXIS2_PLACEMENT_3D ( 'NONE', #7374, #17990, #18329 ) ;
#42977=ORIENTED_EDGE ( 'NONE', *, *, #62939, .T. ) ;
#42980=DIRECTION ( 'NONE',  ( 0.000000000000000000, -1.000000000000000000, 0.000000000000000000 ) ) ;
#42996=CARTESIAN_POINT ( 'NONE',  ( 290.0000000000000000, 50.00000000000000000, 26.50000000000000000 ) ) ;
#43003=VECTOR ( 'NONE', #39918, 1000.000000000000000 ) ;
#43004=DIRECTION ( 'NONE',  ( -1.000000000000000000, 0.000000000000000000, 0.000000000000000000 ) ) ;
#43006=EDGE_LOOP ( 'NONE', ( #60450, #8187, #33977, #30808 ) ) ;
#43009=DIRECTION ( 'NONE',  ( 0.000000000000000000, 0.000000000000000000, -1.000000000000000000 ) ) ;
#43011=CARTESIAN_POINT ( 'NONE',  ( 275.0000000000000000, -21.00000000000000000, 5.000000000000000000 ) ) ;
#43044=CIRCLE ( 'NONE', #46420, 0.4999999999979551912 ) ;
#43049=DIRECTION ( 'NONE',  ( 0.000000000000000000, 0.000000000000000000, -1.000000000000000000 ) ) ;
#43064=DIRECTION ( 'NONE',  ( 0.000000000000000000, 0.000000000000000000, -1.000000000000000000 ) ) ;
#43066=ADVANCED_FACE ( 'NONE', ( #31443 ), #9870, .T. ) ;
#43102=ORIENTED_EDGE ( 'NONE', *, *, #66179, .T. ) ;
#43120=VECTOR ( 'NONE', #25602, 1000.000000000000000 ) ;
#43134=CARTESIAN_POINT ( 'NONE',  ( 283.0000000000000568, -25.00000000000299849, -9.079999998829670460 ) ) ;
#43139=DIRECTION ( 'NONE',  ( 0.000000000000000000, 1.000000000000000000, 0.000000000000000000 ) ) ;
#43144=DIRECTION ( 'NONE',  ( 0.000000000000000000, 0.000000000000000000, -1.000000000000000000 ) ) ;
#43188=VERTEX_POINT ( 'NONE', #11566 ) ;
#43213=ORIENTED_EDGE ( 'NONE', *, *, #52783, .T. ) ;
#43226=VECTOR ( 'NONE', #24446, 1000.000000000000114 ) ;
#43231=FACE_OUTER_BOUND ( 'NONE', #32982, .T. ) ;
#43240=DIRECTION ( 'NONE',  ( -1.000000000000000000, 0.000000000000000000, 0.000000000000000000 ) ) ;
#43249=CARTESIAN_POINT ( 'NONE',  ( 283.0000000000000568, -30.80000000000000071, -12.20000000000000107 ) ) ;
#43255=DIRECTION ( 'NONE',  ( 1.000000000000000000, -0.000000000000000000, -0.000000000000000000 ) ) ;
#43257=AXIS2_PLACEMENT_3D ( 'NONE', #62560, #3540, #51973 ) ;
#43278=VECTOR ( 'NONE', #64767, 1000.000000000000000 ) ;
#43280=CARTESIAN_POINT ( 'NONE',  ( 7.000000000000000000, -26.06132420600899735, 10.13999572156699891 ) ) ;
#43293=VECTOR ( 'NONE', #33894, 1000.000000000000000 ) ;
#43310=VECTOR ( 'NONE', #13265, 1000.000000000000114 ) ;
#43322=DIRECTION ( 'NONE',  ( -1.000000000000000000, 0.000000000000000000, 0.000000000000000000 ) ) ;
#43325=DIRECTION ( 'NONE',  ( 0.000000000000000000, 0.000000000000000000, 1.000000000000000000 ) ) ;
#43334=LINE ( 'NONE', #53969, #25715 ) ;
#43339=EDGE_CURVE ( 'NONE', #48215, #51726, #28372, .T. ) ;
#43348=ORIENTED_EDGE ( 'NONE', *, *, #1750, .F. ) ;
#43398=ORIENTED_EDGE ( 'NONE', *, *, #27545, .T. ) ;
#43406=LINE ( 'NONE', #49065, #12289 ) ;
#43418=CARTESIAN_POINT ( 'NONE',  ( 275.0000000000000000, -31.30000000000045191, -8.900000000000430234 ) ) ;
#43433=CYLINDRICAL_SURFACE ( 'NONE', #2, 0.4999999999979829468 ) ;
#43455=DIRECTION ( 'NONE',  ( -1.000000000000000000, 0.000000000000000000, 0.000000000000000000 ) ) ;
#43464=ORIENTED_EDGE ( 'NONE', *, *, #14685, .F. ) ;
#43466=CARTESIAN_POINT ( 'NONE',  ( 14.75000000000000178, -0.2500000000000000000, -26.75000000000000000 ) ) ;
#43469=AXIS2_PLACEMENT_3D ( 'NONE', #7138, #44979, #28717 ) ;
#43480=EDGE_LOOP ( 'NONE', ( #893, #4638, #42088, #55403 ) ) ;
#43491=AXIS2_PLACEMENT_3D ( 'NONE', #50437, #1998, #24259 ) ;
#43492=VECTOR ( 'NONE', #26841, 1000.000000000000000 ) ;
#43509=ADVANCED_FACE ( 'NONE', ( #60887 ), #55600, .F. ) ;
#43522=CARTESIAN_POINT ( 'NONE',  ( 0.000000000000000000, -42.00000000000000000, 30.00000000000000000 ) ) ;
#43534=ORIENTED_EDGE ( 'NONE', *, *, #45316, .T. ) ;
#43552=LINE ( 'NONE', #1799, #28101 ) ;
#43573=ORIENTED_EDGE ( 'NONE', *, *, #69644, .F. ) ;
#43595=CIRCLE ( 'NONE', #52642, 0.5000000000009284795 ) ;
#43596=DIRECTION ( 'NONE',  ( 0.000000000000000000, 0.000000000000000000, -1.000000000000000000 ) ) ;
#43604=AXIS2_PLACEMENT_3D ( 'NONE', #45595, #34283, #39932 ) ;
#43634=LINE ( 'NONE', #38334, #20928 ) ;
#43643=CARTESIAN_POINT ( 'NONE',  ( 275.0000000000000000, -32.95000000000000284, 7.700000000000000178 ) ) ;
#43650=CIRCLE ( 'NONE', #8660, 4.000000000000000000 ) ;
#43660=CIRCLE ( 'NONE', #21092, 0.4999999999945519691 ) ;
#43663=ORIENTED_EDGE ( 'NONE', *, *, #65264, .T. ) ;
#43664=ORIENTED_EDGE ( 'NONE', *, *, #61279, .F. ) ;
#43665=VERTEX_POINT ( 'NONE', #53448 ) ;
#43667=VECTOR ( 'NONE', #16527, 1000.000000000000000 ) ;
#43683=ORIENTED_EDGE ( 'NONE', *, *, #46389, .F. ) ;
#43725=ORIENTED_EDGE ( 'NONE', *, *, #51056, .T. ) ;
#43730=CARTESIAN_POINT ( 'NONE',  ( 283.0000000000000568, -20.85424868893542438, -17.35424868893542438 ) ) ;
#43737=LINE ( 'NONE', #33117, #48969 ) ;
#43750=PLANE ( 'NONE',  #19446 ) ;
#43754=AXIS2_PLACEMENT_3D ( 'NONE', #15688, #64141, #53519 ) ;
#43767=EDGE_CURVE ( 'NONE', #62902, #18763, #32277, .T. ) ;
#43787=PLANE ( 'NONE',  #46002 ) ;
#43811=EDGE_CURVE ( 'NONE', #38349, #27791, #12014, .T. ) ;
#43813=CYLINDRICAL_SURFACE ( 'NONE', #44576, 0.5000000000009320322 ) ;
#43824=CARTESIAN_POINT ( 'NONE',  ( 15.00000000000000000, -26.42999999999999972, 5.874955318979029784 ) ) ;
#43838=CARTESIAN_POINT ( 'NONE',  ( 275.0000000000000000, -0.5000000000000000000, 26.50000000000000000 ) ) ;
#43858=CARTESIAN_POINT ( 'NONE',  ( 283.0000000000000568, -25.93000000000544958, 9.412893218815410634 ) ) ;
#43865=CARTESIAN_POINT ( 'NONE',  ( 282.8893988437589542, -25.27116123426317884, 17.22883876573682826 ) ) ;
#43877=CARTESIAN_POINT ( 'NONE',  ( 283.0000000000000568, -37.15000000000001279, 7.700000000000000178 ) ) ;
#43879=ORIENTED_EDGE ( 'NONE', *, *, #22222, .F. ) ;
#43914=LINE ( 'NONE', #6446, #7121 ) ;
#43919=CARTESIAN_POINT ( 'NONE',  ( 0.000000000000000000, 0.000000000000000000, 0.000000000000000000 ) ) ;
#43920=VERTEX_POINT ( 'NONE', #25432 ) ;
#43927=CARTESIAN_POINT ( 'NONE',  ( 7.000000000000000000, -20.49999999999999645, -16.03137303340311348 ) ) ;
#43938=LINE ( 'NONE', #54918, #48577 ) ;
#43941=CARTESIAN_POINT ( 'NONE',  ( 277.0217896459287203, -20.81978353999699749, -17.31978353999699749 ) ) ;
#43948=CARTESIAN_POINT ( 'NONE',  ( 7.000000000000000000, -20.50000000000000000, -17.00000000000000000 ) ) ;
#43964=DIRECTION ( 'NONE',  ( 0.000000000000000000, -1.000000000000000000, 0.000000000000000000 ) ) ;
#44006=ORIENTED_EDGE ( 'NONE', *, *, #7346, .F. ) ;
#44032=LINE ( 'NONE', #61326, #7357 ) ;
#44039=AXIS2_PLACEMENT_3D ( 'NONE', #31795, #63623, #21519 ) ;
#44042=EDGE_LOOP ( 'NONE', ( #10669, #215, #52960, #24290 ) ) ;
#44044=DIRECTION ( 'NONE',  ( 0.000000000000000000, 1.000000000000000000, 0.000000000000000000 ) ) ;
#44066=ADVANCED_FACE ( 'NONE', ( #21184 ), #31797, .F. ) ;
#44075=VERTEX_POINT ( 'NONE', #23242 ) ;
#44079=EDGE_CURVE ( 'NONE', #34291, #46362, #44453, .T. ) ;
#44081=VERTEX_POINT ( 'NONE', #39836 ) ;
#44129=CARTESIAN_POINT ( 'NONE',  ( 14.74999999999998046, -42.24999999999999289, -26.74999999999998934 ) ) ;
#44134=VERTEX_POINT ( 'NONE', #39166 ) ;
#44137=CIRCLE ( 'NONE', #13654, 0.5000000000023396840 ) ;
#44139=DIRECTION ( 'NONE',  ( 0.000000000000000000, -1.901256929667036381E-12, 1.000000000000000000 ) ) ;
#44145=CARTESIAN_POINT ( 'NONE',  ( 7.000000000000000000, -38.64999999999999858, -12.69999999999999929 ) ) ;
#44158=DIRECTION ( 'NONE',  ( 0.000000000000000000, 0.000000000000000000, 1.000000000000000000 ) ) ;
#44159=VECTOR ( 'NONE', #24562, 1000.000000000000114 ) ;
#44164=ORIENTED_EDGE ( 'NONE', *, *, #56847, .T. ) ;
#44171=DIRECTION ( 'NONE',  ( 0.000000000000000000, 0.000000000000000000, 1.000000000000000000 ) ) ;
#44172=CARTESIAN_POINT ( 'NONE',  ( 275.0000000000000000, -38.65000000000095781, -14.49999999999903899 ) ) ;
#44176=CARTESIAN_POINT ( 'NONE',  ( 290.0000000000000000, -42.50000000000000000, -27.00000000000000000 ) ) ;
#44177=VECTOR ( 'NONE', #7828, 1000.000000000000000 ) ;
#44179=ADVANCED_FACE ( 'NONE', ( #67774 ), #24995, .F. ) ;
#44197=CYLINDRICAL_SURFACE ( 'NONE', #57520, 1.999999999999312994 ) ;
#44205=CIRCLE ( 'NONE', #49817, 0.9999999999984534593 ) ;
#44211=DIRECTION ( 'NONE',  ( 0.000000000000000000, 1.000000000000000000, 0.000000000000000000 ) ) ;
#44254=ORIENTED_EDGE ( 'NONE', *, *, #23728, .F. ) ;
#44279=ORIENTED_EDGE ( 'NONE', *, *, #44954, .T. ) ;
#44302=CARTESIAN_POINT ( 'NONE',  ( 7.000000000000000000, -42.00000000000000000, 7.000000000000000000 ) ) ;
#44333=ORIENTED_EDGE ( 'NONE', *, *, #49989, .F. ) ;
#44338=EDGE_LOOP ( 'NONE', ( #58600, #22095 ) ) ;
#44342=FACE_OUTER_BOUND ( 'NONE', #28550, .T. ) ;
#44349=CARTESIAN_POINT ( 'NONE',  ( 275.0000000000000000, -39.79999999999954952, 8.900000000000419575 ) ) ;
#44360=EDGE_CURVE ( 'NONE', #53303, #40434, #21435, .T. ) ;
#44376=CARTESIAN_POINT ( 'NONE',  ( 7.000000000000000000, -25.60000000000000142, -17.60000000000000142 ) ) ;
#44390=AXIS2_PLACEMENT_3D ( 'NONE', #35691, #8833, #9190 ) ;
#44391=CIRCLE ( 'NONE', #13928, 0.2999999999994937827 ) ;
#44419=DIRECTION ( 'NONE',  ( 0.000000000000000000, 0.000000000000000000, -1.000000000000000000 ) ) ;
#44424=ORIENTED_EDGE ( 'NONE', *, *, #5256, .F. ) ;
#44453=LINE ( 'NONE', #44803, #4066 ) ;
#44461=CARTESIAN_POINT ( 'NONE',  ( 275.0000000000000000, -42.00000000000000000, 26.50000000000000000 ) ) ;
#44464=ORIENTED_EDGE ( 'NONE', *, *, #56932, .F. ) ;
#44466=EDGE_CURVE ( 'NONE', #54250, #58687, #44032, .T. ) ;
#44491=AXIS2_PLACEMENT_3D ( 'NONE', #18154, #12157, #39716 ) ;
#44498=CIRCLE ( 'NONE', #20794, 1.499999999997024602 ) ;
#44501=EDGE_LOOP ( 'NONE', ( #58171, #5955, #66755, #35920, #16357, #27894, #22590 ) ) ;
#44517=EDGE_CURVE ( 'NONE', #42310, #65332, #68357, .T. ) ;
#44518=DIRECTION ( 'NONE',  ( 0.000000000000000000, -0.5017180897718488408, -0.8650311892618017806 ) ) ;
#44539=LINE ( 'NONE', #17686, #5098 ) ;
#44568=VERTEX_POINT ( 'NONE', #4057 ) ;
#44575=LINE ( 'NONE', #55553, #12737 ) ;
#44576=AXIS2_PLACEMENT_3D ( 'NONE', #38178, #32525, #1038 ) ;
#44582=VERTEX_POINT ( 'NONE', #57085 ) ;
#44593=CIRCLE ( 'NONE', #31105, 1.999999999999314770 ) ;
#44603=LINE ( 'NONE', #39651, #10893 ) ;
#44609=DIRECTION ( 'NONE',  ( -0.000000000000000000, -1.000000000000000000, -0.000000000000000000 ) ) ;
#44621=ORIENTED_EDGE ( 'NONE', *, *, #58200, .F. ) ;
#44630=AXIS2_PLACEMENT_3D ( 'NONE', #23596, #12629, #28220 ) ;
#44649=DIRECTION ( 'NONE',  ( 0.000000000000000000, -0.9239212585478484563, -0.3825826812642726948 ) ) ;
#44655=LINE ( 'NONE', #17804, #24865 ) ;
#44659=EDGE_CURVE ( 'NONE', #40699, #16092, #36941, .T. ) ;
#44664=ORIENTED_EDGE ( 'NONE', *, *, #33454, .F. ) ;
#44677=EDGE_LOOP ( 'NONE', ( #53872, #52266, #64418, #6226 ) ) ;
#44685=ORIENTED_EDGE ( 'NONE', *, *, #47759, .T. ) ;
#44701=ORIENTED_EDGE ( 'NONE', *, *, #5564, .F. ) ;
#44710=DIRECTION ( 'NONE',  ( 0.000000000000000000, -0.7071067811865480168, 0.7071067811865470176 ) ) ;
#44711=PLANE ( 'NONE',  #27393 ) ;
#44713=ORIENTED_EDGE ( 'NONE', *, *, #69132, .T. ) ;
#44721=DIRECTION ( 'NONE',  ( 0.000000000000000000, 0.7071067811865074937, 0.7071067811865876518 ) ) ;
#44729=AXIS2_PLACEMENT_3D ( 'NONE', #12484, #7874, #2583 ) ;
#44735=ORIENTED_EDGE ( 'NONE', *, *, #52442, .F. ) ;
#44741=VECTOR ( 'NONE', #6, 1000.000000000000000 ) ;
#44758=CARTESIAN_POINT ( 'NONE',  ( 283.0000000000000568, -20.40000000000000213, -12.40000000000000213 ) ) ;
#44773=CARTESIAN_POINT ( 'NONE',  ( 283.0000000000000568, -32.95000000000000284, -14.50000000000000000 ) ) ;
#44779=AXIS2_PLACEMENT_3D ( 'NONE', #19963, #66998, #24920 ) ;
#44799=ADVANCED_FACE ( 'NONE', ( #23079 ), #60217, .F. ) ;
#44803=CARTESIAN_POINT ( 'NONE',  ( 283.0000000000000568, -25.56180396883900130, -14.25872597390799967 ) ) ;
#44805=DIRECTION ( 'NONE',  ( 1.000000000000000000, 0.000000000000000000, 0.000000000000000000 ) ) ;
#44813=DIRECTION ( 'NONE',  ( 0.000000000000000000, 1.000000000000000000, 0.000000000000000000 ) ) ;
#44815=PLANE ( 'NONE',  #677 ) ;
#44857=PLANE ( 'NONE',  #41219 ) ;
#44867=PLANE ( 'NONE',  #26704 ) ;
#44873=CARTESIAN_POINT ( 'NONE',  ( 7.000000000000000000, -27.13000000000000611, -15.49999999999930012 ) ) ;
#44886=EDGE_CURVE ( 'NONE', #33439, #45646, #13165, .T. ) ;
#44891=AXIS2_PLACEMENT_3D ( 'NONE', #28185, #38130, #988 ) ;
#44893=LINE ( 'NONE', #13760, #31976 ) ;
#44917=DIRECTION ( 'NONE',  ( -1.000000000000000000, 0.000000000000000000, 0.000000000000000000 ) ) ;
#44922=ORIENTED_EDGE ( 'NONE', *, *, #17652, .T. ) ;
#44927=CARTESIAN_POINT ( 'NONE',  ( 15.00000000000000000, -20.40000000000000213, -17.60000000000000142 ) ) ;
#44933=DIRECTION ( 'NONE',  ( -1.000000000000000000, 0.000000000000000000, 0.000000000000000000 ) ) ;
#44938=CARTESIAN_POINT ( 'NONE',  ( 7.000000000000000000, -21.00000000000000000, 0.000000000000000000 ) ) ;
#44954=EDGE_CURVE ( 'NONE', #66792, #13533, #21198, .T. ) ;
#44956=LINE ( 'NONE', #50613, #48984 ) ;
#44966=FACE_OUTER_BOUND ( 'NONE', #51000, .T. ) ;
#44969=DIRECTION ( 'NONE',  ( 0.000000000000000000, 0.000000000000000000, 1.000000000000000000 ) ) ;
#44972=FACE_OUTER_BOUND ( 'NONE', #62198, .T. ) ;
#44979=DIRECTION ( 'NONE',  ( 0.7071067811865475727, -0.7071067811865475727, 0.000000000000000000 ) ) ;
#44982=CARTESIAN_POINT ( 'NONE',  ( 7.500000000000000000, -25.60000000000000142, -20.00000000000000000 ) ) ;
#44995=VERTEX_POINT ( 'NONE', #65706 ) ;
#44998=PLANE ( 'NONE',  #67424 ) ;
#45028=ORIENTED_EDGE ( 'NONE', *, *, #13739, .F. ) ;
#45042=FACE_BOUND ( 'NONE', #41820, .T. ) ;
#45058=CARTESIAN_POINT ( 'NONE',  ( 275.0000000000000000, -32.94999999999885176, 8.199999999997979572 ) ) ;
#45060=ADVANCED_FACE ( 'NONE', ( #56138 ), #44815, .T. ) ;
#45083=CARTESIAN_POINT ( 'NONE',  ( 283.0000000000000568, -31.30000000000000071, -12.69999999999999929 ) ) ;
#45098=PLANE ( 'NONE',  #54932 ) ;
#45105=CIRCLE ( 'NONE', #16865, 0.3000000000005387246 ) ;
#45110=ORIENTED_EDGE ( 'NONE', *, *, #57868, .T. ) ;
#45118=ORIENTED_EDGE ( 'NONE', *, *, #54549, .F. ) ;
#45120=CARTESIAN_POINT ( 'NONE',  ( 289.5000000000000000, -42.50000000000000000, -26.50000000000000000 ) ) ;
#45136=CARTESIAN_POINT ( 'NONE',  ( 280.0000000000000000, -25.60000000000000142, -16.00000000000000711 ) ) ;
#45137=CIRCLE ( 'NONE', #44039, 0.5000000000009302559 ) ;
#45138=ADVANCED_FACE ( 'NONE', ( #39848 ), #66036, .T. ) ;
#45144=CARTESIAN_POINT ( 'NONE',  ( 15.00000000000000000, -21.00000000000000000, 5.000000000000000000 ) ) ;
#45155=ORIENTED_EDGE ( 'NONE', *, *, #48918, .F. ) ;
#45174=ORIENTED_EDGE ( 'NONE', *, *, #2176, .F. ) ;
#45175=DIRECTION ( 'NONE',  ( 0.000000000000000000, -9.159339953149780582E-13, 1.000000000000000000 ) ) ;
#45184=EDGE_CURVE ( 'NONE', #61271, #47033, #67083, .T. ) ;
#45187=AXIS2_PLACEMENT_3D ( 'NONE', #65609, #17164, #38728 ) ;
#45198=EDGE_CURVE ( 'NONE', #8330, #8968, #63184, .T. ) ;
#45200=FACE_OUTER_BOUND ( 'NONE', #21286, .T. ) ;
#45203=ORIENTED_EDGE ( 'NONE', *, *, #67542, .F. ) ;
#45211=CARTESIAN_POINT ( 'NONE',  ( 14.50000000000000000, -0.4999999999999923950, -27.00000000000000711 ) ) ;
#45219=DIRECTION ( 'NONE',  ( -1.000000000000000000, 0.000000000000000000, 0.000000000000000000 ) ) ;
#45227=CARTESIAN_POINT ( 'NONE',  ( 283.0000000000000568, -26.06128899128900045, -10.14003097807800025 ) ) ;
#45240=EDGE_CURVE ( 'NONE', #37106, #52181, #47276, .T. ) ;
#45289=VECTOR ( 'NONE', #5286, 1000.000000000000000 ) ;
#45316=EDGE_CURVE ( 'NONE', #52106, #65495, #27826, .T. ) ;
#45338=ORIENTED_EDGE ( 'NONE', *, *, #12211, .T. ) ;
#45340=DIRECTION ( 'NONE',  ( 0.000000000000000000, -1.000000000000000000, 0.000000000000000000 ) ) ;
#45355=VERTEX_POINT ( 'NONE', #19233 ) ;
#45365=ORIENTED_EDGE ( 'NONE', *, *, #47569, .T. ) ;
#45366=CARTESIAN_POINT ( 'NONE',  ( 7.000000000000000000, -32.44999999999905071, -13.20000000000091944 ) ) ;
#45387=ORIENTED_EDGE ( 'NONE', *, *, #31648, .T. ) ;
#45390=CARTESIAN_POINT ( 'NONE',  ( 7.000000000000000000, -42.50000000000000000, 10.20000000000000107 ) ) ;
#45392=VECTOR ( 'NONE', #6762, 1000.000000000000000 ) ;
#45416=PLANE ( 'NONE',  #23015 ) ;
#45420=LINE ( 'NONE', #63013, #5204 ) ;
#45422=LINE ( 'NONE', #50386, #55274 ) ;
#45440=ORIENTED_EDGE ( 'NONE', *, *, #33695, .T. ) ;
#45478=EDGE_CURVE ( 'NONE', #16868, #50939, #41143, .T. ) ;
#45521=CARTESIAN_POINT ( 'NONE',  ( 1.000000000000000000, -21.00000000000000000, -4.000000000000000000 ) ) ;
#45522=AXIS2_PLACEMENT_3D ( 'NONE', #47454, #30145, #30845 ) ;
#45523=VERTEX_POINT ( 'NONE', #47505 ) ;
#45526=ORIENTED_EDGE ( 'NONE', *, *, #42043, .F. ) ;
#45530=ORIENTED_EDGE ( 'NONE', *, *, #61939, .T. ) ;
#45539=EDGE_CURVE ( 'NONE', #68300, #37771, #8620, .T. ) ;
#45544=ORIENTED_EDGE ( 'NONE', *, *, #46966, .T. ) ;
#45551=VECTOR ( 'NONE', #59097, 1000.000000000000000 ) ;
#45578=ORIENTED_EDGE ( 'NONE', *, *, #65116, .T. ) ;
#45580=EDGE_CURVE ( 'NONE', #1599, #32551, #30196, .T. ) ;
#45581=DIRECTION ( 'NONE',  ( 0.000000000000000000, 1.000000000000000000, 0.000000000000000000 ) ) ;
#45595=CARTESIAN_POINT ( 'NONE',  ( 283.0000000000000568, -39.79999999999954952, -8.900000000000419575 ) ) ;
#45605=EDGE_LOOP ( 'NONE', ( #59786, #69490, #49281, #51715 ) ) ;
#45633=( BOUNDED_CURVE ( )  B_SPLINE_CURVE ( 3, ( #21070, #42630, #64216, #15766 ),
 .UNSPECIFIED., .F., .F. ) 
 B_SPLINE_CURVE_WITH_KNOTS ( ( 4, 4 ),
 ( 2.245927859731927878, 2.418858405776376674 ),
 .UNSPECIFIED. ) 
 CURVE ( )  GEOMETRIC_REPRESENTATION_ITEM ( )  RATIONAL_B_SPLINE_CURVE ( ( 1.000000000000000000, 0.9975094710839674805, 0.9975094710839674805, 1.000000000000000000 ) ) 
 REPRESENTATION_ITEM ( '' )  );
#45634=CARTESIAN_POINT ( 'NONE',  ( 283.0000000000000568, -25.50000000000000355, -17.00000000000000000 ) ) ;
#45639=CARTESIAN_POINT ( 'NONE',  ( 0.000000000000000000, -0.5000000000000000000, -26.50000000000000000 ) ) ;
#45646=VERTEX_POINT ( 'NONE', #12778 ) ;
#45647=VECTOR ( 'NONE', #9442, 1000.000000000000000 ) ;
#45655=CARTESIAN_POINT ( 'NONE',  ( 283.0000000000000568, -53.81370849898476649, -17.35424868893542438 ) ) ;
#45675=DIRECTION ( 'NONE',  ( 1.000000000000000000, -0.000000000000000000, -0.000000000000000000 ) ) ;
#45677=EDGE_CURVE ( 'NONE', #41506, #5501, #2884, .T. ) ;
#45695=EDGE_CURVE ( 'NONE', #7061, #187, #66878, .T. ) ;
#45701=ORIENTED_EDGE ( 'NONE', *, *, #14327, .F. ) ;
#45721=CARTESIAN_POINT ( 'NONE',  ( 283.0000000000000568, -39.79999999999905214, -12.19999999999906315 ) ) ;
#45744=EDGE_CURVE ( 'NONE', #21817, #67535, #8530, .T. ) ;
#45765=EDGE_CURVE ( 'NONE', #3117, #52106, #30138, .T. ) ;
#45805=LINE ( 'NONE', #57465, #56711 ) ;
#45808=DIRECTION ( 'NONE',  ( 0.000000000000000000, 0.000000000000000000, 1.000000000000000000 ) ) ;
#45810=VECTOR ( 'NONE', #64135, 1000.000000000000000 ) ;
#45815=EDGE_CURVE ( 'NONE', #43665, #69628, #38038, .T. ) ;
#45816=DIRECTION ( 'NONE',  ( 0.000000000000000000, 0.000000000000000000, -1.000000000000000000 ) ) ;
#45819=AXIS2_PLACEMENT_3D ( 'NONE', #598, #38092, #21811 ) ;
#45838=DIRECTION ( 'NONE',  ( 0.000000000000000000, 0.000000000000000000, -1.000000000000000000 ) ) ;
#45851=CARTESIAN_POINT ( 'NONE',  ( 7.000000000000000000, -42.00000000000000000, -15.00000000000000000 ) ) ;
#45867=DIRECTION ( 'NONE',  ( 0.000000000000000000, 0.000000000000000000, -1.000000000000000000 ) ) ;
#45868=DIRECTION ( 'NONE',  ( 0.000000000000000000, 0.000000000000000000, 1.000000000000000000 ) ) ;
#45872=AXIS2_PLACEMENT_3D ( 'NONE', #53949, #54642, #33743 ) ;
#45900=EDGE_LOOP ( 'NONE', ( #16026, #4083, #57539, #64682 ) ) ;
#45905=ORIENTED_EDGE ( 'NONE', *, *, #45478, .T. ) ;
#45913=AXIS2_PLACEMENT_3D ( 'NONE', #20740, #4149, #25718 ) ;
#45918=AXIS2_PLACEMENT_3D ( 'NONE', #22775, #53934, #32355 ) ;
#45932=DIRECTION ( 'NONE',  ( -1.000000000000000000, 0.000000000000000000, 0.000000000000000000 ) ) ;
#45937=EDGE_LOOP ( 'NONE', ( #35798, #48986, #65137, #1120, #15222, #68862, #31334, #14391, #68511, #26830, #35968, #3249, #59377, #17745, #53858 ) ) ;
#45939=CARTESIAN_POINT ( 'NONE',  ( 283.0000000000000568, -21.00000000000000000, -12.50000000000000000 ) ) ;
#45951=( GEOMETRIC_REPRESENTATION_CONTEXT ( 3 ) GLOBAL_UNCERTAINTY_ASSIGNED_CONTEXT ( ( #35923 ) ) GLOBAL_UNIT_ASSIGNED_CONTEXT ( ( #397, #53451, #11339 ) ) REPRESENTATION_CONTEXT ( 'NONE', 'WORKASPACE' ) );
#45955=ORIENTED_EDGE ( 'NONE', *, *, #35433, .F. ) ;
#45975=CARTESIAN_POINT ( 'NONE',  ( 7.000000000000000000, -26.42999999999999972, -9.412893218813501051 ) ) ;
#45978=VERTEX_POINT ( 'NONE', #12346 ) ;
#45986=DIRECTION ( 'NONE',  ( -1.000000000000000000, 0.000000000000000000, 0.000000000000000000 ) ) ;
#46002=AXIS2_PLACEMENT_3D ( 'NONE', #16915, #48401, #59355 ) ;
#46012=CARTESIAN_POINT ( 'NONE',  ( 276.8775010008008053, -21.00000000000000000, -17.50000000000000000 ) ) ;
#46019=CARTESIAN_POINT ( 'NONE',  ( 283.0000000000000568, -26.50000000000000000, -0.5000000000000000000 ) ) ;
#46023=AXIS2_PLACEMENT_3D ( 'NONE', #141, #42911, #58502 ) ;
#46037=DIRECTION ( 'NONE',  ( -1.000000000000000000, 0.000000000000000000, 0.000000000000000000 ) ) ;
#46054=DIRECTION ( 'NONE',  ( 0.000000000000000000, 0.5017180897718488408, -0.8650311892618017806 ) ) ;
#46055=PLANE ( 'NONE',  #63582 ) ;
#46069=LINE ( 'NONE', #19899, #17296 ) ;
#46077=ORIENTED_EDGE ( 'NONE', *, *, #45478, .F. ) ;
#46097=DIRECTION ( 'NONE',  ( 0.000000000000000000, -0.7071067811865875408, 0.7071067811865076047 ) ) ;
#46105=DIRECTION ( 'NONE',  ( 0.000000000000000000, 0.000000000000000000, 1.000000000000000000 ) ) ;
#46106=FACE_OUTER_BOUND ( 'NONE', #46918, .T. ) ;
#46139=CARTESIAN_POINT ( 'NONE',  ( 283.0000000000000568, -20.50000000000000000, 17.00000000000000000 ) ) ;
#46152=ORIENTED_EDGE ( 'NONE', *, *, #19421, .T. ) ;
#46177=FACE_OUTER_BOUND ( 'NONE', #60261, .T. ) ;
#46183=CARTESIAN_POINT ( 'NONE',  ( 7.000000000000000000, -20.50000000000000000, -13.00000000000000178 ) ) ;
#46188=ORIENTED_EDGE ( 'NONE', *, *, #7123, .T. ) ;
#46199=DIRECTION ( 'NONE',  ( 0.7071067811865465735, -0.7071067811865485719, 0.000000000000000000 ) ) ;
#46202=CARTESIAN_POINT ( 'NONE',  ( 0.000000000000000000, -21.00000000000000000, 5.000000000000000000 ) ) ;
#46207=PLANE ( 'NONE',  #56700 ) ;
#46227=ORIENTED_EDGE ( 'NONE', *, *, #15534, .T. ) ;
#46237=DIRECTION ( 'NONE',  ( -1.000000000000000000, 0.000000000000000000, 0.000000000000000000 ) ) ;
#46267=AXIS2_PLACEMENT_3D ( 'NONE', #8649, #30920, #3346 ) ;
#46287=LINE ( 'NONE', #35674, #56053 ) ;
#46297=ORIENTED_EDGE ( 'NONE', *, *, #52966, .F. ) ;
#46309=AXIS2_PLACEMENT_3D ( 'NONE', #43643, #513, #60585 ) ;
#46313=VERTEX_POINT ( 'NONE', #38806 ) ;
#46325=VECTOR ( 'NONE', #17017, 1000.000000000000114 ) ;
#46362=VERTEX_POINT ( 'NONE', #22556 ) ;
#46379=PLANE ( 'NONE',  #69651 ) ;
#46380=DIRECTION ( 'NONE',  ( -1.000000000000000000, 0.000000000000000000, 0.000000000000000000 ) ) ;
#46389=EDGE_CURVE ( 'NONE', #63351, #17105, #49437, .T. ) ;
#46398=FACE_OUTER_BOUND ( 'NONE', #20680, .T. ) ;
#46399=CARTESIAN_POINT ( 'NONE',  ( 275.5000000000000000, -42.50000000000000000, 26.50000000000000000 ) ) ;
#46420=AXIS2_PLACEMENT_3D ( 'NONE', #39699, #67630, #66918 ) ;
#46442=LINE ( 'NONE', #62700, #55324 ) ;
#46447=CARTESIAN_POINT ( 'NONE',  ( 15.00000000000000000, -42.50000000000000000, 27.00000000000000000 ) ) ;
#46485=ADVANCED_FACE ( 'NONE', ( #7309 ), #60720, .T. ) ;
#46486=DIRECTION ( 'NONE',  ( -0.5773502691896201799, -0.5773502691896285066, -0.5773502691896285066 ) ) ;
#46487=DIRECTION ( 'NONE',  ( 0.000000000000000000, 0.5017180897718492849, 0.8650311892618014475 ) ) ;
#46494=CARTESIAN_POINT ( 'NONE',  ( 0.5000000000000000000, -42.00000000000000000, -27.00000000000000000 ) ) ;
#46507=ORIENTED_EDGE ( 'NONE', *, *, #45316, .F. ) ;
#46511=ORIENTED_EDGE ( 'NONE', *, *, #64152, .T. ) ;
#46516=ORIENTED_EDGE ( 'NONE', *, *, #27545, .F. ) ;
#46523=CYLINDRICAL_SURFACE ( 'NONE', #7402, 0.4999999999979499732 ) ;
#46531=EDGE_CURVE ( 'NONE', #30152, #29737, #23234, .T. ) ;
#46552=DIRECTION ( 'NONE',  ( -1.000000000000000000, 0.000000000000000000, 0.000000000000000000 ) ) ;
#46558=ORIENTED_EDGE ( 'NONE', *, *, #23177, .T. ) ;
#46604=DIRECTION ( 'NONE',  ( 1.000000000000000000, 0.000000000000000000, 0.000000000000000000 ) ) ;
#46606=ORIENTED_EDGE ( 'NONE', *, *, #38296, .F. ) ;
#46619=DIRECTION ( 'NONE',  ( 1.000000000000000000, 0.000000000000000000, 0.000000000000000000 ) ) ;
#46651=DIRECTION ( 'NONE',  ( 0.000000000000000000, -2.123301534585676023E-12, 1.000000000000000000 ) ) ;
#46669=EDGE_LOOP ( 'NONE', ( #65156, #30721, #51805, #31924 ) ) ;
#46672=VERTEX_POINT ( 'NONE', #4482 ) ;
#46675=LINE ( 'NONE', #30424, #52774 ) ;
#46681=CIRCLE ( 'NONE', #43257, 0.4999999999979768961 ) ;
#46689=VERTEX_POINT ( 'NONE', #14020 ) ;
#46697=ORIENTED_EDGE ( 'NONE', *, *, #64279, .T. ) ;
#46699=DIRECTION ( 'NONE',  ( -1.000000000000000000, 0.000000000000000000, 0.000000000000000000 ) ) ;
#46711=ORIENTED_EDGE ( 'NONE', *, *, #42787, .F. ) ;
#46731=ORIENTED_EDGE ( 'NONE', *, *, #60922, .F. ) ;
#46740=CARTESIAN_POINT ( 'NONE',  ( 275.0000000000000000, -31.99999999999889866, -7.899999999997660893 ) ) ;
#46761=VECTOR ( 'NONE', #47538, 1000.000000000000000 ) ;
#46762=LINE ( 'NONE', #52080, #9653 ) ;
#46767=EDGE_LOOP ( 'NONE', ( #50563, #19188, #30129, #50048, #55892, #51642 ) ) ;
#46777=EDGE_CURVE ( 'NONE', #38349, #65427, #43334, .T. ) ;
#46782=ADVANCED_FACE ( 'NONE', ( #6211 ), #64571, .F. ) ;
#46785=ORIENTED_EDGE ( 'NONE', *, *, #29694, .T. ) ;
#46787=DIRECTION ( 'NONE',  ( 0.000000000000000000, -0.7071067811865076047, -0.7071067811865875408 ) ) ;
#46795=EDGE_CURVE ( 'NONE', #52522, #49901, #22129, .T. ) ;
#46809=ORIENTED_EDGE ( 'NONE', *, *, #19765, .T. ) ;
#46823=DIRECTION ( 'NONE',  ( 0.000000000000000000, 0.000000000000000000, -1.000000000000000000 ) ) ;
#46828=FACE_OUTER_BOUND ( 'NONE', #11656, .T. ) ;
#46829=DIRECTION ( 'NONE',  ( -1.000000000000000000, 0.000000000000000000, 0.000000000000000000 ) ) ;
#46861=LINE ( 'NONE', #20005, #30492 ) ;
#46910=EDGE_LOOP ( 'NONE', ( #6842, #5095 ) ) ;
#46911=DIRECTION ( 'NONE',  ( 0.000000000000000000, 1.000000000000000000, 0.000000000000000000 ) ) ;
#46918=EDGE_LOOP ( 'NONE', ( #29141, #14773, #3493, #47560, #41505 ) ) ;
#46926=CARTESIAN_POINT ( 'NONE',  ( 15.00000000000000000, -42.00000000000000000, -26.50000000000000000 ) ) ;
#46928=AXIS2_PLACEMENT_3D ( 'NONE', #49720, #49393, #26783 ) ;
#46938=DIRECTION ( 'NONE',  ( 0.000000000000000000, -0.7071067811865480168, 0.7071067811865470176 ) ) ;
#46951=DIRECTION ( 'NONE',  ( -0.7071067811865480168, 0.000000000000000000, -0.7071067811865470176 ) ) ;
#46963=EDGE_CURVE ( 'NONE', #7638, #14513, #38185, .T. ) ;
#46966=EDGE_CURVE ( 'NONE', #21056, #12243, #23508, .T. ) ;
#46973=EDGE_CURVE ( 'NONE', #1040, #60826, #69824, .T. ) ;
#46983=VERTEX_POINT ( 'NONE', #56730 ) ;
#46998=FACE_OUTER_BOUND ( 'NONE', #19756, .T. ) ;
#46999=ORIENTED_EDGE ( 'NONE', *, *, #29294, .T. ) ;
#47000=AXIS2_PLACEMENT_3D ( 'NONE', #23258, #28219, #33861 ) ;
#47013=LINE ( 'NONE', #69645, #32708 ) ;
#47025=VECTOR ( 'NONE', #36032, 999.9999999999998863 ) ;
#47033=VERTEX_POINT ( 'NONE', #57079 ) ;
#47037=LINE ( 'NONE', #53057, #68836 ) ;
#47039=FACE_OUTER_BOUND ( 'NONE', #15194, .T. ) ;
#47044=AXIS2_PLACEMENT_3D ( 'NONE', #28845, #50430, #45816 ) ;
#47086=DIRECTION ( 'NONE',  ( 0.000000000000000000, -0.5017180897718492849, 0.8650311892618014475 ) ) ;
#47105=EDGE_CURVE ( 'NONE', #11772, #56785, #50579, .T. ) ;
#47111=ORIENTED_EDGE ( 'NONE', *, *, #14962, .T. ) ;
#47132=CARTESIAN_POINT ( 'NONE',  ( 15.00000000000000000, -21.00000000000000000, 4.000000000000000000 ) ) ;
#47133=DIRECTION ( 'NONE',  ( 0.000000000000000000, 0.000000000000000000, -1.000000000000000000 ) ) ;
#47135=ORIENTED_EDGE ( 'NONE', *, *, #11516, .T. ) ;
#47136=ORIENTED_EDGE ( 'NONE', *, *, #67128, .F. ) ;
#47144=( NAMED_UNIT ( * ) SI_UNIT ( $, .STERADIAN. ) SOLID_ANGLE_UNIT ( ) );
#47166=LINE ( 'NONE', #3673, #43120 ) ;
#47180=ORIENTED_EDGE ( 'NONE', *, *, #45240, .F. ) ;
#47185=AXIS2_PLACEMENT_3D ( 'NONE', #6276, #65339, #43064 ) ;
#47187=DIRECTION ( 'NONE',  ( 0.000000000000000000, -1.000000000000000000, -1.838806884531994514E-12 ) ) ;
#47200=CARTESIAN_POINT ( 'NONE',  ( 275.0000000000000000, -25.60000000000000142, 17.60000000000000142 ) ) ;
#47211=ORIENTED_EDGE ( 'NONE', *, *, #5210, .T. ) ;
#47234=ORIENTED_EDGE ( 'NONE', *, *, #22531, .F. ) ;
#47242=FACE_OUTER_BOUND ( 'NONE', #20743, .T. ) ;
#47248=ORIENTED_EDGE ( 'NONE', *, *, #9205, .F. ) ;
#47264=ORIENTED_EDGE ( 'NONE', *, *, #9372, .F. ) ;
#47276=LINE ( 'NONE', #15104, #52677 ) ;
#47292=DIRECTION ( 'NONE',  ( 0.000000000000000000, 0.000000000000000000, -1.000000000000000000 ) ) ;
#47337=AXIS2_PLACEMENT_3D ( 'NONE', #25964, #54228, #27353 ) ;
#47343=ORIENTED_EDGE ( 'NONE', *, *, #15756, .F. ) ;
#47354=ORIENTED_EDGE ( 'NONE', *, *, #38493, .T. ) ;
#47362=EDGE_CURVE ( 'NONE', #46672, #45646, #39338, .T. ) ;
#47364=EDGE_LOOP ( 'NONE', ( #28772, #1251, #41804, #13361, #47926, #57278, #58891, #17441, #35980, #36145, #61278, #48282 ) ) ;
#47365=EDGE_CURVE ( 'NONE', #16188, #26187, #61232, .T. ) ;
#47388=AXIS2_PLACEMENT_3D ( 'NONE', #392, #47425, #9967 ) ;
#47402=AXIS2_PLACEMENT_3D ( 'NONE', #40595, #62495, #35269 ) ;
#47425=DIRECTION ( 'NONE',  ( 0.000000000000000000, 1.000000000000000000, 0.000000000000000000 ) ) ;
#47430=DIRECTION ( 'NONE',  ( -1.000000000000000000, 0.000000000000000000, 0.000000000000000000 ) ) ;
#47444=LINE ( 'NONE', #9981, #955 ) ;
#47449=DIRECTION ( 'NONE',  ( -0.5773502691896257311, -0.5773502691896257311, 0.5773502691896257311 ) ) ;
#47453=VECTOR ( 'NONE', #55594, 1000.000000000000000 ) ;
#47454=CARTESIAN_POINT ( 'NONE',  ( 275.0000000000000000, -32.44999999999905071, 13.20000000000091944 ) ) ;
#47456=DIRECTION ( 'NONE',  ( 0.000000000000000000, 0.9760787414516765015, 0.2174173187354474512 ) ) ;
#47457=DIRECTION ( 'NONE',  ( 1.000000000000000000, 0.000000000000000000, 0.000000000000000000 ) ) ;
#47468=VECTOR ( 'NONE', #29999, 1000.000000000000000 ) ;
#47491=CARTESIAN_POINT ( 'NONE',  ( 7.000000000000000000, -30.80000000000000071, 8.900000000000000355 ) ) ;
#47494=EDGE_CURVE ( 'NONE', #24019, #3194, #63096, .T. ) ;
#47505=CARTESIAN_POINT ( 'NONE',  ( 7.000000000000000000, -21.00000000000000000, -7.800000000000000711 ) ) ;
#47508=VECTOR ( 'NONE', #28977, 1000.000000000000000 ) ;
#47522=CARTESIAN_POINT ( 'NONE',  ( 7.000000000000000000, -26.06128899128900045, -10.14003097807800025 ) ) ;
#47538=DIRECTION ( 'NONE',  ( 0.000000000000000000, 0.000000000000000000, -1.000000000000000000 ) ) ;
#47549=CARTESIAN_POINT ( 'NONE',  ( 283.0000000000000568, -23.50007830495750127, -12.28007262201345995 ) ) ;
#47560=ORIENTED_EDGE ( 'NONE', *, *, #40134, .T. ) ;
#47568=CARTESIAN_POINT ( 'NONE',  ( 283.0000000000000568, -40.30000000000000426, -12.20000000000000107 ) ) ;
#47569=EDGE_CURVE ( 'NONE', #64136, #45523, #16773, .T. ) ;
#47572=CARTESIAN_POINT ( 'NONE',  ( 275.0000000000001137, -41.99999999999996447, -26.49999999999994316 ) ) ;
#47589=EDGE_CURVE ( 'NONE', #49352, #21570, #6977, .T. ) ;
#47610=DIRECTION ( 'NONE',  ( 0.7071067811865475727, 0.000000000000000000, 0.7071067811865475727 ) ) ;
#47612=CARTESIAN_POINT ( 'NONE',  ( 283.0000000000000568, -38.15000000000000568, 14.50000000000000000 ) ) ;
#47641=CARTESIAN_POINT ( 'NONE',  ( 15.00000000000000000, -21.00000000000000000, -8.000000000000000000 ) ) ;
#47650=CARTESIAN_POINT ( 'NONE',  ( 283.0000000000000568, -25.00000000000000000, 17.50000000000000000 ) ) ;
#47678=VECTOR ( 'NONE', #8441, 1000.000000000000000 ) ;
#47682=CARTESIAN_POINT ( 'NONE',  ( 7.000000000000000000, -32.00000000000000000, -8.400000000000000355 ) ) ;
#47687=VECTOR ( 'NONE', #33645, 1000.000000000000000 ) ;
#47713=CARTESIAN_POINT ( 'NONE',  ( 283.0000000000000568, -25.60000000000000142, 17.35424868893542438 ) ) ;
#47738=DIRECTION ( 'NONE',  ( 0.000000000000000000, 0.000000000000000000, -1.000000000000000000 ) ) ;
#47759=EDGE_CURVE ( 'NONE', #68548, #37548, #34540, .T. ) ;
#47777=DIRECTION ( 'NONE',  ( 0.000000000000000000, 0.000000000000000000, -1.000000000000000000 ) ) ;
#47783=CIRCLE ( 'NONE', #10536, 0.4999999999945534124 ) ;
#47784=DIRECTION ( 'NONE',  ( 1.000000000000000000, 0.000000000000000000, 0.000000000000000000 ) ) ;
#47816=DIRECTION ( 'NONE',  ( 0.000000000000000000, 0.000000000000000000, -1.000000000000000000 ) ) ;
#47818=VERTEX_POINT ( 'NONE', #35955 ) ;
#47821=VERTEX_POINT ( 'NONE', #52581 ) ;
#47836=CARTESIAN_POINT ( 'NONE',  ( 7.000000000000000000, -42.00000000000000000, -15.00000000000000000 ) ) ;
#47840=EDGE_CURVE ( 'NONE', #7061, #38093, #15451, .T. ) ;
#47845=DIRECTION ( 'NONE',  ( 0.000000000000000000, 0.000000000000000000, -1.000000000000000000 ) ) ;
#47846=EDGE_CURVE ( 'NONE', #3117, #1599, #15787, .T. ) ;
#47848=ORIENTED_EDGE ( 'NONE', *, *, #20104, .T. ) ;
#47872=DIRECTION ( 'NONE',  ( -1.000000000000000000, 0.000000000000000000, 0.000000000000000000 ) ) ;
#47879=AXIS2_PLACEMENT_3D ( 'NONE', #48586, #65538, #6495 ) ;
#47883=CARTESIAN_POINT ( 'NONE',  ( 283.0000000000000568, -37.61196062927500350, -8.008708659369300875 ) ) ;
#47887=EDGE_CURVE ( 'NONE', #16165, #65332, #36303, .T. ) ;
#47904=ORIENTED_EDGE ( 'NONE', *, *, #1493, .T. ) ;
#47905=ORIENTED_EDGE ( 'NONE', *, *, #20104, .F. ) ;
#47923=EDGE_CURVE ( 'NONE', #56561, #54968, #14588, .T. ) ;
#47926=ORIENTED_EDGE ( 'NONE', *, *, #60917, .F. ) ;
#47930=VERTEX_POINT ( 'NONE', #58224 ) ;
#47937=VECTOR ( 'NONE', #19102, 1000.000000000000000 ) ;
#47940=VECTOR ( 'NONE', #9331, 1000.000000000000000 ) ;
#47950=CARTESIAN_POINT ( 'NONE',  ( 7.000000000000000000, -23.65000000000000568, -12.40000000000000213 ) ) ;
#47952=AXIS2_PLACEMENT_3D ( 'NONE', #45975, #61518, #23367 ) ;
#47956=EDGE_CURVE ( 'NONE', #52439, #69628, #65614, .T. ) ;
#47963=CARTESIAN_POINT ( 'NONE',  ( 283.0000000000000568, -23.70411739045900390, -12.50000000000000000 ) ) ;
#47965=ORIENTED_EDGE ( 'NONE', *, *, #50305, .F. ) ;
#47986=DIRECTION ( 'NONE',  ( 1.000000000000000000, -0.000000000000000000, -0.000000000000000000 ) ) ;
#48004=CARTESIAN_POINT ( 'NONE',  ( 283.0000000000000568, -29.94999999999999929, 14.50000000000000000 ) ) ;
#48019=CARTESIAN_POINT ( 'NONE',  ( 7.000000000000000000, -20.40000000000000213, -17.60000000000000142 ) ) ;
#48045=DIRECTION ( 'NONE',  ( 0.000000000000000000, 0.000000000000000000, 1.000000000000000000 ) ) ;
#48112=CARTESIAN_POINT ( 'NONE',  ( 15.00000000000000000, -23.65000000000000568, 12.40000000000000213 ) ) ;
#48119=ORIENTED_EDGE ( 'NONE', *, *, #9695, .F. ) ;
#48125=EDGE_CURVE ( 'NONE', #66609, #48603, #45422, .T. ) ;
#48128=FACE_OUTER_BOUND ( 'NONE', #60693, .T. ) ;
#48132=CARTESIAN_POINT ( 'NONE',  ( 280.0000000000000000, -25.50000000000000355, -20.00000000000000000 ) ) ;
#48133=CARTESIAN_POINT ( 'NONE',  ( 7.000000000000000000, -25.60000000000000142, 15.10000000000000142 ) ) ;
#48139=DIRECTION ( 'NONE',  ( -1.000000000000000000, 0.000000000000000000, 0.000000000000000000 ) ) ;
#48142=LINE ( 'NONE', #69717, #32199 ) ;
#48163=CARTESIAN_POINT ( 'NONE',  ( 275.0000000000000000, -20.40000000000000213, 12.40000000000000213 ) ) ;
#48181=LINE ( 'NONE', #47132, #10671 ) ;
#48186=EDGE_LOOP ( 'NONE', ( #4523, #69580, #36271, #63832, #46077 ) ) ;
#48187=LINE ( 'NONE', #14262, #60401 ) ;
#48202=ORIENTED_EDGE ( 'NONE', *, *, #15496, .T. ) ;
#48215=VERTEX_POINT ( 'NONE', #8651 ) ;
#48227=VERTEX_POINT ( 'NONE', #68405 ) ;
#48230=FACE_OUTER_BOUND ( 'NONE', #18128, .T. ) ;
#48236=DIRECTION ( 'NONE',  ( 0.000000000000000000, 0.000000000000000000, -1.000000000000000000 ) ) ;
#48248=VECTOR ( 'NONE', #20114, 1000.000000000000000 ) ;
#48255=VECTOR ( 'NONE', #63807, 1000.000000000000000 ) ;
#48270=EDGE_LOOP ( 'NONE', ( #53449, #26243, #4354, #16197 ) ) ;
#48272=ORIENTED_EDGE ( 'NONE', *, *, #47105, .F. ) ;
#48273=ADVANCED_FACE ( 'NONE', ( #15011 ), #3701, .T. ) ;
#48282=ORIENTED_EDGE ( 'NONE', *, *, #67400, .F. ) ;
#48301=VECTOR ( 'NONE', #4725, 1000.000000000000000 ) ;
#48328=LINE ( 'NONE', #37717, #1737 ) ;
#48330=FACE_OUTER_BOUND ( 'NONE', #67829, .T. ) ;
#48333=VERTEX_POINT ( 'NONE', #69450 ) ;
#48353=( BOUNDED_CURVE ( )  B_SPLINE_CURVE ( 3, ( #30235, #19263, #7603, #7944 ),
 .UNSPECIFIED., .F., .F. ) 
 B_SPLINE_CURVE_WITH_KNOTS ( ( 4, 4 ),
 ( 3.864326901403221104, 4.037257447447658798 ),
 .UNSPECIFIED. ) 
 CURVE ( )  GEOMETRIC_REPRESENTATION_ITEM ( )  RATIONAL_B_SPLINE_CURVE ( ( 1.000000000000000000, 0.9975094710839678136, 0.9975094710839678136, 1.000000000000000000 ) ) 
 REPRESENTATION_ITEM ( '' )  );
#48356=CARTESIAN_POINT ( 'NONE',  ( 7.000000000000000000, -32.45000000000000995, -15.00000000000000000 ) ) ;
#48380=EDGE_CURVE ( 'NONE', #39081, #16092, #45105, .T. ) ;
#48388=PLANE ( 'NONE',  #61222 ) ;
#48401=DIRECTION ( 'NONE',  ( 0.000000000000000000, -0.7071067811865480168, -0.7071067811865470176 ) ) ;
#48409=CARTESIAN_POINT ( 'NONE',  ( 283.0000000000000568, -30.80000000000000071, -8.900000000000000355 ) ) ;
#48417=DIRECTION ( 'NONE',  ( 0.000000000000000000, 1.000000000000000000, 0.000000000000000000 ) ) ;
#48420=PLANE ( 'NONE',  #63667 ) ;
#48428=LINE ( 'NONE', #59034, #31023 ) ;
#48429=EDGE_LOOP ( 'NONE', ( #13799, #16310, #49092, #57108 ) ) ;
#48440=DIRECTION ( 'NONE',  ( 0.000000000000000000, 1.000000000000000000, 0.000000000000000000 ) ) ;
#48445=LINE ( 'NONE', #54790, #30825 ) ;
#48457=ORIENTED_EDGE ( 'NONE', *, *, #2507, .T. ) ;
#48460=PLANE ( 'NONE',  #57185 ) ;
#48475=DIRECTION ( 'NONE',  ( 0.000000000000000000, 0.7071067811865474617, -0.7071067811865474617 ) ) ;
#48476=EDGE_CURVE ( 'NONE', #27121, #7467, #58718, .T. ) ;
#48496=AXIS2_PLACEMENT_3D ( 'NONE', #762, #22331, #11684 ) ;
#48529=ORIENTED_EDGE ( 'NONE', *, *, #16331, .T. ) ;
#48540=DIRECTION ( 'NONE',  ( 0.000000000000000000, 0.000000000000000000, 1.000000000000000000 ) ) ;
#48551=CARTESIAN_POINT ( 'NONE',  ( 283.0000000000000568, -21.00000000000000000, 17.50000000000000000 ) ) ;
#48568=ORIENTED_EDGE ( 'NONE', *, *, #54995, .T. ) ;
#48577=VECTOR ( 'NONE', #1167, 1000.000000000000000 ) ;
#48580=ORIENTED_EDGE ( 'NONE', *, *, #22713, .T. ) ;
#48586=CARTESIAN_POINT ( 'NONE',  ( 283.0000000000000568, -38.65000000000095781, 13.20000000000094253 ) ) ;
#48603=VERTEX_POINT ( 'NONE', #67272 ) ;
#48615=VECTOR ( 'NONE', #36533, 1000.000000000000000 ) ;
#48632=DIRECTION ( 'NONE',  ( -0.7071067811865470176, 0.7071067811865480168, 0.000000000000000000 ) ) ;
#48646=EDGE_CURVE ( 'NONE', #56856, #5501, #35788, .T. ) ;
#48651=PLANE ( 'NONE',  #13849 ) ;
#48655=VECTOR ( 'NONE', #31993, 1000.000000000000000 ) ;
#48663=VECTOR ( 'NONE', #58529, 1000.000000000000000 ) ;
#48689=ORIENTED_EDGE ( 'NONE', *, *, #35353, .T. ) ;
#48715=LINE ( 'NONE', #9489, #31734 ) ;
#48736=CARTESIAN_POINT ( 'NONE',  ( 7.000000000000000000, -42.50000000000000000, 14.50000000000000000 ) ) ;
#48748=VECTOR ( 'NONE', #54129, 1000.000000000000114 ) ;
#48758=CONICAL_SURFACE ( 'NONE', #10399, 7.799999999999999822, 1.047197551196693555 ) ;
#48759=CLOSED_SHELL ( 'NONE', ( #33227, #16147, #59851, #65940, #19887, #22992, #14593, #20203, #15856, #61783, #65616, #62991, #24764, #19043, #50779, #12915, #41118, #66565, #7191, #26518, #12436, #30422, #18836, #63429, #27886, #28978, #64914, #7071, #67139, #56375, #40270, #22777, #17107, #34628, #66700, #34085, #9334, #20297, #16401, #30678, #63462, #65263, #69478, #60435, #22620, #22409, #37569, #20754, #32639, #59815, #45138, #45060, #2824, #40578, #43509, #26850, #44179, #63236, #9434, #12931, #51698, #13983, #8297, #62035, #66906, #39396, #3460, #69224, #15559, #31015, #6375, #60466, #10966, #55008, #14202, #48273, #33683, #8935, #43066, #9930, #35288, #53331, #44066, #62280, #39618, #26695, #42327, #38149, #31644, #3657, #12330, #31573, #40889, #21300, #35124, #22463, #53609, #24040, #19833, #32537, #15364, #34773, #15789, #28096, #56161, #29855, #22989, #62755, #15069, #57415, #60583, #41282, #55677, #1645, #33199, #51639, #32977, #67443, #60979, #46782, #39476, #29309, #41996, #56905, #37088, #460, #4699, #55714, #51547, #41048, #65578, #55461, #54768, #53150, #58846, #5477, #20977, #59897, #19645, #60974, #35840, #25931, #61723, #12592, #34861, #21436, #50542, #914, #949, #44799, #49128, #33704, #61492, #49614, #65015, #4284, #23404, #62826, #23314, #49401, #7665, #55735, #53284, #37784, #23481, #3658, #53203, #68119, #8219, #37077, #58475, #34992, #31501, #37587, #40429, #4030, #61301, #8139, #41513, #19884, #68752, #28868, #29813, #29768, #4434, #41600, #57160, #46485, #42464, #41101, #68223 ) ) ;
#48804=ORIENTED_EDGE ( 'NONE', *, *, #26189, .T. ) ;
#48808=EDGE_CURVE ( 'NONE', #57192, #28510, #32930, .T. ) ;
#48822=CARTESIAN_POINT ( 'NONE',  ( 7.000000000000000000, -32.95000000000000284, 13.19999999999999929 ) ) ;
#48835=EDGE_CURVE ( 'NONE', #62567, #53126, #65460, .T. ) ;
#48849=ORIENTED_EDGE ( 'NONE', *, *, #28435, .F. ) ;
#48859=DIRECTION ( 'NONE',  ( 0.000000000000000000, -1.000000000000000000, 3.819861094142539476E-12 ) ) ;
#48892=EDGE_LOOP ( 'NONE', ( #45530, #95, #13911, #46516 ) ) ;
#48900=ORIENTED_EDGE ( 'NONE', *, *, #50688, .F. ) ;
#48918=EDGE_CURVE ( 'NONE', #34291, #46672, #1022, .T. ) ;
#48942=CIRCLE ( 'NONE', #27479, 0.3000000000005387246 ) ;
#48952=CARTESIAN_POINT ( 'NONE',  ( 283.0000000000000568, -32.00000000000000000, 8.400000000000000355 ) ) ;
#48969=VECTOR ( 'NONE', #49398, 1000.000000000000114 ) ;
#48980=ORIENTED_EDGE ( 'NONE', *, *, #25495, .T. ) ;
#48984=VECTOR ( 'NONE', #8164, 1000.000000000000000 ) ;
#48986=ORIENTED_EDGE ( 'NONE', *, *, #68644, .F. ) ;
#48989=DIRECTION ( 'NONE',  ( 0.000000000000000000, -1.000000000000000000, 0.000000000000000000 ) ) ;
#49009=DIRECTION ( 'NONE',  ( 0.000000000000000000, 0.000000000000000000, -1.000000000000000000 ) ) ;
#49015=PLANE ( 'NONE',  #53418 ) ;
#49019=ORIENTED_EDGE ( 'NONE', *, *, #15496, .F. ) ;
#49035=EDGE_LOOP ( 'NONE', ( #68019, #2748, #37196, #3807 ) ) ;
#49062=AXIS2_PLACEMENT_3D ( 'NONE', #4348, #47457, #69025 ) ;
#49065=CARTESIAN_POINT ( 'NONE',  ( 15.00000000000000000, -42.00000000000000000, -15.10000000000000142 ) ) ;
#49070=DIRECTION ( 'NONE',  ( 1.000000000000000000, 0.000000000000000000, 0.000000000000000000 ) ) ;
#49082=DIRECTION ( 'NONE',  ( 0.000000000000000000, -1.000000000000000000, 0.000000000000000000 ) ) ;
#49092=ORIENTED_EDGE ( 'NONE', *, *, #13739, .T. ) ;
#49095=VECTOR ( 'NONE', #64587, 1000.000000000000000 ) ;
#49101=DIRECTION ( 'NONE',  ( 0.5773502691896230665, 0.5773502691896271743, 0.5773502691896271743 ) ) ;
#49104=AXIS2_PLACEMENT_3D ( 'NONE', #42480, #26927, #32916 ) ;
#49119=ORIENTED_EDGE ( 'NONE', *, *, #11687, .T. ) ;
#49128=ADVANCED_FACE ( 'NONE', ( #9193 ), #52329, .F. ) ;
#49129=VERTEX_POINT ( 'NONE', #14851 ) ;
#49162=DIRECTION ( 'NONE',  ( 0.000000000000000000, -1.000000000000000000, 0.000000000000000000 ) ) ;
#49171=CARTESIAN_POINT ( 'NONE',  ( 275.0000000000000000, -39.79999999999954952, -8.900000000000419575 ) ) ;
#49172=EDGE_CURVE ( 'NONE', #51726, #25149, #55156, .T. ) ;
#49180=ORIENTED_EDGE ( 'NONE', *, *, #64530, .T. ) ;
#49189=CARTESIAN_POINT ( 'NONE',  ( 7.000000000000000000, -25.50000000000000355, 14.74860679774999994 ) ) ;
#49192=EDGE_CURVE ( 'NONE', #65388, #35918, #21359, .T. ) ;
#49211=PLANE ( 'NONE',  #9188 ) ;
#49220=EDGE_CURVE ( 'NONE', #21056, #5435, #13466, .T. ) ;
#49223=DIRECTION ( 'NONE',  ( 0.000000000000000000, 1.000000000000000000, 0.000000000000000000 ) ) ;
#49230=CARTESIAN_POINT ( 'NONE',  ( 283.0000000000000568, -42.00000000000000000, -15.00000000000000000 ) ) ;
#49233=ORIENTED_EDGE ( 'NONE', *, *, #12348, .F. ) ;
#49239=VECTOR ( 'NONE', #64665, 1000.000000000000000 ) ;
#49262=DIRECTION ( 'NONE',  ( 0.000000000000000000, 0.000000000000000000, -1.000000000000000000 ) ) ;
#49269=VECTOR ( 'NONE', #33670, 1000.000000000000000 ) ;
#49281=ORIENTED_EDGE ( 'NONE', *, *, #3314, .F. ) ;
#49300=EDGE_CURVE ( 'NONE', #37343, #28935, #31355, .T. ) ;
#49302=VERTEX_POINT ( 'NONE', #68106 ) ;
#49328=ORIENTED_EDGE ( 'NONE', *, *, #69182, .F. ) ;
#49346=ORIENTED_EDGE ( 'NONE', *, *, #12640, .F. ) ;
#49352=VERTEX_POINT ( 'NONE', #20025 ) ;
#49353=LINE ( 'NONE', #55011, #23415 ) ;
#49366=PLANE ( 'NONE',  #45187 ) ;
#49377=AXIS2_PLACEMENT_3D ( 'NONE', #68956, #31838, #53402 ) ;
#49393=DIRECTION ( 'NONE',  ( 0.000000000000000000, 0.000000000000000000, 1.000000000000000000 ) ) ;
#49398=DIRECTION ( 'NONE',  ( 0.000000000000000000, 0.7071067811865474617, -0.7071067811865474617 ) ) ;
#49401=ADVANCED_FACE ( 'NONE', ( #44972 ), #17764, .F. ) ;
#49433=ORIENTED_EDGE ( 'NONE', *, *, #54904, .T. ) ;
#49437=LINE ( 'NONE', #11238, #40382 ) ;
#49449=CARTESIAN_POINT ( 'NONE',  ( 283.0000000000000568, -42.00000000000000000, 15.00000000000000000 ) ) ;
#49461=AXIS2_PLACEMENT_3D ( 'NONE', #54428, #10938, #32158 ) ;
#49471=ORIENTED_EDGE ( 'NONE', *, *, #66951, .T. ) ;
#49474=ORIENTED_EDGE ( 'NONE', *, *, #26721, .T. ) ;
#49475=AXIS2_PLACEMENT_3D ( 'NONE', #15356, #2999, #57779 ) ;
#49479=ORIENTED_EDGE ( 'NONE', *, *, #29751, .F. ) ;
#49482=LINE ( 'NONE', #1048, #44741 ) ;
#49483=EDGE_CURVE ( 'NONE', #12124, #26706, #32661, .T. ) ;
#49494=VERTEX_POINT ( 'NONE', #32388 ) ;
#49500=CARTESIAN_POINT ( 'NONE',  ( 283.0000000000000568, -38.64999999999999858, -12.69999999999999929 ) ) ;
#49504=LINE ( 'NONE', #38881, #12029 ) ;
#49552=ORIENTED_EDGE ( 'NONE', *, *, #28315, .F. ) ;
#49564=EDGE_LOOP ( 'NONE', ( #37112, #35810, #50755, #23163 ) ) ;
#49567=CARTESIAN_POINT ( 'NONE',  ( 283.0000000000000568, -38.65000000000095781, -15.00000000000000000 ) ) ;
#49588=ORIENTED_EDGE ( 'NONE', *, *, #16806, .F. ) ;
#49592=EDGE_CURVE ( 'NONE', #66065, #51967, #9353, .T. ) ;
#49614=ADVANCED_FACE ( 'NONE', ( #62737 ), #30229, .F. ) ;
#49633=CARTESIAN_POINT ( 'NONE',  ( 7.000000000000000000, -38.64999999999999858, 12.69999999999999929 ) ) ;
#49636=DIRECTION ( 'NONE',  ( 1.000000000000000000, 0.000000000000000000, 0.000000000000000000 ) ) ;
#49656=EDGE_LOOP ( 'NONE', ( #2160, #13069, #42367, #64673 ) ) ;
#49663=AXIS2_PLACEMENT_3D ( 'NONE', #34032, #2215, #61243 ) ;
#49667=EDGE_CURVE ( 'NONE', #37106, #7061, #54845, .T. ) ;
#49677=ORIENTED_EDGE ( 'NONE', *, *, #4202, .F. ) ;
#49696=VECTOR ( 'NONE', #56050, 1000.000000000000000 ) ;
#49699=FACE_OUTER_BOUND ( 'NONE', #35437, .T. ) ;
#49705=PLANE ( 'NONE',  #20374 ) ;
#49715=ORIENTED_EDGE ( 'NONE', *, *, #46973, .F. ) ;
#49716=AXIS2_PLACEMENT_3D ( 'NONE', #2454, #13412, #35308 ) ;
#49720=CARTESIAN_POINT ( 'NONE',  ( 283.0000000000000568, -25.60000000000000142, -17.60000000000000142 ) ) ;
#49738=ORIENTED_EDGE ( 'NONE', *, *, #23877, .F. ) ;
#49739=CIRCLE ( 'NONE', #19251, 0.5000000000009459100 ) ;
#49743=AXIS2_PLACEMENT_3D ( 'NONE', #44176, #12681, #34254 ) ;
#49777=EDGE_CURVE ( 'NONE', #288, #7467, #12365, .T. ) ;
#49793=DIRECTION ( 'NONE',  ( 0.000000000000000000, 1.000000000000000000, 0.000000000000000000 ) ) ;
#49800=CIRCLE ( 'NONE', #36281, 0.5000000000023407942 ) ;
#49806=CARTESIAN_POINT ( 'NONE',  ( 7.000000000000000000, -38.15000000000000568, 13.19999999999999929 ) ) ;
#49807=ORIENTED_EDGE ( 'NONE', *, *, #40003, .T. ) ;
#49812=LINE ( 'NONE', #23282, #6470 ) ;
#49817=AXIS2_PLACEMENT_3D ( 'NONE', #59536, #26307, #16392 ) ;
#49818=PLANE ( 'NONE',  #11810 ) ;
#49822=ORIENTED_EDGE ( 'NONE', *, *, #54017, .T. ) ;
#49849=CARTESIAN_POINT ( 'NONE',  ( 283.0000000000000568, -32.45000000000000995, -12.69999999999999929 ) ) ;
#49850=DIRECTION ( 'NONE',  ( 0.7071067811865475727, -0.7071067811865475727, 0.000000000000000000 ) ) ;
#49859=VECTOR ( 'NONE', #37217, 1000.000000000000000 ) ;
#49862=ORIENTED_EDGE ( 'NONE', *, *, #51576, .F. ) ;
#49883=DIRECTION ( 'NONE',  ( -1.000000000000000000, 0.000000000000000000, 0.000000000000000000 ) ) ;
#49891=ORIENTED_EDGE ( 'NONE', *, *, #69147, .T. ) ;
#49901=VERTEX_POINT ( 'NONE', #56228 ) ;
#49912=EDGE_CURVE ( 'NONE', #28510, #19038, #40654, .T. ) ;
#49947=CARTESIAN_POINT ( 'NONE',  ( 276.8000000000000682, -20.40000000000000213, 17.60000000000000142 ) ) ;
#49948=CARTESIAN_POINT ( 'NONE',  ( 275.0000000000000000, -20.50000000000000000, -17.00000000000000000 ) ) ;
#49952=ORIENTED_EDGE ( 'NONE', *, *, #27846, .T. ) ;
#49967=ORIENTED_EDGE ( 'NONE', *, *, #41471, .T. ) ;
#49978=ORIENTED_EDGE ( 'NONE', *, *, #3929, .T. ) ;
#49986=CARTESIAN_POINT ( 'NONE',  ( 7.000000000000000000, -32.95000000000000284, 7.700000000000000178 ) ) ;
#49989=EDGE_CURVE ( 'NONE', #24682, #52181, #47013, .T. ) ;
#49993=VERTEX_POINT ( 'NONE', #47713 ) ;
#50007=DIRECTION ( 'NONE',  ( 0.000000000000000000, 0.000000000000000000, -1.000000000000000000 ) ) ;
#50043=CARTESIAN_POINT ( 'NONE',  ( 283.0000000000000568, -25.60000000000000142, 17.60000000000000142 ) ) ;
#50048=ORIENTED_EDGE ( 'NONE', *, *, #59324, .F. ) ;
#50071=DIRECTION ( 'NONE',  ( -1.000000000000000000, 0.000000000000000000, 0.000000000000000000 ) ) ;
#50082=PLANE ( 'NONE',  #55297 ) ;
#50097=AXIS2_PLACEMENT_3D ( 'NONE', #69833, #58883, #53932 ) ;
#50102=ORIENTED_EDGE ( 'NONE', *, *, #69960, .F. ) ;
#50113=ORIENTED_EDGE ( 'NONE', *, *, #21994, .F. ) ;
#50118=CARTESIAN_POINT ( 'NONE',  ( 15.00000000000000000, -21.00000000000000000, 0.000000000000000000 ) ) ;
#50124=DIRECTION ( 'NONE',  ( -1.000000000000000000, 0.000000000000000000, 0.000000000000000000 ) ) ;
#50132=EDGE_CURVE ( 'NONE', #21706, #9319, #28223, .T. ) ;
#50185=VECTOR ( 'NONE', #31829, 1000.000000000000114 ) ;
#50190=DIRECTION ( 'NONE',  ( 0.000000000000000000, 0.000000000000000000, 1.000000000000000000 ) ) ;
#50202=ORIENTED_EDGE ( 'NONE', *, *, #35388, .F. ) ;
#50218=AXIS2_PLACEMENT_3D ( 'NONE', #14434, #36697, #67481 ) ;
#50229=ORIENTED_EDGE ( 'NONE', *, *, #58771, .T. ) ;
#50232=LINE ( 'NONE', #14046, #65456 ) ;
#50236=ORIENTED_EDGE ( 'NONE', *, *, #3434, .F. ) ;
#50255=CARTESIAN_POINT ( 'NONE',  ( 283.0000000000000568, -20.50000000000000000, 13.00000000000000178 ) ) ;
#50257=EDGE_LOOP ( 'NONE', ( #44664, #21238, #61983, #48849, #25804, #28959 ) ) ;
#50280=CARTESIAN_POINT ( 'NONE',  ( 7.000000000000000000, -23.29603921945599865, -12.50000000000000000 ) ) ;
#50291=CARTESIAN_POINT ( 'NONE',  ( 7.000000000000000000, -39.80000000000000426, 12.69999999999999929 ) ) ;
#50298=EDGE_CURVE ( 'NONE', #67535, #61781, #35244, .T. ) ;
#50305=EDGE_CURVE ( 'NONE', #38230, #39720, #3448, .T. ) ;
#50318=DIRECTION ( 'NONE',  ( 0.000000000000000000, 0.000000000000000000, -1.000000000000000000 ) ) ;
#50319=VERTEX_POINT ( 'NONE', #67794 ) ;
#50343=ORIENTED_EDGE ( 'NONE', *, *, #27494, .F. ) ;
#50345=ORIENTED_EDGE ( 'NONE', *, *, #44954, .F. ) ;
#50356=AXIS2_PLACEMENT_3D ( 'NONE', #29382, #39311, #51305 ) ;
#50357=CARTESIAN_POINT ( 'NONE',  ( 283.0000000000000568, -39.80000000000000426, 8.400000000000000355 ) ) ;
#50369=ORIENTED_EDGE ( 'NONE', *, *, #13231, .F. ) ;
#50386=CARTESIAN_POINT ( 'NONE',  ( 7.000000000000000000, -38.15000000000000568, -14.50000000000000000 ) ) ;
#50389=CIRCLE ( 'NONE', #19913, 0.4999999999979497511 ) ;
#50405=FACE_OUTER_BOUND ( 'NONE', #50622, .T. ) ;
#50407=LINE ( 'NONE', #7616, #37506 ) ;
#50430=DIRECTION ( 'NONE',  ( 0.000000000000000000, -1.000000000000000000, 0.000000000000000000 ) ) ;
#50437=CARTESIAN_POINT ( 'NONE',  ( 275.0000000000000000, -27.13000000000000611, 13.50000000000000000 ) ) ;
#50479=ORIENTED_EDGE ( 'NONE', *, *, #24933, .T. ) ;
#50505=AXIS2_PLACEMENT_3D ( 'NONE', #33699, #43964, #66232 ) ;
#50506=VECTOR ( 'NONE', #8618, 1000.000000000000000 ) ;
#50519=ORIENTED_EDGE ( 'NONE', *, *, #47887, .F. ) ;
#50525=CARTESIAN_POINT ( 'NONE',  ( 275.0000000000000000, -30.45000000000094786, 14.49999999999906031 ) ) ;
#50528=ORIENTED_EDGE ( 'NONE', *, *, #64152, .F. ) ;
#50538=ORIENTED_EDGE ( 'NONE', *, *, #24933, .F. ) ;
#50542=ADVANCED_FACE ( 'NONE', ( #59969 ), #27454, .F. ) ;
#50546=ORIENTED_EDGE ( 'NONE', *, *, #27846, .F. ) ;
#50554=CARTESIAN_POINT ( 'NONE',  ( 3.552713678800500929E-15, -0.4999999999999964473, 26.50000000000000355 ) ) ;
#50563=ORIENTED_EDGE ( 'NONE', *, *, #62701, .F. ) ;
#50579=CIRCLE ( 'NONE', #49475, 8.000000000000000000 ) ;
#50580=CARTESIAN_POINT ( 'NONE',  ( 275.0000000000000000, -40.30000000000000426, -12.20000000000000107 ) ) ;
#50581=VERTEX_POINT ( 'NONE', #22154 ) ;
#50584=ORIENTED_EDGE ( 'NONE', *, *, #45695, .F. ) ;
#50587=DIRECTION ( 'NONE',  ( 1.000000000000000000, 0.000000000000000000, 0.000000000000000000 ) ) ;
#50613=CARTESIAN_POINT ( 'NONE',  ( 283.0000000000000568, -37.61196062927500350, 8.008708659369300875 ) ) ;
#50622=EDGE_LOOP ( 'NONE', ( #18220, #16987, #29397 ) ) ;
#50626=ORIENTED_EDGE ( 'NONE', *, *, #30616, .F. ) ;
#50655=AXIS2_PLACEMENT_3D ( 'NONE', #25069, #46619, #34257 ) ;
#50672=CARTESIAN_POINT ( 'NONE',  ( 7.000000000000000000, -42.50000000000000000, 15.10000000000000142 ) ) ;
#50682=EDGE_LOOP ( 'NONE', ( #60804, #50626, #44164, #69043, #25729 ) ) ;
#50688=EDGE_CURVE ( 'NONE', #69932, #69253, #66661, .T. ) ;
#50699=DIRECTION ( 'NONE',  ( 0.000000000000000000, 0.000000000000000000, 1.000000000000000000 ) ) ;
#50718=DIRECTION ( 'NONE',  ( -1.000000000000000000, 0.000000000000000000, 0.000000000000000000 ) ) ;
#50748=DIRECTION ( 'NONE',  ( 0.000000000000000000, -1.901256929667050114E-12, 1.000000000000000000 ) ) ;
#50751=DIRECTION ( 'NONE',  ( 0.000000000000000000, 1.000000000000000000, 0.000000000000000000 ) ) ;
#50752=ORIENTED_EDGE ( 'NONE', *, *, #21520, .F. ) ;
#50755=ORIENTED_EDGE ( 'NONE', *, *, #57006, .T. ) ;
#50767=EDGE_LOOP ( 'NONE', ( #51755, #6740, #36529, #19329 ) ) ;
#50769=ORIENTED_EDGE ( 'NONE', *, *, #9444, .F. ) ;
#50770=DIRECTION ( 'NONE',  ( 0.000000000000000000, -1.000000000000000000, -7.802196388977322746E-10 ) ) ;
#50779=ADVANCED_FACE ( 'NONE', ( #50405 ), #23530, .F. ) ;
#50782=EDGE_CURVE ( 'NONE', #32093, #31208, #4076, .T. ) ;
#50786=AXIS2_PLACEMENT_3D ( 'NONE', #16774, #38342, #27726 ) ;
#50800=CARTESIAN_POINT ( 'NONE',  ( 14.50000000000000000, -42.00000000000000000, -27.00000000000000000 ) ) ;
#50802=CARTESIAN_POINT ( 'NONE',  ( 283.0000000000000568, -32.45000000000000995, 15.00000000000000000 ) ) ;
#50809=LINE ( 'NONE', #29945, #1409 ) ;
#50823=CARTESIAN_POINT ( 'NONE',  ( 283.0000000000000568, -32.46196062927499781, 8.091291340630698770 ) ) ;
#50848=ORIENTED_EDGE ( 'NONE', *, *, #37480, .F. ) ;
#50855=DIRECTION ( 'NONE',  ( 0.000000000000000000, 1.000000000000000000, 0.000000000000000000 ) ) ;
#50862=ORIENTED_EDGE ( 'NONE', *, *, #17185, .F. ) ;
#50866=CARTESIAN_POINT ( 'NONE',  ( 275.0000000000000000, -32.45000000000000995, -15.00000000000000000 ) ) ;
#50875=PLANE ( 'NONE',  #36955 ) ;
#50912=CARTESIAN_POINT ( 'NONE',  ( 10.14575131106465378, -20.50000000000000000, 17.00000000000000000 ) ) ;
#50924=VERTEX_POINT ( 'NONE', #59889 ) ;
#50939=VERTEX_POINT ( 'NONE', #166 ) ;
#50940=DIRECTION ( 'NONE',  ( -0.000000000000000000, -1.000000000000000000, -0.000000000000000000 ) ) ;
#50947=LINE ( 'NONE', #7803, #17446 ) ;
#50967=EDGE_CURVE ( 'NONE', #64136, #9816, #37644, .T. ) ;
#50968=DIRECTION ( 'NONE',  ( -1.000000000000000000, 0.000000000000000000, 0.000000000000000000 ) ) ;
#50969=CYLINDRICAL_SURFACE ( 'NONE', #31697, 0.5000000000009302559 ) ;
#50975=LINE ( 'NONE', #45655, #41371 ) ;
#50989=LINE ( 'NONE', #50291, #23867 ) ;
#51000=EDGE_LOOP ( 'NONE', ( #64741, #496, #2448, #24928, #45526, #12168, #51752, #35217, #60367, #1633 ) ) ;
#51014=LINE ( 'NONE', #39359, #22708 ) ;
#51027=CARTESIAN_POINT ( 'NONE',  ( 289.7499999999998863, -0.2499999999999431288, 26.74999999999993250 ) ) ;
#51043=VECTOR ( 'NONE', #59360, 1000.000000000000000 ) ;
#51048=EDGE_CURVE ( 'NONE', #2551, #11956, #13656, .T. ) ;
#51049=DIRECTION ( 'NONE',  ( 0.000000000000000000, 0.000000000000000000, 1.000000000000000000 ) ) ;
#51056=EDGE_CURVE ( 'NONE', #67984, #18617, #49800, .T. ) ;
#51064=CARTESIAN_POINT ( 'NONE',  ( 275.0000000000000000, -31.30000000000000071, 8.400000000000000355 ) ) ;
#51069=CARTESIAN_POINT ( 'NONE',  ( 7.000000000000000000, -30.45000000000000639, -15.00000000000000000 ) ) ;
#51084=EDGE_CURVE ( 'NONE', #11694, #41475, #51014, .T. ) ;
#51090=EDGE_CURVE ( 'NONE', #21069, #135, #6825, .T. ) ;
#51102=EDGE_CURVE ( 'NONE', #29889, #35918, #43044, .T. ) ;
#51116=VECTOR ( 'NONE', #36965, 1000.000000000000000 ) ;
#51144=DIRECTION ( 'NONE',  ( 0.000000000000000000, 0.000000000000000000, -1.000000000000000000 ) ) ;
#51146=ORIENTED_EDGE ( 'NONE', *, *, #7773, .F. ) ;
#51174=CARTESIAN_POINT ( 'NONE',  ( 7.000000000000000000, -40.30000000000000426, -12.20000000000000107 ) ) ;
#51185=CIRCLE ( 'NONE', #33126, 1.999999999999314770 ) ;
#51201=DIRECTION ( 'NONE',  ( 1.000000000000000000, 0.000000000000000000, 0.000000000000000000 ) ) ;
#51207=CARTESIAN_POINT ( 'NONE',  ( 283.0000000000000568, -32.44999999999905071, -14.49999999999906031 ) ) ;
#51218=CARTESIAN_POINT ( 'NONE',  ( 289.7500000000000000, -0.2500000000000000000, -26.75000000000000000 ) ) ;
#51244=DIRECTION ( 'NONE',  ( 0.5773502691896257311, -0.5773502691896257311, -0.5773502691896257311 ) ) ;
#51245=CARTESIAN_POINT ( 'NONE',  ( 275.0000000000000000, -27.13000000000000611, -15.49999999999930012 ) ) ;
#51253=DIRECTION ( 'NONE',  ( 1.000000000000000000, -0.000000000000000000, -0.000000000000000000 ) ) ;
#51269=LINE ( 'NONE', #13081, #8819 ) ;
#51273=FACE_OUTER_BOUND ( 'NONE', #69702, .T. ) ;
#51289=VECTOR ( 'NONE', #47816, 1000.000000000000000 ) ;
#51305=DIRECTION ( 'NONE',  ( -1.000000000000000000, 0.000000000000000000, 0.000000000000000000 ) ) ;
#51314=DIRECTION ( 'NONE',  ( 0.5773502691896257311, 0.5773502691896257311, 0.5773502691896257311 ) ) ;
#51360=EDGE_LOOP ( 'NONE', ( #58780, #23383, #45174, #27912 ) ) ;
#51365=VECTOR ( 'NONE', #47430, 1000.000000000000000 ) ;
#51396=PLANE ( 'NONE',  #54226 ) ;
#51474=ORIENTED_EDGE ( 'NONE', *, *, #52517, .F. ) ;
#51476=CARTESIAN_POINT ( 'NONE',  ( 275.0000000000000000, -31.30000000000000071, -12.69999999999999929 ) ) ;
#51482=ORIENTED_EDGE ( 'NONE', *, *, #19765, .F. ) ;
#51493=AXIS2_PLACEMENT_3D ( 'NONE', #4919, #26482, #48045 ) ;
#51511=DIRECTION ( 'NONE',  ( 0.000000000000000000, -1.000000000000000000, -1.922073611378672844E-12 ) ) ;
#51516=ORIENTED_EDGE ( 'NONE', *, *, #22120, .T. ) ;
#51524=DIRECTION ( 'NONE',  ( -1.000000000000000000, 0.000000000000000000, 0.000000000000000000 ) ) ;
#51531=CARTESIAN_POINT ( 'NONE',  ( 0.2500000000000000000, -0.2499999999999970302, -26.75000000000000000 ) ) ;
#51534=CARTESIAN_POINT ( 'NONE',  ( 275.2500000000000000, -42.25000000000000000, -26.75000000000000000 ) ) ;
#51539=ORIENTED_EDGE ( 'NONE', *, *, #31831, .F. ) ;
#51547=ADVANCED_FACE ( 'NONE', ( #24050 ), #39278, .F. ) ;
#51559=STYLED_ITEM ( 'NONE', ( #17334 ), #20363 ) ;
#51569=SHAPE_DEFINITION_REPRESENTATION ( #13649, #64253 ) ;
#51576=EDGE_CURVE ( 'NONE', #40696, #39543, #60834, .T. ) ;
#51579=DIRECTION ( 'NONE',  ( -0.7071067811865474617, 0.7071067811865474617, 0.000000000000000000 ) ) ;
#51581=ORIENTED_EDGE ( 'NONE', *, *, #12897, .F. ) ;
#51601=CARTESIAN_POINT ( 'NONE',  ( 283.0000000000000568, -23.65000000000000568, 12.40000000000000213 ) ) ;
#51611=CARTESIAN_POINT ( 'NONE',  ( 282.6457513110646005, -25.50000000000000355, 17.00000000000000000 ) ) ;
#51620=VECTOR ( 'NONE', #28540, 1000.000000000000000 ) ;
#51624=AXIS2_PLACEMENT_3D ( 'NONE', #41091, #45340, #66912 ) ;
#51635=CARTESIAN_POINT ( 'NONE',  ( 7.000000000000000000, -30.80000000000000071, 12.20000000000000107 ) ) ;
#51639=ADVANCED_FACE ( 'NONE', ( #66148 ), #59290, .F. ) ;
#51642=ORIENTED_EDGE ( 'NONE', *, *, #23682, .F. ) ;
#51656=DIRECTION ( 'NONE',  ( 0.000000000000000000, 1.000000000000000000, 0.000000000000000000 ) ) ;
#51659=ORIENTED_EDGE ( 'NONE', *, *, #9454, .T. ) ;
#51664=ORIENTED_EDGE ( 'NONE', *, *, #51102, .T. ) ;
#51673=CARTESIAN_POINT ( 'NONE',  ( 289.5000000000000000, 0.000000000000000000, 26.50000000000000000 ) ) ;
#51675=EDGE_CURVE ( 'NONE', #19785, #58687, #54416, .T. ) ;
#51677=VECTOR ( 'NONE', #50968, 1000.000000000000000 ) ;
#51680=DIRECTION ( 'NONE',  ( -1.000000000000000000, 0.000000000000000000, 0.000000000000000000 ) ) ;
#51692=LINE ( 'NONE', #40720, #8623 ) ;
#51698=ADVANCED_FACE ( 'NONE', ( #31396 ), #48758, .T. ) ;
#51700=ORIENTED_EDGE ( 'NONE', *, *, #58383, .F. ) ;
#51703=DIRECTION ( 'NONE',  ( 0.000000000000000000, 0.000000000000000000, -1.000000000000000000 ) ) ;
#51715=ORIENTED_EDGE ( 'NONE', *, *, #49912, .T. ) ;
#51726=VERTEX_POINT ( 'NONE', #15476 ) ;
#51735=DIRECTION ( 'NONE',  ( 0.000000000000000000, 0.000000000000000000, -1.000000000000000000 ) ) ;
#51744=DIRECTION ( 'NONE',  ( 0.000000000000000000, 0.000000000000000000, -1.000000000000000000 ) ) ;
#51747=ORIENTED_EDGE ( 'NONE', *, *, #31827, .F. ) ;
#51751=EDGE_LOOP ( 'NONE', ( #14672, #11372, #58053 ) ) ;
#51752=ORIENTED_EDGE ( 'NONE', *, *, #42701, .F. ) ;
#51755=ORIENTED_EDGE ( 'NONE', *, *, #33387, .T. ) ;
#51757=CARTESIAN_POINT ( 'NONE',  ( 283.0000000000000568, -26.28355339059299922, 9.766446609406699508 ) ) ;
#51763=FACE_BOUND ( 'NONE', #52145, .T. ) ;
#51766=CARTESIAN_POINT ( 'NONE',  ( 283.0000000000000568, -20.40000000000000213, -12.40000000000000213 ) ) ;
#51769=DIRECTION ( 'NONE',  ( 0.5773502691896175154, 0.5773502691896339467, -0.5773502691896257311 ) ) ;
#51797=ORIENTED_EDGE ( 'NONE', *, *, #30187, .F. ) ;
#51805=ORIENTED_EDGE ( 'NONE', *, *, #6172, .F. ) ;
#51810=ORIENTED_EDGE ( 'NONE', *, *, #3929, .F. ) ;
#51812=LINE ( 'NONE', #28827, #13757 ) ;
#51826=VERTEX_POINT ( 'NONE', #43730 ) ;
#51831=ORIENTED_EDGE ( 'NONE', *, *, #15503, .F. ) ;
#51836=ORIENTED_EDGE ( 'NONE', *, *, #26448, .F. ) ;
#51840=DIRECTION ( 'NONE',  ( 0.000000000000000000, -1.000000000000000000, 0.000000000000000000 ) ) ;
#51857=CARTESIAN_POINT ( 'NONE',  ( 290.0000000000000000, 0.000000000000000000, 27.00000000000000000 ) ) ;
#51875=DIRECTION ( 'NONE',  ( 0.000000000000000000, 0.000000000000000000, -1.000000000000000000 ) ) ;
#51879=CARTESIAN_POINT ( 'NONE',  ( 290.0000000000000000, 0.000000000000000000, 0.000000000000000000 ) ) ;
#51888=ORIENTED_EDGE ( 'NONE', *, *, #50967, .T. ) ;
#51904=VERTEX_POINT ( 'NONE', #35903 ) ;
#51911=VECTOR ( 'NONE', #56605, 1000.000000000000000 ) ;
#51913=DIRECTION ( 'NONE',  ( 1.000000000000000000, -0.000000000000000000, -0.000000000000000000 ) ) ;
#51916=ORIENTED_EDGE ( 'NONE', *, *, #5210, .F. ) ;
#51944=EDGE_CURVE ( 'NONE', #27522, #53301, #51812, .T. ) ;
#51963=DIRECTION ( 'NONE',  ( -1.000000000000000000, 0.000000000000000000, 0.000000000000000000 ) ) ;
#51967=VERTEX_POINT ( 'NONE', #23537 ) ;
#51973=DIRECTION ( 'NONE',  ( 0.000000000000000000, 0.000000000000000000, -1.000000000000000000 ) ) ;
#51974=CIRCLE ( 'NONE', #30520, 0.5000000000004167777 ) ;
#51986=DIRECTION ( 'NONE',  ( 0.000000000000000000, 0.000000000000000000, 1.000000000000000000 ) ) ;
#51988=ORIENTED_EDGE ( 'NONE', *, *, #26777, .F. ) ;
#51989=EDGE_CURVE ( 'NONE', #31769, #37208, #54464, .T. ) ;
#51994=ORIENTED_EDGE ( 'NONE', *, *, #29112, .F. ) ;
#51999=EDGE_CURVE ( 'NONE', #31208, #58107, #3033, .T. ) ;
#52017=DIRECTION ( 'NONE',  ( -1.000000000000000000, 0.000000000000000000, 0.000000000000000000 ) ) ;
#52025=VECTOR ( 'NONE', #62984, 1000.000000000000000 ) ;
#52080=CARTESIAN_POINT ( 'NONE',  ( 15.00000000000000000, -42.00000000000000000, -15.10000000000000142 ) ) ;
#52104=CARTESIAN_POINT ( 'NONE',  ( 7.000000000000000000, -25.60000000000000142, 15.10000000000000142 ) ) ;
#52106=VERTEX_POINT ( 'NONE', #14681 ) ;
#52117=CARTESIAN_POINT ( 'NONE',  ( 7.000000000000000000, -26.50000000000000000, 5.809475019311129529 ) ) ;
#52125=PLANE ( 'NONE',  #18791 ) ;
#52145=EDGE_LOOP ( 'NONE', ( #1078, #29146, #18048, #14766 ) ) ;
#52156=VECTOR ( 'NONE', #7211, 1000.000000000000000 ) ;
#52162=DIRECTION ( 'NONE',  ( 0.000000000000000000, -0.7051282051282052876, -0.7090798363602477394 ) ) ;
#52181=VERTEX_POINT ( 'NONE', #4781 ) ;
#52189=EDGE_CURVE ( 'NONE', #45523, #13089, #53358, .T. ) ;
#52200=ORIENTED_EDGE ( 'NONE', *, *, #56244, .T. ) ;
#52203=CARTESIAN_POINT ( 'NONE',  ( 7.000000000000000000, -41.99999999999906208, -14.49999999999903899 ) ) ;
#52220=ORIENTED_EDGE ( 'NONE', *, *, #56678, .T. ) ;
#52243=EDGE_CURVE ( 'NONE', #520, #22636, #6524, .T. ) ;
#52254=ORIENTED_EDGE ( 'NONE', *, *, #19014, .F. ) ;
#52259=DIRECTION ( 'NONE',  ( -1.000000000000000000, 0.000000000000000000, 0.000000000000000000 ) ) ;
#52261=LINE ( 'NONE', #47650, #23307 ) ;
#52263=DIRECTION ( 'NONE',  ( 0.5773502691896257311, -0.5773502691896257311, -0.5773502691896257311 ) ) ;
#52266=ORIENTED_EDGE ( 'NONE', *, *, #11155, .F. ) ;
#52288=CARTESIAN_POINT ( 'NONE',  ( 282.7711612342632179, -25.38939884375893641, -17.11060115624107425 ) ) ;
#52295=DIRECTION ( 'NONE',  ( 0.000000000000000000, 0.000000000000000000, -1.000000000000000000 ) ) ;
#52300=CARTESIAN_POINT ( 'NONE',  ( 283.0000000000000568, -25.50000000000000355, 17.00000000000000000 ) ) ;
#52329=PLANE ( 'NONE',  #52961 ) ;
#52330=ORIENTED_EDGE ( 'NONE', *, *, #16945, .F. ) ;
#52342=ORIENTED_EDGE ( 'NONE', *, *, #37897, .T. ) ;
#52349=LINE ( 'NONE', #42687, #67012 ) ;
#52363=LINE ( 'NONE', #35372, #19710 ) ;
#52390=CARTESIAN_POINT ( 'NONE',  ( 280.0000000000000000, -20.49999999999999645, -20.00000000000000000 ) ) ;
#52409=VECTOR ( 'NONE', #9292, 1000.000000000000000 ) ;
#52414=CARTESIAN_POINT ( 'NONE',  ( 275.2500000000000000, -0.2499999999999893141, -26.74999999999999645 ) ) ;
#52419=DIRECTION ( 'NONE',  ( -1.000000000000000000, 0.000000000000000000, 0.000000000000000000 ) ) ;
#52429=EDGE_CURVE ( 'NONE', #33919, #46313, #2238, .T. ) ;
#52434=CIRCLE ( 'NONE', #67094, 0.5000000000009459100 ) ;
#52439=VERTEX_POINT ( 'NONE', #3289 ) ;
#52441=ORIENTED_EDGE ( 'NONE', *, *, #41043, .F. ) ;
#52442=EDGE_CURVE ( 'NONE', #68520, #46672, #40048, .T. ) ;
#52464=ORIENTED_EDGE ( 'NONE', *, *, #12640, .T. ) ;
#52478=ORIENTED_EDGE ( 'NONE', *, *, #66181, .T. ) ;
#52490=CARTESIAN_POINT ( 'NONE',  ( 7.500000000000000000, -53.81370849898476649, -16.00000000000000000 ) ) ;
#52492=VECTOR ( 'NONE', #21576, 1000.000000000000000 ) ;
#52494=ORIENTED_EDGE ( 'NONE', *, *, #35278, .T. ) ;
#52515=CARTESIAN_POINT ( 'NONE',  ( 10.62249899919920004, -25.00000000000000000, 17.50000000000000000 ) ) ;
#52517=EDGE_CURVE ( 'NONE', #39720, #42310, #3997, .T. ) ;
#52518=EDGE_CURVE ( 'NONE', #10988, #54968, #48181, .T. ) ;
#52522=VERTEX_POINT ( 'NONE', #30862 ) ;
#52542=LINE ( 'NONE', #26366, #40091 ) ;
#52562=CARTESIAN_POINT ( 'NONE',  ( 15.00000000000000000, 0.000000000000000000, 27.00000000000000000 ) ) ;
#52581=CARTESIAN_POINT ( 'NONE',  ( 14.50000000000000000, -42.50000000000000000, -15.10000000000000142 ) ) ;
#52586=ORIENTED_EDGE ( 'NONE', *, *, #62428, .F. ) ;
#52588=CARTESIAN_POINT ( 'NONE',  ( 275.0000000000000000, -0.5000000000000000000, 26.50000000000000000 ) ) ;
#52601=DIRECTION ( 'NONE',  ( 0.000000000000000000, 0.9760787414516765015, 0.2174173187354474512 ) ) ;
#52617=PLANE ( 'NONE',  #8775 ) ;
#52642=AXIS2_PLACEMENT_3D ( 'NONE', #23886, #28825, #50748 ) ;
#52648=FACE_OUTER_BOUND ( 'NONE', #67070, .T. ) ;
#52677=VECTOR ( 'NONE', #14037, 999.9999999999998863 ) ;
#52684=EDGE_CURVE ( 'NONE', #26683, #18078, #6132, .T. ) ;
#52702=ORIENTED_EDGE ( 'NONE', *, *, #29694, .F. ) ;
#52710=CIRCLE ( 'NONE', #34597, 0.3000000000005387246 ) ;
#52712=CARTESIAN_POINT ( 'NONE',  ( 7.000000000000000000, -42.50000000000000000, 10.20000000000000107 ) ) ;
#52714=ORIENTED_EDGE ( 'NONE', *, *, #47956, .T. ) ;
#52729=AXIS2_PLACEMENT_3D ( 'NONE', #15617, #26212, #53791 ) ;
#52740=ORIENTED_EDGE ( 'NONE', *, *, #51084, .T. ) ;
#52771=CARTESIAN_POINT ( 'NONE',  ( 0.000000000000000000, -42.00000000000000000, -26.50000000000000000 ) ) ;
#52772=DIRECTION ( 'NONE',  ( 0.000000000000000000, -0.7071067811865077157, 0.7071067811865873187 ) ) ;
#52774=VECTOR ( 'NONE', #8136, 1000.000000000000000 ) ;
#52775=VERTEX_POINT ( 'NONE', #23720 ) ;
#52783=EDGE_CURVE ( 'NONE', #16805, #38091, #64841, .T. ) ;
#52789=DIRECTION ( 'NONE',  ( 1.000000000000000000, -0.000000000000000000, -0.000000000000000000 ) ) ;
#52791=PLANE ( 'NONE',  #49062 ) ;
#52794=ORIENTED_EDGE ( 'NONE', *, *, #26789, .T. ) ;
#52797=EDGE_LOOP ( 'NONE', ( #9686, #25743, #54189, #51659 ) ) ;
#52805=CARTESIAN_POINT ( 'NONE',  ( 275.0000000000000000, -23.65000000000000568, 12.40000000000000213 ) ) ;
#52807=ORIENTED_EDGE ( 'NONE', *, *, #45184, .F. ) ;
#52813=FACE_OUTER_BOUND ( 'NONE', #32712, .T. ) ;
#52826=ORIENTED_EDGE ( 'NONE', *, *, #54242, .T. ) ;
#52835=AXIS2_PLACEMENT_3D ( 'NONE', #42648, #16479, #54309 ) ;
#52867=CARTESIAN_POINT ( 'NONE',  ( 283.0000000000000568, -30.45000000000000639, -15.00000000000000000 ) ) ;
#52874=DIRECTION ( 'NONE',  ( 1.000000000000000000, -0.000000000000000000, -0.000000000000000000 ) ) ;
#52883=DIRECTION ( 'NONE',  ( -1.000000000000000000, 0.000000000000000000, 0.000000000000000000 ) ) ;
#52891=EDGE_LOOP ( 'NONE', ( #32782, #39279, #34179, #30330, #62664, #53249, #12757, #34779, #19916, #61371, #54653, #50752, #33049, #7198, #25123, #42006, #65906, #7033, #20638, #35859, #11134, #12374, #47904, #20269, #68663, #14179, #34656, #10420, #2262, #36525, #59610, #24846, #54630, #64763 ) ) ;
#52898=LINE ( 'NONE', #16091, #6563 ) ;
#52928=EDGE_CURVE ( 'NONE', #41344, #520, #58370, .T. ) ;
#52937=CARTESIAN_POINT ( 'NONE',  ( 15.00000000000000000, -21.00000000000000000, 0.000000000000000000 ) ) ;
#52947=CARTESIAN_POINT ( 'NONE',  ( 290.0000000000000000, -42.00000000000000000, -26.50000000000000000 ) ) ;
#52950=CARTESIAN_POINT ( 'NONE',  ( 283.0000000000000568, -32.95000000000000284, -13.19999999999999929 ) ) ;
#52954=CARTESIAN_POINT ( 'NONE',  ( 7.000000000000000000, -32.95000000000000284, -7.700000000000000178 ) ) ;
#52958=VECTOR ( 'NONE', #20292, 1000.000000000000000 ) ;
#52960=ORIENTED_EDGE ( 'NONE', *, *, #44659, .T. ) ;
#52961=AXIS2_PLACEMENT_3D ( 'NONE', #20148, #41709, #63284 ) ;
#52966=EDGE_CURVE ( 'NONE', #66065, #54243, #61466, .T. ) ;
#52973=LINE ( 'NONE', #6843, #32163 ) ;
#52987=LINE ( 'NONE', #37755, #58193 ) ;
#52989=CARTESIAN_POINT ( 'NONE',  ( 283.0000000000000568, -23.65000000000000568, -12.40000000000000213 ) ) ;
#52990=ORIENTED_EDGE ( 'NONE', *, *, #42043, .T. ) ;
#52999=CARTESIAN_POINT ( 'NONE',  ( 7.000000000000000000, -42.50000000000000000, 9.700000000000002842 ) ) ;
#53004=DIRECTION ( 'NONE',  ( 0.000000000000000000, 0.000000000000000000, -1.000000000000000000 ) ) ;
#53042=VECTOR ( 'NONE', #9226, 1000.000000000000000 ) ;
#53045=CARTESIAN_POINT ( 'NONE',  ( 275.0000000000000000, -25.60000000000000142, 15.10000000000000142 ) ) ;
#53055=VERTEX_POINT ( 'NONE', #15225 ) ;
#53057=CARTESIAN_POINT ( 'NONE',  ( 290.0000000000000000, -0.5000000000000000000, 26.50000000000000000 ) ) ;
#53058=LINE ( 'NONE', #4616, #65183 ) ;
#53080=CARTESIAN_POINT ( 'NONE',  ( 7.000000000000000000, -32.45000000000000995, 12.69999999999999929 ) ) ;
#53081=CARTESIAN_POINT ( 'NONE',  ( 283.0000000000000568, -32.95000000000000284, 14.50000000000000000 ) ) ;
#53082=EDGE_CURVE ( 'NONE', #57476, #50581, #28496, .T. ) ;
#53098=DIRECTION ( 'NONE',  ( 0.000000000000000000, -1.000000000000000000, 0.000000000000000000 ) ) ;
#53103=ORIENTED_EDGE ( 'NONE', *, *, #23655, .T. ) ;
#53126=VERTEX_POINT ( 'NONE', #10602 ) ;
#53133=CIRCLE ( 'NONE', #32763, 0.4999999999979551912 ) ;
#53150=ADVANCED_FACE ( 'NONE', ( #24338 ), #49818, .F. ) ;
#53179=ORIENTED_EDGE ( 'NONE', *, *, #52189, .T. ) ;
#53203=ADVANCED_FACE ( 'NONE', ( #13011 ), #17974, .F. ) ;
#53221=AXIS2_PLACEMENT_3D ( 'NONE', #28395, #34042, #50318 ) ;
#53236=VERTEX_POINT ( 'NONE', #2071 ) ;
#53249=ORIENTED_EDGE ( 'NONE', *, *, #1322, .T. ) ;
#53254=DIRECTION ( 'NONE',  ( 0.000000000000000000, -1.000000000000000000, -1.838806884531994514E-12 ) ) ;
#53260=VERTEX_POINT ( 'NONE', #40241 ) ;
#53282=VERTEX_POINT ( 'NONE', #19714 ) ;
#53284=ADVANCED_FACE ( 'NONE', ( #14442 ), #56850, .F. ) ;
#53285=PLANE ( 'NONE',  #56505 ) ;
#53301=VERTEX_POINT ( 'NONE', #69221 ) ;
#53303=VERTEX_POINT ( 'NONE', #41648 ) ;
#53325=EDGE_CURVE ( 'NONE', #15713, #27791, #3129, .T. ) ;
#53331=ADVANCED_FACE ( 'NONE', ( #68877 ), #30343, .F. ) ;
#53344=FACE_OUTER_BOUND ( 'NONE', #33586, .T. ) ;
#53348=ORIENTED_EDGE ( 'NONE', *, *, #44517, .F. ) ;
#53358=CIRCLE ( 'NONE', #22847, 7.800000000000000711 ) ;
#53362=FACE_OUTER_BOUND ( 'NONE', #50257, .T. ) ;
#53381=CARTESIAN_POINT ( 'NONE',  ( 7.000000000000000000, -26.42999999999999972, -9.412893218813501051 ) ) ;
#53383=DIRECTION ( 'NONE',  ( 0.000000000000000000, 0.000000000000000000, -1.000000000000000000 ) ) ;
#53394=DIRECTION ( 'NONE',  ( 0.000000000000000000, -1.000000000000000000, 0.000000000000000000 ) ) ;
#53395=VERTEX_POINT ( 'NONE', #15492 ) ;
#53402=DIRECTION ( 'NONE',  ( 0.000000000000000000, 0.000000000000000000, -1.000000000000000000 ) ) ;
#53418=AXIS2_PLACEMENT_3D ( 'NONE', #38071, #12547, #16833 ) ;
#53420=CARTESIAN_POINT ( 'NONE',  ( 283.0000000000000568, -23.50007830495750127, 12.28007262201345995 ) ) ;
#53442=LINE ( 'NONE', #59083, #12449 ) ;
#53448=CARTESIAN_POINT ( 'NONE',  ( 7.000000000000000000, -30.80000000000000071, -8.900000000000000355 ) ) ;
#53449=ORIENTED_EDGE ( 'NONE', *, *, #45539, .T. ) ;
#53451=( NAMED_UNIT ( * ) PLANE_ANGLE_UNIT ( ) SI_UNIT ( $, .RADIAN. ) );
#53459=PLANE ( 'NONE',  #40767 ) ;
#53462=CARTESIAN_POINT ( 'NONE',  ( 7.000000000000000000, -30.80000000000000071, 12.20000000000000107 ) ) ;
#53463=DIRECTION ( 'NONE',  ( -1.000000000000000000, 0.000000000000000000, 0.000000000000000000 ) ) ;
#53466=CYLINDRICAL_SURFACE ( 'NONE', #25301, 0.5000000000023432367 ) ;
#53510=EDGE_LOOP ( 'NONE', ( #22276, #42175, #24002, #31477 ) ) ;
#53511=ORIENTED_EDGE ( 'NONE', *, *, #53325, .T. ) ;
#53514=LINE ( 'NONE', #22379, #69550 ) ;
#53516=VERTEX_POINT ( 'NONE', #49986 ) ;
#53519=DIRECTION ( 'NONE',  ( 0.000000000000000000, -0.7071067811828075644, 0.7071067811902875810 ) ) ;
#53553=VERTEX_POINT ( 'NONE', #17150 ) ;
#53566=DIRECTION ( 'NONE',  ( 0.000000000000000000, 0.000000000000000000, -1.000000000000000000 ) ) ;
#53570=AXIS2_PLACEMENT_3D ( 'NONE', #58352, #63651, #51986 ) ;
#53580=DIRECTION ( 'NONE',  ( 0.5773502691896201799, -0.5773502691896285066, -0.5773502691896285066 ) ) ;
#53582=ORIENTED_EDGE ( 'NONE', *, *, #22543, .T. ) ;
#53592=CARTESIAN_POINT ( 'NONE',  ( 275.0000000000000000, -26.28355339059299922, -9.766446609406699508 ) ) ;
#53600=EDGE_CURVE ( 'NONE', #69904, #53395, #29144, .T. ) ;
#53601=ORIENTED_EDGE ( 'NONE', *, *, #59586, .F. ) ;
#53607=CARTESIAN_POINT ( 'NONE',  ( 275.0000000000000000, -24.99999999999915090, 9.080000000000110205 ) ) ;
#53609=ADVANCED_FACE ( 'NONE', ( #56368 ), #29493, .F. ) ;
#53619=DIRECTION ( 'NONE',  ( 0.000000000000000000, 0.000000000000000000, -1.000000000000000000 ) ) ;
#53642=EDGE_LOOP ( 'NONE', ( #52807, #44424, #61378, #546 ) ) ;
#53643=ORIENTED_EDGE ( 'NONE', *, *, #27289, .T. ) ;
#53657=LINE ( 'NONE', #27823, #19574 ) ;
#53661=CIRCLE ( 'NONE', #49104, 0.5000000000004306555 ) ;
#53668=DIRECTION ( 'NONE',  ( 1.000000000000000000, -0.000000000000000000, -0.000000000000000000 ) ) ;
#53671=ORIENTED_EDGE ( 'NONE', *, *, #51090, .F. ) ;
#53674=AXIS2_PLACEMENT_3D ( 'NONE', #45366, #29464, #13551 ) ;
#53703=ORIENTED_EDGE ( 'NONE', *, *, #2713, .T. ) ;
#53709=EDGE_CURVE ( 'NONE', #49302, #40699, #2985, .T. ) ;
#53738=CARTESIAN_POINT ( 'NONE',  ( 283.0000000000000568, -42.50000000000000000, -15.10000000000000142 ) ) ;
#53747=CARTESIAN_POINT ( 'NONE',  ( 6.884529946162100345, -21.00000000000000000, 8.000000000000000000 ) ) ;
#53750=ORIENTED_EDGE ( 'NONE', *, *, #57743, .T. ) ;
#53781=VECTOR ( 'NONE', #22914, 1000.000000000000000 ) ;
#53791=DIRECTION ( 'NONE',  ( 0.000000000000000000, 0.000000000000000000, -1.000000000000000000 ) ) ;
#53798=CARTESIAN_POINT ( 'NONE',  ( 283.0000000000000568, -39.80000000000000426, -8.400000000000000355 ) ) ;
#53806=VECTOR ( 'NONE', #52883, 1000.000000000000000 ) ;
#53813=CARTESIAN_POINT ( 'NONE',  ( 283.0000000000000568, -24.99999999999915090, 9.080000000000110205 ) ) ;
#53833=DIRECTION ( 'NONE',  ( 0.000000000000000000, 0.000000000000000000, 1.000000000000000000 ) ) ;
#53844=CARTESIAN_POINT ( 'NONE',  ( 7.000000000000000000, -21.00000000000000000, -7.799999999999999822 ) ) ;
#53853=EDGE_CURVE ( 'NONE', #42177, #20434, #42560, .T. ) ;
#53858=ORIENTED_EDGE ( 'NONE', *, *, #29105, .T. ) ;
#53863=FACE_OUTER_BOUND ( 'NONE', #25899, .T. ) ;
#53872=ORIENTED_EDGE ( 'NONE', *, *, #9372, .T. ) ;
#53882=AXIS2_PLACEMENT_3D ( 'NONE', #14068, #51913, #58620 ) ;
#53905=EDGE_CURVE ( 'NONE', #54243, #18078, #10727, .T. ) ;
#53906=ORIENTED_EDGE ( 'NONE', *, *, #3469, .T. ) ;
#53921=DIRECTION ( 'NONE',  ( 0.000000000000000000, -0.7071067811865474617, -0.7071067811865474617 ) ) ;
#53932=DIRECTION ( 'NONE',  ( 0.000000000000000000, 0.000000000000000000, 1.000000000000000000 ) ) ;
#53934=DIRECTION ( 'NONE',  ( 0.000000000000000000, 0.000000000000000000, 1.000000000000000000 ) ) ;
#53949=CARTESIAN_POINT ( 'NONE',  ( 283.0000000000000568, -25.93000000000544958, -9.412893218815410634 ) ) ;
#53953=ORIENTED_EDGE ( 'NONE', *, *, #17685, .T. ) ;
#53969=CARTESIAN_POINT ( 'NONE',  ( 289.5000000000000000, -42.00000000000000000, 27.00000000000000000 ) ) ;
#53970=EDGE_CURVE ( 'NONE', #53516, #7467, #43938, .T. ) ;
#53976=DIRECTION ( 'NONE',  ( 0.000000000000000000, 1.000000000000000000, 0.000000000000000000 ) ) ;
#53981=EDGE_CURVE ( 'NONE', #56310, #67044, #2193, .T. ) ;
#53986=EDGE_CURVE ( 'NONE', #26187, #62567, #28034, .T. ) ;
#53994=VERTEX_POINT ( 'NONE', #7135 ) ;
#54017=EDGE_CURVE ( 'NONE', #57464, #17601, #53133, .T. ) ;
#54025=EDGE_LOOP ( 'NONE', ( #40860, #30117, #14362, #29006, #32095, #48457, #59012, #35282, #67555, #42712, #61525, #16274, #58197, #64024, #37399, #53953, #61719, #63231, #46731, #32435 ) ) ;
#54041=DIRECTION ( 'NONE',  ( 0.000000000000000000, 0.000000000000000000, 1.000000000000000000 ) ) ;
#54049=LINE ( 'NONE', #16566, #11520 ) ;
#54073=DIRECTION ( 'NONE',  ( 0.000000000000000000, 0.000000000000000000, -1.000000000000000000 ) ) ;
#54077=VECTOR ( 'NONE', #11765, 1000.000000000000000 ) ;
#54078=DIRECTION ( 'NONE',  ( -0.7071067811865474617, 0.7071067811865474617, 0.000000000000000000 ) ) ;
#54096=DIRECTION ( 'NONE',  ( 1.000000000000000000, 0.000000000000000000, 0.000000000000000000 ) ) ;
#54099=CARTESIAN_POINT ( 'NONE',  ( 10.31889768521803141, -25.34729925119248151, 17.15270074880751494 ) ) ;
#54129=DIRECTION ( 'NONE',  ( 0.000000000000000000, 0.7071067811865474617, 0.7071067811865474617 ) ) ;
#54148=VECTOR ( 'NONE', #24439, 1000.000000000000000 ) ;
#54167=CARTESIAN_POINT ( 'NONE',  ( 283.0000000000000568, -39.80000000000000426, 12.69999999999999929 ) ) ;
#54171=CARTESIAN_POINT ( 'NONE',  ( 7.000000000000000000, -25.93000000000544958, -9.412893218815410634 ) ) ;
#54172=LINE ( 'NONE', #32599, #43278 ) ;
#54176=ORIENTED_EDGE ( 'NONE', *, *, #67595, .T. ) ;
#54179=ORIENTED_EDGE ( 'NONE', *, *, #3259, .F. ) ;
#54182=DIRECTION ( 'NONE',  ( -1.000000000000000000, 0.000000000000000000, 0.000000000000000000 ) ) ;
#54183=DIRECTION ( 'NONE',  ( -1.000000000000000000, 0.000000000000000000, 0.000000000000000000 ) ) ;
#54189=ORIENTED_EDGE ( 'NONE', *, *, #59944, .F. ) ;
#54210=DIRECTION ( 'NONE',  ( -0.4999999999999170108, 0.000000000000000000, 0.8660254037844865582 ) ) ;
#54211=CARTESIAN_POINT ( 'NONE',  ( 283.0000000000000568, -42.50000000000000000, 15.10000000000000142 ) ) ;
#54226=AXIS2_PLACEMENT_3D ( 'NONE', #51757, #46097, #46787 ) ;
#54228=DIRECTION ( 'NONE',  ( 1.000000000000000000, -0.000000000000000000, -0.000000000000000000 ) ) ;
#54231=CARTESIAN_POINT ( 'NONE',  ( 1.000000000000000000, -21.00000000000000000, -5.000000000000000000 ) ) ;
#54242=EDGE_CURVE ( 'NONE', #39584, #38450, #53442, .T. ) ;
#54243=VERTEX_POINT ( 'NONE', #36836 ) ;
#54244=VECTOR ( 'NONE', #51579, 1000.000000000000114 ) ;
#54250=VERTEX_POINT ( 'NONE', #64738 ) ;
#54251=DIRECTION ( 'NONE',  ( 0.5773502691896237327, 0.5773502691896237327, 0.5773502691896298389 ) ) ;
#54261=CARTESIAN_POINT ( 'NONE',  ( 275.0000000000000000, -20.40000000000000213, 12.40000000000000213 ) ) ;
#54275=ORIENTED_EDGE ( 'NONE', *, *, #3314, .T. ) ;
#54291=CARTESIAN_POINT ( 'NONE',  ( 283.0000000000000568, -31.30000000000095284, 12.19999999999906315 ) ) ;
#54292=AXIS2_PLACEMENT_3D ( 'NONE', #48019, #42362, #37418 ) ;
#54293=CARTESIAN_POINT ( 'NONE',  ( 283.0000000000000568, -37.15000000000001279, -7.700000000000000178 ) ) ;
#54307=CARTESIAN_POINT ( 'NONE',  ( 15.00000000000000000, -0.5000000000000000000, -27.00000000000000000 ) ) ;
#54309=DIRECTION ( 'NONE',  ( 0.000000000000000000, 0.000000000000000000, -1.000000000000000000 ) ) ;
#54311=AXIS2_PLACEMENT_3D ( 'NONE', #67812, #56839, #46938 ) ;
#54317=LINE ( 'NONE', #11502, #56013 ) ;
#54338=EDGE_CURVE ( 'NONE', #32551, #47033, #27269, .T. ) ;
#54353=LINE ( 'NONE', #60684, #67486 ) ;
#54398=PLANE ( 'NONE',  #13196 ) ;
#54409=EDGE_CURVE ( 'NONE', #23962, #53126, #60115, .T. ) ;
#54416=CIRCLE ( 'NONE', #63444, 0.5000000000009320322 ) ;
#54425=CARTESIAN_POINT ( 'NONE',  ( 7.500000000000000000, -25.50000000000000355, -16.00000000000000000 ) ) ;
#54428=CARTESIAN_POINT ( 'NONE',  ( 275.0000000000000000, -25.93000000000544958, -9.412893218815410634 ) ) ;
#54434=ORIENTED_EDGE ( 'NONE', *, *, #61304, .F. ) ;
#54439=CARTESIAN_POINT ( 'NONE',  ( 7.000000000000000000, -26.79000000000000625, 0.000000000000000000 ) ) ;
#54455=EDGE_CURVE ( 'NONE', #41475, #26457, #24891, .T. ) ;
#54463=CARTESIAN_POINT ( 'NONE',  ( 283.0000000000000568, -53.81370849898476649, 17.35424868893542438 ) ) ;
#54464=CIRCLE ( 'NONE', #249, 4.000000000000000000 ) ;
#54466=DIRECTION ( 'NONE',  ( 0.000000000000000000, 0.000000000000000000, -1.000000000000000000 ) ) ;
#54471=CIRCLE ( 'NONE', #36385, 0.5000000000004236611 ) ;
#54473=CARTESIAN_POINT ( 'NONE',  ( 280.0000000000000000, -25.60000000000000142, -20.00000000000000000 ) ) ;
#54491=CARTESIAN_POINT ( 'NONE',  ( 289.5000000000000000, -42.00000000000000000, -27.00000000000000000 ) ) ;
#54496=VERTEX_POINT ( 'NONE', #62539 ) ;
#54503=VERTEX_POINT ( 'NONE', #45227 ) ;
#54515=DIRECTION ( 'NONE',  ( 0.000000000000000000, 0.000000000000000000, 1.000000000000000000 ) ) ;
#54521=DIRECTION ( 'NONE',  ( 0.000000000000000000, -0.7071067811865474617, -0.7071067811865474617 ) ) ;
#54549=EDGE_CURVE ( 'NONE', #49129, #50581, #30732, .T. ) ;
#54563=FACE_OUTER_BOUND ( 'NONE', #36874, .T. ) ;
#54567=PLANE ( 'NONE',  #18755 ) ;
#54577=CARTESIAN_POINT ( 'NONE',  ( 283.0000000000000568, -23.70411739045900390, -12.50000000000000000 ) ) ;
#54583=ORIENTED_EDGE ( 'NONE', *, *, #21532, .F. ) ;
#54596=DIRECTION ( 'NONE',  ( 0.000000000000000000, 0.000000000000000000, -1.000000000000000000 ) ) ;
#54597=ORIENTED_EDGE ( 'NONE', *, *, #47365, .F. ) ;
#54600=DIRECTION ( 'NONE',  ( 0.000000000000000000, 0.000000000000000000, -1.000000000000000000 ) ) ;
#54630=ORIENTED_EDGE ( 'NONE', *, *, #45198, .T. ) ;
#54642=DIRECTION ( 'NONE',  ( -1.000000000000000000, 0.000000000000000000, 0.000000000000000000 ) ) ;
#54653=ORIENTED_EDGE ( 'NONE', *, *, #34019, .F. ) ;
#54684=ORIENTED_EDGE ( 'NONE', *, *, #46966, .F. ) ;
#54703=VERTEX_POINT ( 'NONE', #32128 ) ;
#54704=VECTOR ( 'NONE', #29686, 1000.000000000000000 ) ;
#54713=VECTOR ( 'NONE', #37033, 1000.000000000000114 ) ;
#54738=FACE_OUTER_BOUND ( 'NONE', #15624, .T. ) ;
#54749=ORIENTED_EDGE ( 'NONE', *, *, #46531, .T. ) ;
#54750=DIRECTION ( 'NONE',  ( 0.000000000000000000, -1.000000000000000000, 0.000000000000000000 ) ) ;
#54760=AXIS2_PLACEMENT_3D ( 'NONE', #25174, #4325, #57342 ) ;
#54768=ADVANCED_FACE ( 'NONE', ( #54738 ), #34177, .F. ) ;
#54777=ORIENTED_EDGE ( 'NONE', *, *, #66110, .T. ) ;
#54781=CARTESIAN_POINT ( 'NONE',  ( 7.000000000000000000, -42.00000000000000000, 7.000000000000000000 ) ) ;
#54790=CARTESIAN_POINT ( 'NONE',  ( 275.0000000000000000, -20.40000000000000213, -17.60000000000000142 ) ) ;
#54806=EDGE_CURVE ( 'NONE', #21069, #20434, #40735, .T. ) ;
#54815=CARTESIAN_POINT ( 'NONE',  ( 10.47821035407137558, -20.81978353999702236, 17.31978353999702236 ) ) ;
#54816=ORIENTED_EDGE ( 'NONE', *, *, #55165, .F. ) ;
#54832=VERTEX_POINT ( 'NONE', #48736 ) ;
#54837=ORIENTED_EDGE ( 'NONE', *, *, #916, .T. ) ;
#54844=PLANE ( 'NONE',  #57360 ) ;
#54845=LINE ( 'NONE', #2130, #25961 ) ;
#54848=ORIENTED_EDGE ( 'NONE', *, *, #10226, .T. ) ;
#54896=ORIENTED_EDGE ( 'NONE', *, *, #2333, .F. ) ;
#54899=DIRECTION ( 'NONE',  ( 0.000000000000000000, 0.000000000000000000, -1.000000000000000000 ) ) ;
#54901=ORIENTED_EDGE ( 'NONE', *, *, #43811, .F. ) ;
#54904=EDGE_CURVE ( 'NONE', #49129, #44568, #35736, .T. ) ;
#54907=EDGE_CURVE ( 'NONE', #66121, #53994, #41160, .T. ) ;
#54911=ORIENTED_EDGE ( 'NONE', *, *, #14388, .T. ) ;
#54915=CIRCLE ( 'NONE', #2955, 8.000000000000000000 ) ;
#54918=CARTESIAN_POINT ( 'NONE',  ( 7.000000000000000000, -32.95000000000000284, 7.700000000000000178 ) ) ;
#54921=DIRECTION ( 'NONE',  ( 1.000000000000000000, 0.000000000000000000, 0.000000000000000000 ) ) ;
#54924=AXIS2_PLACEMENT_3D ( 'NONE', #18373, #34284, #1776 ) ;
#54932=AXIS2_PLACEMENT_3D ( 'NONE', #61718, #62059, #47133 ) ;
#54968=VERTEX_POINT ( 'NONE', #20300 ) ;
#54981=ORIENTED_EDGE ( 'NONE', *, *, #4113, .F. ) ;
#54995=EDGE_CURVE ( 'NONE', #16805, #15647, #44205, .T. ) ;
#54998=LINE ( 'NONE', #54293, #824 ) ;
#55003=CARTESIAN_POINT ( 'NONE',  ( 7.000000000000000000, -26.42999999999999972, 9.412893218813501051 ) ) ;
#55006=CARTESIAN_POINT ( 'NONE',  ( 10.70000000000000107, -25.60000000000000142, 17.60000000000000142 ) ) ;
#55008=ADVANCED_FACE ( 'NONE', ( #27359 ), #65197, .T. ) ;
#55011=CARTESIAN_POINT ( 'NONE',  ( 283.0000000000000568, -42.50000000000000000, 10.20000000000000107 ) ) ;
#55013=DIRECTION ( 'NONE',  ( -1.000000000000000000, 0.000000000000000000, 0.000000000000000000 ) ) ;
#55019=DIRECTION ( 'NONE',  ( 0.000000000000000000, 0.000000000000000000, 1.000000000000000000 ) ) ;
#55031=ORIENTED_EDGE ( 'NONE', *, *, #41107, .F. ) ;
#55033=FACE_OUTER_BOUND ( 'NONE', #48186, .T. ) ;
#55046=VERTEX_POINT ( 'NONE', #69440 ) ;
#55050=ORIENTED_EDGE ( 'NONE', *, *, #7064, .F. ) ;
#55053=ORIENTED_EDGE ( 'NONE', *, *, #66110, .F. ) ;
#55054=FACE_OUTER_BOUND ( 'NONE', #13504, .T. ) ;
#55059=ORIENTED_EDGE ( 'NONE', *, *, #5575, .T. ) ;
#55081=FACE_OUTER_BOUND ( 'NONE', #68906, .T. ) ;
#55095=PLANE ( 'NONE',  #34643 ) ;
#55104=PLANE ( 'NONE',  #3367 ) ;
#55121=LINE ( 'NONE', #37473, #14122 ) ;
#55137=DIRECTION ( 'NONE',  ( -1.000000000000000000, 0.000000000000000000, 0.000000000000000000 ) ) ;
#55150=EDGE_CURVE ( 'NONE', #24019, #19038, #50989, .T. ) ;
#55156=( BOUNDED_CURVE ( )  B_SPLINE_CURVE ( 3, ( #29567, #55419, #61040, #28189 ),
 .UNSPECIFIED., .F., .F. ) 
 B_SPLINE_CURVE_WITH_KNOTS ( ( 4, 4 ),
 ( 5.387520513321711668, 5.560451059366170234 ),
 .UNSPECIFIED. ) 
 CURVE ( )  GEOMETRIC_REPRESENTATION_ITEM ( )  RATIONAL_B_SPLINE_CURVE ( ( 1.000000000000000000, 0.9975094710839671475, 0.9975094710839671475, 1.000000000000000000 ) ) 
 REPRESENTATION_ITEM ( '' )  );
#55157=DIRECTION ( 'NONE',  ( 0.000000000000000000, 0.000000000000000000, -1.000000000000000000 ) ) ;
#55164=CIRCLE ( 'NONE', #50655, 0.4999999999945519691 ) ;
#55165=EDGE_CURVE ( 'NONE', #36190, #13533, #8055, .T. ) ;
#55207=ORIENTED_EDGE ( 'NONE', *, *, #7562, .T. ) ;
#55243=ORIENTED_EDGE ( 'NONE', *, *, #24137, .F. ) ;
#55256=ORIENTED_EDGE ( 'NONE', *, *, #58339, .F. ) ;
#55274=VECTOR ( 'NONE', #19259, 1000.000000000000000 ) ;
#55297=AXIS2_PLACEMENT_3D ( 'NONE', #61736, #1308, #66690 ) ;
#55303=EDGE_CURVE ( 'NONE', #47033, #8022, #56986, .T. ) ;
#55324=VECTOR ( 'NONE', #24179, 1000.000000000000000 ) ;
#55328=EDGE_CURVE ( 'NONE', #32653, #51904, #8544, .T. ) ;
#55342=LINE ( 'NONE', #18535, #32059 ) ;
#55347=DIRECTION ( 'NONE',  ( 0.000000000000000000, 0.000000000000000000, 1.000000000000000000 ) ) ;
#55354=DIRECTION ( 'NONE',  ( -1.000000000000000000, 0.000000000000000000, 0.000000000000000000 ) ) ;
#55362=CARTESIAN_POINT ( 'NONE',  ( 282.7711612342632179, -20.61060115624107780, -17.11060115624107425 ) ) ;
#55363=CARTESIAN_POINT ( 'NONE',  ( 7.000000000000000000, -31.30000000000095284, 12.19999999999906315 ) ) ;
#55403=ORIENTED_EDGE ( 'NONE', *, *, #30303, .T. ) ;
#55404=EDGE_CURVE ( 'NONE', #24235, #55546, #36849, .T. ) ;
#55405=CARTESIAN_POINT ( 'NONE',  ( 290.0000000000000000, -21.00000000000000000, 5.000000000000000000 ) ) ;
#55419=CARTESIAN_POINT ( 'NONE',  ( 10.47821035407137025, -20.81978353999701170, -17.31978353999701170 ) ) ;
#55431=CARTESIAN_POINT ( 'NONE',  ( 0.2499999999999893141, -0.2499999999999893141, -26.75000000000001421 ) ) ;
#55456=CARTESIAN_POINT ( 'NONE',  ( 283.0000000000000568, -32.94999999999885176, -8.199999999997979572 ) ) ;
#55461=ADVANCED_FACE ( 'NONE', ( #16306 ), #21279, .F. ) ;
#55468=CARTESIAN_POINT ( 'NONE',  ( 283.0000000000000568, -31.30000000000045191, -8.900000000000430234 ) ) ;
#55475=VECTOR ( 'NONE', #52295, 1000.000000000000000 ) ;
#55496=DIRECTION ( 'NONE',  ( -1.000000000000000000, 0.000000000000000000, 0.000000000000000000 ) ) ;
#55501=ORIENTED_EDGE ( 'NONE', *, *, #5575, .F. ) ;
#55503=CYLINDRICAL_SURFACE ( 'NONE', #5307, 0.5000000000009406920 ) ;
#55528=ORIENTED_EDGE ( 'NONE', *, *, #49592, .T. ) ;
#55546=VERTEX_POINT ( 'NONE', #27609 ) ;
#55547=AXIS2_PLACEMENT_3D ( 'NONE', #33921, #49850, #28624 ) ;
#55548=CARTESIAN_POINT ( 'NONE',  ( 15.00000000000000000, -42.00000000000000000, 15.10000000000000142 ) ) ;
#55552=CARTESIAN_POINT ( 'NONE',  ( 283.0000000000000568, -30.80000000000000071, 12.20000000000000107 ) ) ;
#55553=CARTESIAN_POINT ( 'NONE',  ( 7.000000000000000000, -38.64999999999999858, -12.69999999999999929 ) ) ;
#55567=( BOUNDED_CURVE ( )  B_SPLINE_CURVE ( 3, ( #9156, #52288, #27073, #21769 ),
 .UNSPECIFIED., .F., .F. ) 
 B_SPLINE_CURVE_WITH_KNOTS ( ( 4, 4 ),
 ( 3.864326901403209558, 3.989654732571277229 ),
 .UNSPECIFIED. ) 
 CURVE ( )  GEOMETRIC_REPRESENTATION_ITEM ( )  RATIONAL_B_SPLINE_CURVE ( ( 1.000000000000000000, 0.9986915061577686936, 0.9986915061577686936, 1.000000000000000000 ) ) 
 REPRESENTATION_ITEM ( '' )  );
#55568=CARTESIAN_POINT ( 'NONE',  ( 283.0000000000000568, -25.50000000000000355, -17.00000000000000000 ) ) ;
#55571=ORIENTED_EDGE ( 'NONE', *, *, #56131, .T. ) ;
#55587=DIRECTION ( 'NONE',  ( -1.000000000000000000, 0.000000000000000000, 0.000000000000000000 ) ) ;
#55594=DIRECTION ( 'NONE',  ( -1.000000000000000000, 0.000000000000000000, 0.000000000000000000 ) ) ;
#55600=PLANE ( 'NONE',  #43469 ) ;
#55601=EDGE_LOOP ( 'NONE', ( #54981, #51700, #27030, #31397 ) ) ;
#55608=ORIENTED_EDGE ( 'NONE', *, *, #47923, .F. ) ;
#55646=DIRECTION ( 'NONE',  ( 1.000000000000000000, -0.000000000000000000, -0.000000000000000000 ) ) ;
#55647=VERTEX_POINT ( 'NONE', #17335 ) ;
#55673=VECTOR ( 'NONE', #34531, 1000.000000000000000 ) ;
#55677=ADVANCED_FACE ( 'NONE', ( #68579 ), #30039, .F. ) ;
#55683=LINE ( 'NONE', #1943, #29640 ) ;
#55713=ORIENTED_EDGE ( 'NONE', *, *, #53709, .T. ) ;
#55714=ADVANCED_FACE ( 'NONE', ( #13425 ), #68219, .F. ) ;
#55735=ADVANCED_FACE ( 'NONE', ( #67165 ), #35320, .F. ) ;
#55736=DIRECTION ( 'NONE',  ( -1.000000000000000000, 0.000000000000000000, 0.000000000000000000 ) ) ;
#55738=EDGE_LOOP ( 'NONE', ( #25313, #4077, #60754, #49019, #56755, #28807 ) ) ;
#55748=VERTEX_POINT ( 'NONE', #19079 ) ;
#55755=VECTOR ( 'NONE', #25303, 1000.000000000000000 ) ;
#55757=DIRECTION ( 'NONE',  ( 0.000000000000000000, 1.000000000000000000, 0.000000000000000000 ) ) ;
#55771=LINE ( 'NONE', #33513, #51620 ) ;
#55774=LINE ( 'NONE', #6974, #22056 ) ;
#55855=FACE_OUTER_BOUND ( 'NONE', #24641, .T. ) ;
#55857=CARTESIAN_POINT ( 'NONE',  ( 275.0000000000000000, 0.000000000000000000, 0.000000000000000000 ) ) ;
#55885=CARTESIAN_POINT ( 'NONE',  ( 7.000000000000000000, -20.40000000000000213, 17.60000000000000142 ) ) ;
#55892=ORIENTED_EDGE ( 'NONE', *, *, #8290, .T. ) ;
#55893=CARTESIAN_POINT ( 'NONE',  ( 10.14575131106459160, -20.49999999999999645, -17.00000000000000000 ) ) ;
#55917=FACE_OUTER_BOUND ( 'NONE', #69893, .T. ) ;
#55931=ORIENTED_EDGE ( 'NONE', *, *, #53082, .T. ) ;
#55941=ORIENTED_EDGE ( 'NONE', *, *, #12348, .T. ) ;
#55947=CARTESIAN_POINT ( 'NONE',  ( 0.4999999999999982792, -42.00000000000000000, -27.00000000000000000 ) ) ;
#55953=VECTOR ( 'NONE', #19342, 1000.000000000000114 ) ;
#55966=CIRCLE ( 'NONE', #32316, 7.999999999999998224 ) ;
#55983=DIRECTION ( 'NONE',  ( 0.000000000000000000, 0.000000000000000000, 1.000000000000000000 ) ) ;
#55991=VERTEX_POINT ( 'NONE', #28892 ) ;
#55992=DIRECTION ( 'NONE',  ( 0.000000000000000000, 0.000000000000000000, -1.000000000000000000 ) ) ;
#56001=EDGE_LOOP ( 'NONE', ( #21544, #2588, #24315, #69944 ) ) ;
#56010=ORIENTED_EDGE ( 'NONE', *, *, #31068, .F. ) ;
#56013=VECTOR ( 'NONE', #55019, 1000.000000000000000 ) ;
#56021=VECTOR ( 'NONE', #66335, 1000.000000000000114 ) ;
#56036=DIRECTION ( 'NONE',  ( 1.000000000000000000, -0.000000000000000000, -0.000000000000000000 ) ) ;
#56050=DIRECTION ( 'NONE',  ( 0.000000000000000000, 0.000000000000000000, -1.000000000000000000 ) ) ;
#56053=VECTOR ( 'NONE', #41335, 1000.000000000000000 ) ;
#56054=AXIS2_PLACEMENT_3D ( 'NONE', #54473, #37859, #59426 ) ;
#56067=CIRCLE ( 'NONE', #53882, 0.5000000000009459100 ) ;
#56070=EDGE_LOOP ( 'NONE', ( #2103, #50519, #68997, #68289 ) ) ;
#56110=ORIENTED_EDGE ( 'NONE', *, *, #28509, .T. ) ;
#56131=EDGE_CURVE ( 'NONE', #6538, #47930, #61408, .T. ) ;
#56138=FACE_OUTER_BOUND ( 'NONE', #5452, .T. ) ;
#56140=EDGE_CURVE ( 'NONE', #749, #66609, #50809, .T. ) ;
#56145=ORIENTED_EDGE ( 'NONE', *, *, #11909, .T. ) ;
#56156=AXIS2_PLACEMENT_3D ( 'NONE', #12256, #22549, #56445 ) ;
#56161=ADVANCED_FACE ( 'NONE', ( #57519 ), #19335, .F. ) ;
#56187=ORIENTED_EDGE ( 'NONE', *, *, #54409, .F. ) ;
#56200=LINE ( 'NONE', #2793, #55475 ) ;
#56209=FACE_OUTER_BOUND ( 'NONE', #56001, .T. ) ;
#56217=AXIS2_PLACEMENT_3D ( 'NONE', #12005, #17319, #38223 ) ;
#56226=CARTESIAN_POINT ( 'NONE',  ( 7.000000000000000000, -21.00000000000000000, 12.50000000000000000 ) ) ;
#56228=CARTESIAN_POINT ( 'NONE',  ( 283.0000000000000568, -42.00000000000000000, -7.000000000000000000 ) ) ;
#56230=DIRECTION ( 'NONE',  ( 0.000000000000000000, -1.000000000000000000, 0.000000000000000000 ) ) ;
#56238=PLANE ( 'NONE',  #10684 ) ;
#56244=EDGE_CURVE ( 'NONE', #41347, #60663, #9803, .T. ) ;
#56260=CARTESIAN_POINT ( 'NONE',  ( 7.000000000000000000, -37.15000000000001279, 7.700000000000000178 ) ) ;
#56264=PLANE ( 'NONE',  #63678 ) ;
#56281=LINE ( 'NONE', #67242, #44177 ) ;
#56290=ORIENTED_EDGE ( 'NONE', *, *, #60842, .F. ) ;
#56303=AXIS2_PLACEMENT_3D ( 'NONE', #33803, #50071, #45808 ) ;
#56310=VERTEX_POINT ( 'NONE', #36657 ) ;
#56340=CARTESIAN_POINT ( 'NONE',  ( 14.50000000000000000, -42.00000000000000000, -27.00000000000000000 ) ) ;
#56368=FACE_OUTER_BOUND ( 'NONE', #26736, .T. ) ;
#56375=ADVANCED_FACE ( 'NONE', ( #49699 ), #49015, .T. ) ;
#56393=ORIENTED_EDGE ( 'NONE', *, *, #17169, .F. ) ;
#56408=AXIS2_PLACEMENT_3D ( 'NONE', #26567, #48139, #5705 ) ;
#56426=ORIENTED_EDGE ( 'NONE', *, *, #51090, .T. ) ;
#56445=DIRECTION ( 'NONE',  ( 0.000000000000000000, 0.000000000000000000, -1.000000000000000000 ) ) ;
#56473=LINE ( 'NONE', #12971, #11741 ) ;
#56476=CARTESIAN_POINT ( 'NONE',  ( 275.0000000000000000, -20.40000000000000213, -12.40000000000000213 ) ) ;
#56483=EDGE_LOOP ( 'NONE', ( #62541, #24750, #64395, #57803, #36888, #67518 ) ) ;
#56497=VECTOR ( 'NONE', #4301, 1000.000000000000000 ) ;
#56505=AXIS2_PLACEMENT_3D ( 'NONE', #42996, #47610, #69177 ) ;
#56516=PLANE ( 'NONE',  #15247 ) ;
#56517=VERTEX_POINT ( 'NONE', #24219 ) ;
#56533=EDGE_LOOP ( 'NONE', ( #46227, #60753, #52200, #44621, #46511, #25456 ) ) ;
#56546=DIRECTION ( 'NONE',  ( 0.5773502691896257311, 0.5773502691896257311, 0.5773502691896257311 ) ) ;
#56561=VERTEX_POINT ( 'NONE', #29518 ) ;
#56576=DIRECTION ( 'NONE',  ( 1.000000000000000000, -0.000000000000000000, -0.000000000000000000 ) ) ;
#56590=CARTESIAN_POINT ( 'NONE',  ( 7.500000000000000000, -20.49999999999999645, -20.00000000000000000 ) ) ;
#56597=EDGE_CURVE ( 'NONE', #10503, #69064, #19262, .T. ) ;
#56599=ORIENTED_EDGE ( 'NONE', *, *, #13432, .F. ) ;
#56602=EDGE_CURVE ( 'NONE', #42657, #2683, #39766, .T. ) ;
#56605=DIRECTION ( 'NONE',  ( 0.000000000000000000, 0.000000000000000000, -1.000000000000000000 ) ) ;
#56613=ORIENTED_EDGE ( 'NONE', *, *, #39135, .T. ) ;
#56648=ORIENTED_EDGE ( 'NONE', *, *, #31347, .T. ) ;
#56656=ORIENTED_EDGE ( 'NONE', *, *, #39762, .F. ) ;
#56659=ORIENTED_EDGE ( 'NONE', *, *, #53853, .T. ) ;
#56678=EDGE_CURVE ( 'NONE', #43920, #55991, #58146, .T. ) ;
#56697=ORIENTED_EDGE ( 'NONE', *, *, #12452, .T. ) ;
#56700=AXIS2_PLACEMENT_3D ( 'NONE', #29237, #34889, #34191 ) ;
#56703=CARTESIAN_POINT ( 'NONE',  ( 7.000000000000000000, -42.50000000000000000, -15.10000000000000142 ) ) ;
#56711=VECTOR ( 'NONE', #13981, 1000.000000000000000 ) ;
#56730=CARTESIAN_POINT ( 'NONE',  ( 15.00000000000000000, -25.60000000000000142, -17.60000000000000142 ) ) ;
#56746=LINE ( 'NONE', #61697, #43310 ) ;
#56755=ORIENTED_EDGE ( 'NONE', *, *, #47840, .F. ) ;
#56762=EDGE_CURVE ( 'NONE', #31998, #66792, #15370, .T. ) ;
#56774=ORIENTED_EDGE ( 'NONE', *, *, #47494, .F. ) ;
#56785=VERTEX_POINT ( 'NONE', #61164 ) ;
#56787=VECTOR ( 'NONE', #23446, 1000.000000000000000 ) ;
#56813=VECTOR ( 'NONE', #56907, 1000.000000000000000 ) ;
#56817=VECTOR ( 'NONE', #39302, 1000.000000000000000 ) ;
#56826=CARTESIAN_POINT ( 'NONE',  ( 7.000000000000000000, -42.50000000000000000, 15.10000000000000142 ) ) ;
#56827=ORIENTED_EDGE ( 'NONE', *, *, #64530, .F. ) ;
#56828=CARTESIAN_POINT ( 'NONE',  ( 283.0000000000000568, -25.14575131106457917, 17.35424868893542438 ) ) ;
#56832=ORIENTED_EDGE ( 'NONE', *, *, #12381, .F. ) ;
#56839=DIRECTION ( 'NONE',  ( 0.000000000000000000, 0.7071067811865470176, 0.7071067811865480168 ) ) ;
#56847=EDGE_CURVE ( 'NONE', #67044, #44995, #12369, .T. ) ;
#56850=PLANE ( 'NONE',  #47402 ) ;
#56855=ORIENTED_EDGE ( 'NONE', *, *, #15503, .T. ) ;
#56856=VERTEX_POINT ( 'NONE', #33952 ) ;
#56879=CARTESIAN_POINT ( 'NONE',  ( 283.0000000000000568, -26.79000000000000625, 0.000000000000000000 ) ) ;
#56882=DIRECTION ( 'NONE',  ( -1.000000000000000000, 0.000000000000000000, 0.000000000000000000 ) ) ;
#56899=VERTEX_POINT ( 'NONE', #50912 ) ;
#56901=CARTESIAN_POINT ( 'NONE',  ( 275.0000000000000000, -32.45000000000000995, 12.69999999999999929 ) ) ;
#56904=CARTESIAN_POINT ( 'NONE',  ( 283.0000000000000568, -26.50000000000000000, -9.080000000000000071 ) ) ;
#56905=ADVANCED_FACE ( 'NONE', ( #66482 ), #39601, .F. ) ;
#56907=DIRECTION ( 'NONE',  ( 0.000000000000000000, 1.000000000000000000, 0.000000000000000000 ) ) ;
#56909=VECTOR ( 'NONE', #51744, 1000.000000000000000 ) ;
#56921=AXIS2_PLACEMENT_3D ( 'NONE', #18055, #39621, #40332 ) ;
#56931=VECTOR ( 'NONE', #27859, 1000.000000000000000 ) ;
#56932=EDGE_CURVE ( 'NONE', #53516, #12410, #46681, .T. ) ;
#56942=ORIENTED_EDGE ( 'NONE', *, *, #53986, .F. ) ;
#56947=CARTESIAN_POINT ( 'NONE',  ( 283.0000000000000568, -42.00000000000000000, -15.00000000000000000 ) ) ;
#56949=ORIENTED_EDGE ( 'NONE', *, *, #60038, .T. ) ;
#56953=VECTOR ( 'NONE', #62467, 1000.000000000000000 ) ;
#56980=CARTESIAN_POINT ( 'NONE',  ( 275.0000000000000000, -20.40000000000000213, 17.60000000000000142 ) ) ;
#56986=LINE ( 'NONE', #18814, #3593 ) ;
#56990=CARTESIAN_POINT ( 'NONE',  ( 283.0000000000000568, -32.44999999999905071, 12.69999999999999929 ) ) ;
#56994=EDGE_CURVE ( 'NONE', #65332, #53236, #62222, .T. ) ;
#57006=EDGE_CURVE ( 'NONE', #65979, #69122, #8263, .T. ) ;
#57015=ORIENTED_EDGE ( 'NONE', *, *, #31873, .T. ) ;
#57017=ORIENTED_EDGE ( 'NONE', *, *, #7426, .F. ) ;
#57025=LINE ( 'NONE', #8585, #67220 ) ;
#57052=FACE_OUTER_BOUND ( 'NONE', #53510, .T. ) ;
#57054=LINE ( 'NONE', #24544, #20514 ) ;
#57056=CARTESIAN_POINT ( 'NONE',  ( 7.000000000000000000, -23.70411739045900390, -12.50000000000000000 ) ) ;
#57059=LINE ( 'NONE', #24892, #47940 ) ;
#57068=VECTOR ( 'NONE', #51840, 1000.000000000000000 ) ;
#57079=CARTESIAN_POINT ( 'NONE',  ( 275.0000000000000000, -23.65000000000000568, -12.40000000000000213 ) ) ;
#57085=CARTESIAN_POINT ( 'NONE',  ( 14.50000000000000000, -42.00000000000000000, -27.00000000000000000 ) ) ;
#57105=CARTESIAN_POINT ( 'NONE',  ( 7.000000000000000000, -20.50000000000000000, 13.00000000000000178 ) ) ;
#57106=CARTESIAN_POINT ( 'NONE',  ( 283.0000000000000568, -38.64999999999999858, -12.69999999999999929 ) ) ;
#57108=ORIENTED_EDGE ( 'NONE', *, *, #59586, .T. ) ;
#57126=EDGE_CURVE ( 'NONE', #56856, #54703, #59022, .T. ) ;
#57137=CARTESIAN_POINT ( 'NONE',  ( 7.000000000000000000, -27.13000000000000611, 13.50000000000000000 ) ) ;
#57160=ADVANCED_FACE ( 'NONE', ( #59370 ), #48420, .F. ) ;
#57163=EDGE_CURVE ( 'NONE', #341, #13015, #36544, .T. ) ;
#57170=VECTOR ( 'NONE', #61929, 1000.000000000000000 ) ;
#57185=AXIS2_PLACEMENT_3D ( 'NONE', #35841, #43144, #64720 ) ;
#57189=VERTEX_POINT ( 'NONE', #22582 ) ;
#57192=VERTEX_POINT ( 'NONE', #12635 ) ;
#57197=EDGE_LOOP ( 'NONE', ( #5424, #22202, #7642, #23390, #44279, #66914, #5639 ) ) ;
#57208=ORIENTED_EDGE ( 'NONE', *, *, #7653, .F. ) ;
#57227=FACE_OUTER_BOUND ( 'NONE', #56483, .T. ) ;
#57240=CARTESIAN_POINT ( 'NONE',  ( 275.0000000000000000, -25.50000000000000355, -17.00000000000000000 ) ) ;
#57251=EDGE_LOOP ( 'NONE', ( #37814, #28498, #56187, #1770, #306 ) ) ;
#57278=ORIENTED_EDGE ( 'NONE', *, *, #2478, .T. ) ;
#57295=DIRECTION ( 'NONE',  ( 0.000000000000000000, -1.000000000000000000, 0.000000000000000000 ) ) ;
#57309=VECTOR ( 'NONE', #31975, 1000.000000000000000 ) ;
#57311=EDGE_CURVE ( 'NONE', #18617, #52439, #17954, .T. ) ;
#57320=LINE ( 'NONE', #51673, #57622 ) ;
#57322=AXIS2_PLACEMENT_3D ( 'NONE', #54171, #27295, #48859 ) ;
#57325=DIRECTION ( 'NONE',  ( 0.000000000000000000, 0.000000000000000000, 1.000000000000000000 ) ) ;
#57342=DIRECTION ( 'NONE',  ( 0.000000000000000000, 0.000000000000000000, -1.000000000000000000 ) ) ;
#57359=VERTEX_POINT ( 'NONE', #56828 ) ;
#57360=AXIS2_PLACEMENT_3D ( 'NONE', #6404, #23685, #22998 ) ;
#57363=CYLINDRICAL_SURFACE ( 'NONE', #45522, 0.5000000000009302559 ) ;
#57368=VERTEX_POINT ( 'NONE', #34904 ) ;
#57384=VERTEX_POINT ( 'NONE', #50823 ) ;
#57387=DIRECTION ( 'NONE',  ( 0.000000000000000000, 0.000000000000000000, -1.000000000000000000 ) ) ;
#57410=DIRECTION ( 'NONE',  ( 0.000000000000000000, -1.000000000000000000, 0.000000000000000000 ) ) ;
#57415=ADVANCED_FACE ( 'NONE', ( #8383 ), #40217, .T. ) ;
#57416=DIRECTION ( 'NONE',  ( 1.000000000000000000, 0.000000000000000000, 0.000000000000000000 ) ) ;
#57425=CYLINDRICAL_SURFACE ( 'NONE', #41357, 5.000000000000000000 ) ;
#57426=EDGE_CURVE ( 'NONE', #46689, #36514, #19471, .T. ) ;
#57464=VERTEX_POINT ( 'NONE', #30945 ) ;
#57465=CARTESIAN_POINT ( 'NONE',  ( 283.0000000000000568, -23.29603921945599865, -12.50000000000000000 ) ) ;
#57476=VERTEX_POINT ( 'NONE', #52515 ) ;
#57484=CARTESIAN_POINT ( 'NONE',  ( 283.0000000000000568, -31.30000000000000071, 12.69999999999999929 ) ) ;
#57490=ORIENTED_EDGE ( 'NONE', *, *, #57311, .F. ) ;
#57494=EDGE_CURVE ( 'NONE', #29414, #22636, #13970, .T. ) ;
#57495=DIRECTION ( 'NONE',  ( 0.000000000000000000, 0.000000000000000000, -1.000000000000000000 ) ) ;
#57497=EDGE_LOOP ( 'NONE', ( #57208, #1089, #57645, #17190, #31856, #8983 ) ) ;
#57519=FACE_OUTER_BOUND ( 'NONE', #38111, .T. ) ;
#57520=AXIS2_PLACEMENT_3D ( 'NONE', #60464, #12013, #33598 ) ;
#57529=AXIS2_PLACEMENT_3D ( 'NONE', #61383, #34519, #45838 ) ;
#57538=LINE ( 'NONE', #30674, #23233 ) ;
#57539=ORIENTED_EDGE ( 'NONE', *, *, #7943, .T. ) ;
#57558=CARTESIAN_POINT ( 'NONE',  ( 289.9999999999998863, -41.99999999999992184, 26.49999999999997158 ) ) ;
#57588=LINE ( 'NONE', #25068, #48248 ) ;
#57622=VECTOR ( 'NONE', #19137, 1000.000000000000000 ) ;
#57645=ORIENTED_EDGE ( 'NONE', *, *, #12294, .T. ) ;
#57661=VERTEX_POINT ( 'NONE', #5124 ) ;
#57676=ORIENTED_EDGE ( 'NONE', *, *, #1322, .F. ) ;
#57687=CARTESIAN_POINT ( 'NONE',  ( 7.000000000000000000, -40.30000000000000426, 8.900000000000000355 ) ) ;
#57690=ORIENTED_EDGE ( 'NONE', *, *, #65651, .T. ) ;
#57700=EDGE_CURVE ( 'NONE', #42130, #69664, #174, .T. ) ;
#57711=DIRECTION ( 'NONE',  ( 0.000000000000000000, 0.000000000000000000, -1.000000000000000000 ) ) ;
#57712=DIRECTION ( 'NONE',  ( 1.000000000000000000, 0.000000000000000000, 0.000000000000000000 ) ) ;
#57743=EDGE_CURVE ( 'NONE', #27522, #51726, #59214, .T. ) ;
#57744=EDGE_LOOP ( 'NONE', ( #51664, #57017, #26150, #41530 ) ) ;
#57779=DIRECTION ( 'NONE',  ( 0.000000000000000000, -0.6787500000000000755, -0.7343694148723788340 ) ) ;
#57783=CARTESIAN_POINT ( 'NONE',  ( 275.0000000000000000, -32.44999999999905071, -13.20000000000091944 ) ) ;
#57803=ORIENTED_EDGE ( 'NONE', *, *, #3536, .T. ) ;
#57819=LINE ( 'NONE', #69134, #928 ) ;
#57837=EDGE_CURVE ( 'NONE', #16097, #36514, #34389, .T. ) ;
#57849=PLANE ( 'NONE',  #20024 ) ;
#57856=CIRCLE ( 'NONE', #34120, 0.5000000000009372503 ) ;
#57868=EDGE_CURVE ( 'NONE', #45355, #22560, #46069, .T. ) ;
#57876=DIRECTION ( 'NONE',  ( 0.000000000000000000, 0.000000000000000000, -1.000000000000000000 ) ) ;
#57877=LINE ( 'NONE', #40210, #33496 ) ;
#57883=AXIS2_PLACEMENT_3D ( 'NONE', #35603, #8749, #30670 ) ;
#57885=DIRECTION ( 'NONE',  ( 1.000000000000000000, -0.000000000000000000, -0.000000000000000000 ) ) ;
#57906=CARTESIAN_POINT ( 'NONE',  ( 15.00000000000000000, -25.93000000000544958, -9.412893218815410634 ) ) ;
#57910=CARTESIAN_POINT ( 'NONE',  ( 275.0000000000000000, -25.00000000000000000, 17.50000000000000000 ) ) ;
#57916=PRODUCT_CONTEXT ( 'NONE', #10589, 'mechanical' ) ;
#57935=DIRECTION ( 'NONE',  ( 0.000000000000000000, 0.7071067811865475727, 0.7071067811865475727 ) ) ;
#57943=CARTESIAN_POINT ( 'NONE',  ( 283.0000000000000568, -21.00000000000000000, 12.50000000000000000 ) ) ;
#57963=DIRECTION ( 'NONE',  ( -1.000000000000000000, 0.000000000000000000, 0.000000000000000000 ) ) ;
#57974=ORIENTED_EDGE ( 'NONE', *, *, #47494, .T. ) ;
#57977=ORIENTED_EDGE ( 'NONE', *, *, #29679, .T. ) ;
#58000=VECTOR ( 'NONE', #56882, 1000.000000000000000 ) ;
#58036=LINE ( 'NONE', #14911, #12326 ) ;
#58053=ORIENTED_EDGE ( 'NONE', *, *, #58480, .F. ) ;
#58059=DIRECTION ( 'NONE',  ( -1.000000000000000000, 0.000000000000000000, 0.000000000000000000 ) ) ;
#58067=DIRECTION ( 'NONE',  ( 0.000000000000000000, 0.000000000000000000, -1.000000000000000000 ) ) ;
#58076=CARTESIAN_POINT ( 'NONE',  ( 275.0000000000000000, -21.00000000000000000, -17.50000000000000000 ) ) ;
#58089=DIRECTION ( 'NONE',  ( 0.000000000000000000, 1.000000000000000000, 0.000000000000000000 ) ) ;
#58096=EDGE_LOOP ( 'NONE', ( #49233, #22667, #950, #63760 ) ) ;
#58107=VERTEX_POINT ( 'NONE', #27307 ) ;
#58111=ORIENTED_EDGE ( 'NONE', *, *, #69100, .F. ) ;
#58130=CARTESIAN_POINT ( 'NONE',  ( 277.0217896459287203, -25.18021646000300606, 17.31978353999699749 ) ) ;
#58140=EDGE_CURVE ( 'NONE', #3647, #2847, #44575, .T. ) ;
#58146=LINE ( 'NONE', #36221, #33106 ) ;
#58167=ORIENTED_EDGE ( 'NONE', *, *, #51999, .F. ) ;
#58171=ORIENTED_EDGE ( 'NONE', *, *, #5743, .F. ) ;
#58193=VECTOR ( 'NONE', #15831, 1000.000000000000000 ) ;
#58197=ORIENTED_EDGE ( 'NONE', *, *, #39388, .T. ) ;
#58199=VECTOR ( 'NONE', #59308, 1000.000000000000000 ) ;
#58200=EDGE_CURVE ( 'NONE', #48227, #60663, #7095, .T. ) ;
#58202=VECTOR ( 'NONE', #28005, 1000.000000000000000 ) ;
#58208=FACE_OUTER_BOUND ( 'NONE', #15753, .T. ) ;
#58219=FACE_OUTER_BOUND ( 'NONE', #27021, .T. ) ;
#58224=CARTESIAN_POINT ( 'NONE',  ( 15.00000000000000000, -0.5000000000000000000, 26.50000000000000000 ) ) ;
#58268=LINE ( 'NONE', #48004, #65074 ) ;
#58292=AXIS2_PLACEMENT_3D ( 'NONE', #17438, #1197, #54600 ) ;
#58301=EDGE_CURVE ( 'NONE', #16822, #43665, #52349, .T. ) ;
#58305=EDGE_LOOP ( 'NONE', ( #48689, #23444, #27741, #55031 ) ) ;
#58320=CARTESIAN_POINT ( 'NONE',  ( 14.50000000000000000, 1.110223024625156540E-16, -26.50000000000000000 ) ) ;
#58334=CARTESIAN_POINT ( 'NONE',  ( 0.2500000000000000000, -42.25000000000000000, -26.75000000000000000 ) ) ;
#58337=FACE_OUTER_BOUND ( 'NONE', #58987, .T. ) ;
#58339=EDGE_CURVE ( 'NONE', #40605, #62248, #42192, .T. ) ;
#58352=CARTESIAN_POINT ( 'NONE',  ( 7.500000000000000000, -25.50000000000000355, -20.00000000000000000 ) ) ;
#58365=CYLINDRICAL_SURFACE ( 'NONE', #2711, 3.999999999999993339 ) ;
#58370=LINE ( 'NONE', #41025, #8425 ) ;
#58371=CARTESIAN_POINT ( 'NONE',  ( 7.000000000000000000, -25.50000000000000355, -14.74860679774999994 ) ) ;
#58383=EDGE_CURVE ( 'NONE', #30690, #35743, #53657, .T. ) ;
#58390=ORIENTED_EDGE ( 'NONE', *, *, #20613, .F. ) ;
#58409=FACE_OUTER_BOUND ( 'NONE', #12607, .T. ) ;
#58414=CARTESIAN_POINT ( 'NONE',  ( 14.50000000000000000, -42.50000000000000000, -26.50000000000000000 ) ) ;
#58419=AXIS2_PLACEMENT_3D ( 'NONE', #14306, #13942, #50718 ) ;
#58436=CARTESIAN_POINT ( 'NONE',  ( 7.500000000000000000, -25.60000000000000142, 20.00000000000000000 ) ) ;
#58475=ADVANCED_FACE ( 'NONE', ( #55054 ), #38097, .T. ) ;
#58480=EDGE_CURVE ( 'NONE', #9620, #25742, #43737, .T. ) ;
#58487=LINE ( 'NONE', #10032, #48301 ) ;
#58500=CARTESIAN_POINT ( 'NONE',  ( 290.0000000000000000, -21.00000000000000000, 0.000000000000000000 ) ) ;
#58502=DIRECTION ( 'NONE',  ( 0.000000000000000000, -0.7071067811865474617, -0.7071067811865474617 ) ) ;
#58508=CIRCLE ( 'NONE', #42688, 0.5000000000009320322 ) ;
#58517=VECTOR ( 'NONE', #45219, 1000.000000000000000 ) ;
#58520=ORIENTED_EDGE ( 'NONE', *, *, #16331, .F. ) ;
#58529=DIRECTION ( 'NONE',  ( -1.000000000000000000, 0.000000000000000000, 0.000000000000000000 ) ) ;
#58532=DIRECTION ( 'NONE',  ( 0.000000000000000000, 1.000000000000000000, 1.922073611378672844E-12 ) ) ;
#58573=ORIENTED_EDGE ( 'NONE', *, *, #68480, .T. ) ;
#58600=ORIENTED_EDGE ( 'NONE', *, *, #4113, .T. ) ;
#58613=CARTESIAN_POINT ( 'NONE',  ( 283.0000000000000568, -37.14999999999894698, 8.200000000002349410 ) ) ;
#58619=ORIENTED_EDGE ( 'NONE', *, *, #47887, .T. ) ;
#58620=DIRECTION ( 'NONE',  ( 0.000000000000000000, -1.887379141859195671E-12, 1.000000000000000000 ) ) ;
#58628=CARTESIAN_POINT ( 'NONE',  ( 283.0000000000000568, -32.95000000000000284, -13.19999999999999929 ) ) ;
#58640=CIRCLE ( 'NONE', #69933, 1.500000000000850875 ) ;
#58673=DIRECTION ( 'NONE',  ( -1.000000000000000000, 0.000000000000000000, 0.000000000000000000 ) ) ;
#58687=VERTEX_POINT ( 'NONE', #41201 ) ;
#58718=CIRCLE ( 'NONE', #49663, 0.5000000000023507862 ) ;
#58725=ORIENTED_EDGE ( 'NONE', *, *, #52928, .T. ) ;
#58735=CARTESIAN_POINT ( 'NONE',  ( 10.62249899919920004, -53.81370849898476649, 17.50000000000000000 ) ) ;
#58741=DIRECTION ( 'NONE',  ( 0.000000000000000000, 0.000000000000000000, 1.000000000000000000 ) ) ;
#58771=EDGE_CURVE ( 'NONE', #55046, #57189, #4093, .T. ) ;
#58772=ORIENTED_EDGE ( 'NONE', *, *, #59770, .T. ) ;
#58778=EDGE_CURVE ( 'NONE', #69932, #65808, #26346, .T. ) ;
#58780=ORIENTED_EDGE ( 'NONE', *, *, #8424, .T. ) ;
#58784=ORIENTED_EDGE ( 'NONE', *, *, #65406, .F. ) ;
#58785=FACE_OUTER_BOUND ( 'NONE', #29719, .T. ) ;
#58823=CARTESIAN_POINT ( 'NONE',  ( 7.000000000000000000, -42.50000000000000000, -15.10000000000000142 ) ) ;
#58828=CARTESIAN_POINT ( 'NONE',  ( 283.0000000000000568, -25.50000000000000355, -17.00000000000000000 ) ) ;
#58829=DIRECTION ( 'NONE',  ( 0.000000000000000000, 0.7071067811865475727, 0.7071067811865475727 ) ) ;
#58830=CARTESIAN_POINT ( 'NONE',  ( 7.000000000000000000, -26.28355339059299922, 9.766446609406699508 ) ) ;
#58835=EDGE_LOOP ( 'NONE', ( #7508, #23642, #54911, #30098, #52254 ) ) ;
#58846=ADVANCED_FACE ( 'NONE', ( #11803 ), #5132, .F. ) ;
#58860=EDGE_CURVE ( 'NONE', #12243, #31223, #11124, .T. ) ;
#58870=ORIENTED_EDGE ( 'NONE', *, *, #59511, .F. ) ;
#58883=DIRECTION ( 'NONE',  ( -1.000000000000000000, 0.000000000000000000, 0.000000000000000000 ) ) ;
#58884=CARTESIAN_POINT ( 'NONE',  ( 283.0000000000000568, -42.50000000000000000, 15.10000000000000142 ) ) ;
#58888=ORIENTED_EDGE ( 'NONE', *, *, #36016, .T. ) ;
#58889=DIRECTION ( 'NONE',  ( 0.5773502691896285066, -0.5773502691896285066, -0.5773502691896201799 ) ) ;
#58891=ORIENTED_EDGE ( 'NONE', *, *, #13432, .T. ) ;
#58896=DIRECTION ( 'NONE',  ( -0.7071067811865490160, 0.7071067811865461294, 0.000000000000000000 ) ) ;
#58900=VECTOR ( 'NONE', #378, 1000.000000000000000 ) ;
#58908=DIRECTION ( 'NONE',  ( 0.000000000000000000, 0.000000000000000000, 1.000000000000000000 ) ) ;
#58916=CARTESIAN_POINT ( 'NONE',  ( 10.70000000000000107, -25.60000000000000142, -17.60000000000000142 ) ) ;
#58926=DIRECTION ( 'NONE',  ( 0.000000000000000000, 0.000000000000000000, -1.000000000000000000 ) ) ;
#58947=CARTESIAN_POINT ( 'NONE',  ( 7.000000000000000000, -21.00000000000000000, 0.000000000000000000 ) ) ;
#58952=ORIENTED_EDGE ( 'NONE', *, *, #64066, .F. ) ;
#58959=DIRECTION ( 'NONE',  ( 0.000000000000000000, 0.000000000000000000, 1.000000000000000000 ) ) ;
#58976=EDGE_CURVE ( 'NONE', #68520, #54250, #25283, .T. ) ;
#58979=DIRECTION ( 'NONE',  ( 1.000000000000000000, -0.000000000000000000, -0.000000000000000000 ) ) ;
#58987=EDGE_LOOP ( 'NONE', ( #50236, #7531, #49978, #49807 ) ) ;
#59012=ORIENTED_EDGE ( 'NONE', *, *, #45184, .T. ) ;
#59013=CARTESIAN_POINT ( 'NONE',  ( 283.0000000000000568, -29.94999999999999929, 14.50000000000000000 ) ) ;
#59019=VECTOR ( 'NONE', #56546, 1000.000000000000114 ) ;
#59022=LINE ( 'NONE', #31817, #27365 ) ;
#59029=EDGE_CURVE ( 'NONE', #44582, #8558, #35106, .T. ) ;
#59034=CARTESIAN_POINT ( 'NONE',  ( 7.000000000000000000, -20.40000000000000213, -12.40000000000000213 ) ) ;
#59038=AXIS2_PLACEMENT_3D ( 'NONE', #52203, #24644, #51511 ) ;
#59039=DIRECTION ( 'NONE',  ( 1.000000000000000000, -0.000000000000000000, -0.000000000000000000 ) ) ;
#59051=DIRECTION ( 'NONE',  ( 0.000000000000000000, 0.000000000000000000, 1.000000000000000000 ) ) ;
#59066=LINE ( 'NONE', #10622, #66222 ) ;
#59083=CARTESIAN_POINT ( 'NONE',  ( 289.5000000000000000, -42.00000000000000000, -27.00000000000000000 ) ) ;
#59085=CARTESIAN_POINT ( 'NONE',  ( 283.0000000000000568, -21.00000000000000000, -12.50000000000000000 ) ) ;
#59088=LINE ( 'NONE', #21615, #14631 ) ;
#59093=SURFACE_STYLE_FILL_AREA ( #38907 ) ;
#59095=CARTESIAN_POINT ( 'NONE',  ( 275.0000000000000000, -32.00000000000000000, -8.400000000000000355 ) ) ;
#59097=DIRECTION ( 'NONE',  ( -1.000000000000000000, 0.000000000000000000, 0.000000000000000000 ) ) ;
#59121=EDGE_CURVE ( 'NONE', #21614, #44081, #30171, .T. ) ;
#59142=ORIENTED_EDGE ( 'NONE', *, *, #38437, .T. ) ;
#59159=DIRECTION ( 'NONE',  ( 0.000000000000000000, 0.000000000000000000, 1.000000000000000000 ) ) ;
#59174=EDGE_LOOP ( 'NONE', ( #13184, #25956, #59221, #67061, #1865 ) ) ;
#59187=EDGE_CURVE ( 'NONE', #60907, #43920, #4005, .T. ) ;
#59200=CARTESIAN_POINT ( 'NONE',  ( 7.000000000000000000, -42.50000000000000000, 7.500000000000000000 ) ) ;
#59202=CARTESIAN_POINT ( 'NONE',  ( 283.0000000000000568, -38.10000000000000142, 8.400000000000000355 ) ) ;
#59211=VECTOR ( 'NONE', #58089, 1000.000000000000000 ) ;
#59214=LINE ( 'NONE', #34049, #308 ) ;
#59221=ORIENTED_EDGE ( 'NONE', *, *, #27103, .T. ) ;
#59236=PLANE ( 'NONE',  #69499 ) ;
#59241=FACE_OUTER_BOUND ( 'NONE', #69591, .T. ) ;
#59261=AXIS2_PLACEMENT_3D ( 'NONE', #34397, #18857, #55992 ) ;
#59276=CARTESIAN_POINT ( 'NONE',  ( 10.70000000000000107, -20.40000000000000213, 17.60000000000000142 ) ) ;
#59290=PLANE ( 'NONE',  #3581 ) ;
#59301=VECTOR ( 'NONE', #8191, 1000.000000000000000 ) ;
#59308=DIRECTION ( 'NONE',  ( -1.000000000000000000, 0.000000000000000000, 0.000000000000000000 ) ) ;
#59311=ORIENTED_EDGE ( 'NONE', *, *, #1405, .T. ) ;
#59324=EDGE_CURVE ( 'NONE', #44995, #24136, #60170, .T. ) ;
#59333=VERTEX_POINT ( 'NONE', #12074 ) ;
#59341=DIRECTION ( 'NONE',  ( 0.000000000000000000, 1.000000000000000000, 0.000000000000000000 ) ) ;
#59346=EDGE_LOOP ( 'NONE', ( #13449, #41355, #68091, #12914 ) ) ;
#59354=CIRCLE ( 'NONE', #29962, 0.5000000000009302559 ) ;
#59355=DIRECTION ( 'NONE',  ( 0.000000000000000000, 0.7071067811865470176, -0.7071067811865480168 ) ) ;
#59360=DIRECTION ( 'NONE',  ( -1.000000000000000000, 0.000000000000000000, 0.000000000000000000 ) ) ;
#59370=FACE_OUTER_BOUND ( 'NONE', #59174, .T. ) ;
#59377=ORIENTED_EDGE ( 'NONE', *, *, #57700, .T. ) ;
#59383=DIRECTION ( 'NONE',  ( 0.000000000000000000, -0.7071067811865475727, -0.7071067811865475727 ) ) ;
#59426=DIRECTION ( 'NONE',  ( 0.000000000000000000, 0.000000000000000000, 1.000000000000000000 ) ) ;
#59428=CARTESIAN_POINT ( 'NONE',  ( 10.14575131106465378, -20.50000000000000000, 17.00000000000000000 ) ) ;
#59435=DIRECTION ( 'NONE',  ( -1.000000000000000000, 0.000000000000000000, 0.000000000000000000 ) ) ;
#59448=ORIENTED_EDGE ( 'NONE', *, *, #10705, .T. ) ;
#59458=AXIS2_PLACEMENT_3D ( 'NONE', #44172, #61841, #60785 ) ;
#59463=CARTESIAN_POINT ( 'NONE',  ( 283.0000000000000568, -20.40000000000000213, 12.40000000000000213 ) ) ;
#59465=DIRECTION ( 'NONE',  ( 0.000000000000000000, 0.000000000000000000, -1.000000000000000000 ) ) ;
#59487=ORIENTED_EDGE ( 'NONE', *, *, #13100, .T. ) ;
#59490=CARTESIAN_POINT ( 'NONE',  ( 283.0000000000000568, -40.30000000000000426, 12.20000000000000107 ) ) ;
#59504=AXIS2_PLACEMENT_3D ( 'NONE', #33913, #2786, #55157 ) ;
#59505=CARTESIAN_POINT ( 'NONE',  ( 7.000000000000000000, -21.00000000000000000, 7.799999999999999822 ) ) ;
#59511=EDGE_CURVE ( 'NONE', #32653, #29119, #50947, .T. ) ;
#59520=VECTOR ( 'NONE', #66422, 1000.000000000000114 ) ;
#59529=CARTESIAN_POINT ( 'NONE',  ( 7.000000000000000000, -23.50007830495750127, 12.58007262201399890 ) ) ;
#59536=CARTESIAN_POINT ( 'NONE',  ( 283.0000000000000568, -28.95000000000155183, 14.49999999999845990 ) ) ;
#59541=ORIENTED_EDGE ( 'NONE', *, *, #12091, .F. ) ;
#59558=PLANE ( 'NONE',  #13661 ) ;
#59563=CARTESIAN_POINT ( 'NONE',  ( 7.000000000000000000, -21.00000000000000000, 0.000000000000000000 ) ) ;
#59569=ORIENTED_EDGE ( 'NONE', *, *, #48646, .T. ) ;
#59572=EDGE_CURVE ( 'NONE', #65336, #54250, #10698, .T. ) ;
#59586=EDGE_CURVE ( 'NONE', #69253, #53260, #52363, .T. ) ;
#59590=DIRECTION ( 'NONE',  ( -0.7071067811865460184, -0.7071067811865489050, 0.000000000000000000 ) ) ;
#59607=DIRECTION ( 'NONE',  ( 0.000000000000000000, 0.000000000000000000, 1.000000000000000000 ) ) ;
#59610=ORIENTED_EDGE ( 'NONE', *, *, #29542, .F. ) ;
#59612=VECTOR ( 'NONE', #59870, 1000.000000000000000 ) ;
#59622=VECTOR ( 'NONE', #53619, 1000.000000000000000 ) ;
#59633=CARTESIAN_POINT ( 'NONE',  ( 7.000000000000000000, -26.50000000000000000, -5.809475019311129529 ) ) ;
#59642=ORIENTED_EDGE ( 'NONE', *, *, #47846, .T. ) ;
#59653=CARTESIAN_POINT ( 'NONE',  ( 283.0000000000000568, -26.42999999999999972, -9.412893218813501051 ) ) ;
#59656=LINE ( 'NONE', #12573, #25705 ) ;
#59666=EDGE_CURVE ( 'NONE', #21706, #22191, #712, .T. ) ;
#59680=CYLINDRICAL_SURFACE ( 'NONE', #40320, 0.5000000000009320322 ) ;
#59688=VERTEX_POINT ( 'NONE', #59750 ) ;
#59717=EDGE_LOOP ( 'NONE', ( #11886, #4264, #5995, #59448 ) ) ;
#59750=CARTESIAN_POINT ( 'NONE',  ( 0.4999999999999940603, -0.5000000000000000000, 27.00000000000000000 ) ) ;
#59769=LINE ( 'NONE', #27256, #58900 ) ;
#59770=EDGE_CURVE ( 'NONE', #22560, #16097, #28595, .T. ) ;
#59774=DIRECTION ( 'NONE',  ( -1.000000000000000000, 0.000000000000000000, 0.000000000000000000 ) ) ;
#59786=ORIENTED_EDGE ( 'NONE', *, *, #67006, .T. ) ;
#59794=EDGE_LOOP ( 'NONE', ( #20120, #14475, #23122, #2362, #38649, #44685, #45387, #56942, #53643, #45578, #36673, #14945, #37672, #39005, #1986, #21644, #65885, #6294, #31124, #6851 ) ) ;
#59807=LINE ( 'NONE', #1111, #68641 ) ;
#59815=ADVANCED_FACE ( 'NONE', ( #23296 ), #44857, .T. ) ;
#59821=DIRECTION ( 'NONE',  ( 0.000000000000000000, 0.000000000000000000, 1.000000000000000000 ) ) ;
#59840=CARTESIAN_POINT ( 'NONE',  ( 283.0000000000000568, -42.50000000000000000, 14.50000000000000000 ) ) ;
#59851=ADVANCED_FACE ( 'NONE', ( #45200 ), #66770, .T. ) ;
#59853=ORIENTED_EDGE ( 'NONE', *, *, #24610, .T. ) ;
#59854=AXIS2_PLACEMENT_3D ( 'NONE', #17241, #38813, #60369 ) ;
#59867=ORIENTED_EDGE ( 'NONE', *, *, #16980, .T. ) ;
#59870=DIRECTION ( 'NONE',  ( 0.000000000000000000, -1.000000000000000000, 0.000000000000000000 ) ) ;
#59876=LINE ( 'NONE', #28381, #65259 ) ;
#59889=CARTESIAN_POINT ( 'NONE',  ( 7.000000000000000000, -42.50000000000000000, -7.500000000000000000 ) ) ;
#59897=ADVANCED_FACE ( 'NONE', ( #9483 ), #56516, .F. ) ;
#59923=ORIENTED_EDGE ( 'NONE', *, *, #57494, .T. ) ;
#59925=ORIENTED_EDGE ( 'NONE', *, *, #61708, .T. ) ;
#59929=ORIENTED_EDGE ( 'NONE', *, *, #2676, .F. ) ;
#59944=EDGE_CURVE ( 'NONE', #68361, #55748, #59354, .T. ) ;
#59969=FACE_OUTER_BOUND ( 'NONE', #51751, .T. ) ;
#59984=ORIENTED_EDGE ( 'NONE', *, *, #66924, .T. ) ;
#59985=DIRECTION ( 'NONE',  ( 0.000000000000000000, -1.000000000000000000, 0.000000000000000000 ) ) ;
#59989=ORIENTED_EDGE ( 'NONE', *, *, #10874, .T. ) ;
#59997=AXIS2_PLACEMENT_3D ( 'NONE', #58613, #5560, #27469 ) ;
#60001=DIRECTION ( 'NONE',  ( -1.000000000000000000, 0.000000000000000000, 0.000000000000000000 ) ) ;
#60004=CARTESIAN_POINT ( 'NONE',  ( 15.00000000000000000, -42.00000000000000000, 26.50000000000000000 ) ) ;
#60018=ORIENTED_EDGE ( 'NONE', *, *, #38413, .F. ) ;
#60019=ORIENTED_EDGE ( 'NONE', *, *, #37886, .F. ) ;
#60038=EDGE_CURVE ( 'NONE', #54703, #38450, #52987, .T. ) ;
#60044=DIRECTION ( 'NONE',  ( 0.000000000000000000, 0.000000000000000000, -1.000000000000000000 ) ) ;
#60059=DIRECTION ( 'NONE',  ( -1.000000000000000000, 0.000000000000000000, 0.000000000000000000 ) ) ;
#60094=DIRECTION ( 'NONE',  ( 0.000000000000000000, -1.000000000000000000, 0.000000000000000000 ) ) ;
#60103=CARTESIAN_POINT ( 'NONE',  ( 283.0000000000000568, -42.50000000000000000, 10.20000000000000107 ) ) ;
#60111=FACE_OUTER_BOUND ( 'NONE', #41086, .T. ) ;
#60115=LINE ( 'NONE', #33923, #15864 ) ;
#60122=LINE ( 'NONE', #34629, #6200 ) ;
#60135=AXIS2_PLACEMENT_3D ( 'NONE', #39413, #33077, #55347 ) ;
#60154=VECTOR ( 'NONE', #55983, 1000.000000000000000 ) ;
#60170=LINE ( 'NONE', #38278, #68231 ) ;
#60177=DIRECTION ( 'NONE',  ( 0.000000000000000000, 0.000000000000000000, 1.000000000000000000 ) ) ;
#60190=ORIENTED_EDGE ( 'NONE', *, *, #51675, .T. ) ;
#60217=PLANE ( 'NONE',  #25511 ) ;
#60219=DIRECTION ( 'NONE',  ( 1.000000000000000000, -0.000000000000000000, -0.000000000000000000 ) ) ;
#60248=DIRECTION ( 'NONE',  ( 0.000000000000000000, -1.000000000000000000, 0.000000000000000000 ) ) ;
#60261=EDGE_LOOP ( 'NONE', ( #59853, #24849, #47905, #69652 ) ) ;
#60263=VECTOR ( 'NONE', #10001, 1000.000000000000000 ) ;
#60270=ORIENTED_EDGE ( 'NONE', *, *, #23829, .T. ) ;
#60326=CARTESIAN_POINT ( 'NONE',  ( 7.000000000000000000, -23.65000000000000568, 12.40000000000000213 ) ) ;
#60332=VERTEX_POINT ( 'NONE', #47491 ) ;
#60338=FACE_OUTER_BOUND ( 'NONE', #57251, .T. ) ;
#60339=ORIENTED_EDGE ( 'NONE', *, *, #67006, .F. ) ;
#60367=ORIENTED_EDGE ( 'NONE', *, *, #54455, .F. ) ;
#60369=DIRECTION ( 'NONE',  ( 0.000000000000000000, -0.6787500000000000755, -0.7343694148723788340 ) ) ;
#60372=FACE_OUTER_BOUND ( 'NONE', #14608, .T. ) ;
#60401=VECTOR ( 'NONE', #3650, 1000.000000000000000 ) ;
#60402=FACE_OUTER_BOUND ( 'NONE', #12184, .T. ) ;
#60410=CARTESIAN_POINT ( 'NONE',  ( 283.0000000000000568, -40.30000000000000426, -8.900000000000000355 ) ) ;
#60412=DIRECTION ( 'NONE',  ( 1.000000000000000000, 0.000000000000000000, 0.000000000000000000 ) ) ;
#60415=DIRECTION ( 'NONE',  ( 0.000000000000000000, 0.000000000000000000, 1.000000000000000000 ) ) ;
#60431=DIRECTION ( 'NONE',  ( 0.5773502691896256200, 0.5773502691896259531, 0.5773502691896256200 ) ) ;
#60435=ADVANCED_FACE ( 'NONE', ( #32971, #53863 ), #37941, .F. ) ;
#60443=CIRCLE ( 'NONE', #32250, 0.5000000000009302559 ) ;
#60450=ORIENTED_EDGE ( 'NONE', *, *, #68591, .T. ) ;
#60463=ORIENTED_EDGE ( 'NONE', *, *, #53325, .F. ) ;
#60464=CARTESIAN_POINT ( 'NONE',  ( 275.0000000000000000, -27.13000000000000611, 15.49999999999930012 ) ) ;
#60465=DIRECTION ( 'NONE',  ( 1.000000000000000000, -0.000000000000000000, -0.000000000000000000 ) ) ;
#60466=ADVANCED_FACE ( 'NONE', ( #38628 ), #5060, .F. ) ;
#60468=ORIENTED_EDGE ( 'NONE', *, *, #31977, .T. ) ;
#60474=CARTESIAN_POINT ( 'NONE',  ( 10.62249899919925866, -21.00000000000000000, 17.50000000000000000 ) ) ;
#60542=LINE ( 'NONE', #17404, #8029 ) ;
#60555=DIRECTION ( 'NONE',  ( 0.000000000000000000, -1.000000000000000000, 0.000000000000000000 ) ) ;
#60558=DIRECTION ( 'NONE',  ( 0.000000000000000000, 1.000000000000000000, 0.000000000000000000 ) ) ;
#60567=DIRECTION ( 'NONE',  ( 0.000000000000000000, 0.000000000000000000, -1.000000000000000000 ) ) ;
#60583=ADVANCED_FACE ( 'NONE', ( #61202 ), #61916, .F. ) ;
#60585=DIRECTION ( 'NONE',  ( -1.000000000000000000, 0.000000000000000000, 0.000000000000000000 ) ) ;
#60606=VECTOR ( 'NONE', #43004, 1000.000000000000000 ) ;
#60618=ORIENTED_EDGE ( 'NONE', *, *, #60038, .F. ) ;
#60628=DIRECTION ( 'NONE',  ( -1.000000000000000000, 0.000000000000000000, 0.000000000000000000 ) ) ;
#60639=DIRECTION ( 'NONE',  ( 0.000000000000000000, 0.000000000000000000, -1.000000000000000000 ) ) ;
#60657=CARTESIAN_POINT ( 'NONE',  ( 275.0000000000000000, -26.28355339059299922, 9.766446609406699508 ) ) ;
#60661=CIRCLE ( 'NONE', #49377, 5.000000000000000000 ) ;
#60663=VERTEX_POINT ( 'NONE', #45639 ) ;
#60667=CARTESIAN_POINT ( 'NONE',  ( 7.000000000000000000, -21.00000000000000000, 0.000000000000000000 ) ) ;
#60682=DIRECTION ( 'NONE',  ( 0.000000000000000000, 0.000000000000000000, -1.000000000000000000 ) ) ;
#60684=CARTESIAN_POINT ( 'NONE',  ( 283.0000000000000568, -31.30000000000000071, 8.400000000000000355 ) ) ;
#60693=EDGE_LOOP ( 'NONE', ( #2600, #50343, #27480, #65681 ) ) ;
#60706=ORIENTED_EDGE ( 'NONE', *, *, #14348, .T. ) ;
#60720=CYLINDRICAL_SURFACE ( 'NONE', #20043, 4.000000000000000000 ) ;
#60739=EDGE_CURVE ( 'NONE', #38230, #67348, #20185, .T. ) ;
#60753=ORIENTED_EDGE ( 'NONE', *, *, #17652, .F. ) ;
#60754=ORIENTED_EDGE ( 'NONE', *, *, #56597, .T. ) ;
#60782=ORIENTED_EDGE ( 'NONE', *, *, #61834, .F. ) ;
#60785=DIRECTION ( 'NONE',  ( 0.000000000000000000, 0.000000000000000000, 1.000000000000000000 ) ) ;
#60803=CARTESIAN_POINT ( 'NONE',  ( 7.500000000000000000, -20.40000000000000213, -20.00000000000000000 ) ) ;
#60804=ORIENTED_EDGE ( 'NONE', *, *, #6291, .F. ) ;
#60824=ORIENTED_EDGE ( 'NONE', *, *, #22186, .F. ) ;
#60826=VERTEX_POINT ( 'NONE', #68974 ) ;
#60834=LINE ( 'NONE', #44927, #5852 ) ;
#60842=EDGE_CURVE ( 'NONE', #18752, #53516, #21928, .T. ) ;
#60863=VECTOR ( 'NONE', #47086, 1000.000000000000114 ) ;
#60871=ORIENTED_EDGE ( 'NONE', *, *, #52684, .F. ) ;
#60887=FACE_OUTER_BOUND ( 'NONE', #56533, .T. ) ;
#60904=LINE ( 'NONE', #13519, #3845 ) ;
#60907=VERTEX_POINT ( 'NONE', #48112 ) ;
#60917=EDGE_CURVE ( 'NONE', #49993, #57359, #21584, .T. ) ;
#60922=EDGE_CURVE ( 'NONE', #41506, #16868, #64716, .T. ) ;
#60925=PLANE ( 'NONE',  #44729 ) ;
#60928=CARTESIAN_POINT ( 'NONE',  ( 275.0000000000000000, -42.00000000000000000, -15.00000000000000000 ) ) ;
#60946=ORIENTED_EDGE ( 'NONE', *, *, #56244, .F. ) ;
#60964=ORIENTED_EDGE ( 'NONE', *, *, #21532, .T. ) ;
#60974=ADVANCED_FACE ( 'NONE', ( #23310 ), #44867, .F. ) ;
#60976=ORIENTED_EDGE ( 'NONE', *, *, #18116, .F. ) ;
#60979=ADVANCED_FACE ( 'NONE', ( #7035 ), #27928, .T. ) ;
#61006=VECTOR ( 'NONE', #2953, 1000.000000000000000 ) ;
#61022=PLANE ( 'NONE',  #18060 ) ;
#61028=CARTESIAN_POINT ( 'NONE',  ( 283.0000000000000568, -30.80000000000000071, 12.20000000000000107 ) ) ;
#61039=CARTESIAN_POINT ( 'NONE',  ( 275.0000000000000000, -30.45000000000094786, -14.49999999999906031 ) ) ;
#61040=CARTESIAN_POINT ( 'NONE',  ( 10.31889768521802253, -20.65270074880750428, -17.15270074880750428 ) ) ;
#61053=DIRECTION ( 'NONE',  ( -1.000000000000000000, 0.000000000000000000, 0.000000000000000000 ) ) ;
#61056=VERTEX_POINT ( 'NONE', #12675 ) ;
#61062=EDGE_CURVE ( 'NONE', #8558, #69064, #23646, .T. ) ;
#61067=VERTEX_POINT ( 'NONE', #11990 ) ;
#61069=LINE ( 'NONE', #11938, #14835 ) ;
#61107=CARTESIAN_POINT ( 'NONE',  ( 283.0000000000000568, -32.95000000000000284, -7.700000000000000178 ) ) ;
#61112=DIRECTION ( 'NONE',  ( 0.7071067811865470176, 0.000000000000000000, 0.7071067811865480168 ) ) ;
#61123=LINE ( 'NONE', #1738, #40704 ) ;
#61127=FACE_OUTER_BOUND ( 'NONE', #45605, .T. ) ;
#61139=EDGE_LOOP ( 'NONE', ( #31632, #69525, #52826, #60618 ) ) ;
#61145=DIRECTION ( 'NONE',  ( -1.000000000000000000, 0.000000000000000000, 0.000000000000000000 ) ) ;
#61164=CARTESIAN_POINT ( 'NONE',  ( 15.00000000000000000, -26.42999999999999972, 5.874955318979029784 ) ) ;
#61173=DIRECTION ( 'NONE',  ( 0.000000000000000000, 0.000000000000000000, 1.000000000000000000 ) ) ;
#61184=DIRECTION ( 'NONE',  ( 0.000000000000000000, 0.000000000000000000, -1.000000000000000000 ) ) ;
#61198=ORIENTED_EDGE ( 'NONE', *, *, #15425, .F. ) ;
#61202=FACE_OUTER_BOUND ( 'NONE', #32706, .T. ) ;
#61222=AXIS2_PLACEMENT_3D ( 'NONE', #26133, #42378, #63967 ) ;
#61228=CARTESIAN_POINT ( 'NONE',  ( 7.000000000000000000, -21.00000000000000000, 0.000000000000000000 ) ) ;
#61232=LINE ( 'NONE', #66558, #54077 ) ;
#61243=DIRECTION ( 'NONE',  ( 0.000000000000000000, -0.9239212585478300266, -0.3825826812643171038 ) ) ;
#61248=FACE_OUTER_BOUND ( 'NONE', #59717, .T. ) ;
#61253=PLANE ( 'NONE',  #15154 ) ;
#61262=FACE_OUTER_BOUND ( 'NONE', #3238, .T. ) ;
#61271=VERTEX_POINT ( 'NONE', #21495 ) ;
#61278=ORIENTED_EDGE ( 'NONE', *, *, #49483, .F. ) ;
#61279=EDGE_CURVE ( 'NONE', #50319, #10944, #38068, .T. ) ;
#61293=DIRECTION ( 'NONE',  ( 0.000000000000000000, -1.000000000000000000, 0.000000000000000000 ) ) ;
#61301=ADVANCED_FACE ( 'NONE', ( #26819 ), #4891, .T. ) ;
#61304=EDGE_CURVE ( 'NONE', #17425, #40699, #52710, .T. ) ;
#61309=EDGE_LOOP ( 'NONE', ( #55608, #33876 ) ) ;
#61310=CARTESIAN_POINT ( 'NONE',  ( 276.8000000000000682, -25.60000000000000142, -17.60000000000000142 ) ) ;
#61326=CARTESIAN_POINT ( 'NONE',  ( 283.0000000000000568, -29.94999999999999929, -14.50000000000000000 ) ) ;
#61357=ORIENTED_EDGE ( 'NONE', *, *, #26576, .T. ) ;
#61361=FACE_OUTER_BOUND ( 'NONE', #28941, .T. ) ;
#61371=ORIENTED_EDGE ( 'NONE', *, *, #55404, .F. ) ;
#61378=ORIENTED_EDGE ( 'NONE', *, *, #45580, .T. ) ;
#61383=CARTESIAN_POINT ( 'NONE',  ( 280.0000000000000000, -20.40000000000000213, 20.00000000000000000 ) ) ;
#61398=LINE ( 'NONE', #55431, #25195 ) ;
#61408=LINE ( 'NONE', #14400, #35253 ) ;
#61438=VECTOR ( 'NONE', #65621, 1000.000000000000000 ) ;
#61448=AXIS2_PLACEMENT_3D ( 'NONE', #44982, #60555, #38651 ) ;
#61466=CIRCLE ( 'NONE', #26525, 0.5000000000009372503 ) ;
#61485=DIRECTION ( 'NONE',  ( 0.000000000000000000, 0.000000000000000000, 1.000000000000000000 ) ) ;
#61490=DIRECTION ( 'NONE',  ( 0.000000000000000000, 0.000000000000000000, -1.000000000000000000 ) ) ;
#61492=ADVANCED_FACE ( 'NONE', ( #11989 ), #28957, .F. ) ;
#61500=ORIENTED_EDGE ( 'NONE', *, *, #58200, .T. ) ;
#61502=CARTESIAN_POINT ( 'NONE',  ( 282.6457513110646005, -25.50000000000000355, -17.00000000000000000 ) ) ;
#61518=DIRECTION ( 'NONE',  ( 0.000000000000000000, 1.000000000000000000, 0.000000000000000000 ) ) ;
#61519=DIRECTION ( 'NONE',  ( 0.000000000000000000, 0.000000000000000000, 1.000000000000000000 ) ) ;
#61525=ORIENTED_EDGE ( 'NONE', *, *, #41037, .F. ) ;
#61533=CARTESIAN_POINT ( 'NONE',  ( 283.0000000000000568, -53.81370849898476649, -17.35424868893542438 ) ) ;
#61549=VECTOR ( 'NONE', #69918, 1000.000000000000000 ) ;
#61574=LINE ( 'NONE', #11756, #17938 ) ;
#61594=ORIENTED_EDGE ( 'NONE', *, *, #2097, .F. ) ;
#61613=ORIENTED_EDGE ( 'NONE', *, *, #28667, .T. ) ;
#61620=CARTESIAN_POINT ( 'NONE',  ( 7.000000000000000000, -26.50000000000000000, 5.530822723609939651 ) ) ;
#61623=CARTESIAN_POINT ( 'NONE',  ( 283.0000000000000568, -28.94999999999999929, -13.50000000000000000 ) ) ;
#61635=EDGE_LOOP ( 'NONE', ( #58772, #16996, #51146, #29830, #63136, #45110 ) ) ;
#61637=VECTOR ( 'NONE', #30211, 1000.000000000000000 ) ;
#61638=ORIENTED_EDGE ( 'NONE', *, *, #2086, .T. ) ;
#61661=VERTEX_POINT ( 'NONE', #51218 ) ;
#61665=VECTOR ( 'NONE', #6343, 1000.000000000000000 ) ;
#61697=CARTESIAN_POINT ( 'NONE',  ( 0.5000000000000008882, -42.49999999999997868, -26.49999999999997868 ) ) ;
#61708=EDGE_CURVE ( 'NONE', #33051, #55647, #25650, .T. ) ;
#61711=AXIS2_PLACEMENT_3D ( 'NONE', #43858, #15954, #69706 ) ;
#61715=ORIENTED_EDGE ( 'NONE', *, *, #5549, .F. ) ;
#61718=CARTESIAN_POINT ( 'NONE',  ( 275.0000000000000000, -26.50000000000000000, -9.080000000000000071 ) ) ;
#61719=ORIENTED_EDGE ( 'NONE', *, *, #54409, .T. ) ;
#61723=ADVANCED_FACE ( 'NONE', ( #13737 ), #15065, .F. ) ;
#61736=CARTESIAN_POINT ( 'NONE',  ( 275.0000000000000000, -26.06132420600899735, 10.13999572156699891 ) ) ;
#61749=DIRECTION ( 'NONE',  ( 0.000000000000000000, 0.000000000000000000, 1.000000000000000000 ) ) ;
#61781=VERTEX_POINT ( 'NONE', #5509 ) ;
#61783=ADVANCED_FACE ( 'NONE', ( #59241 ), #28105, .F. ) ;
#61797=EDGE_CURVE ( 'NONE', #14910, #10609, #32383, .T. ) ;
#61800=EDGE_CURVE ( 'NONE', #53301, #48215, #12177, .T. ) ;
#61812=EDGE_LOOP ( 'NONE', ( #23775, #1874, #54896, #35274, #1749 ) ) ;
#61819=DIRECTION ( 'NONE',  ( 0.7071067811865475727, 0.7071067811865475727, 0.000000000000000000 ) ) ;
#61827=CARTESIAN_POINT ( 'NONE',  ( 283.0000000000000568, -26.50000000000000000, -0.5000000000000000000 ) ) ;
#61829=ORIENTED_EDGE ( 'NONE', *, *, #10169, .T. ) ;
#61832=EDGE_CURVE ( 'NONE', #9816, #1141, #17144, .T. ) ;
#61834=EDGE_CURVE ( 'NONE', #42657, #65388, #54998, .T. ) ;
#61841=DIRECTION ( 'NONE',  ( -1.000000000000000000, 0.000000000000000000, 0.000000000000000000 ) ) ;
#61842=ORIENTED_EDGE ( 'NONE', *, *, #7943, .F. ) ;
#61880=EDGE_CURVE ( 'NONE', #11348, #39584, #3323, .T. ) ;
#61891=VERTEX_POINT ( 'NONE', #29137 ) ;
#61899=ORIENTED_EDGE ( 'NONE', *, *, #36202, .F. ) ;
#61908=DIRECTION ( 'NONE',  ( 0.000000000000000000, -0.7071067811865474617, 0.7071067811865474617 ) ) ;
#61909=VECTOR ( 'NONE', #19445, 1000.000000000000000 ) ;
#61912=ORIENTED_EDGE ( 'NONE', *, *, #22895, .T. ) ;
#61915=DIRECTION ( 'NONE',  ( 1.000000000000000000, 0.000000000000000000, 0.000000000000000000 ) ) ;
#61916=PLANE ( 'NONE',  #50356 ) ;
#61923=LINE ( 'NONE', #13481, #39144 ) ;
#61929=DIRECTION ( 'NONE',  ( -1.000000000000000000, 0.000000000000000000, 0.000000000000000000 ) ) ;
#61939=EDGE_CURVE ( 'NONE', #20854, #27061, #40449, .T. ) ;
#61955=EDGE_CURVE ( 'NONE', #67535, #54832, #12857, .T. ) ;
#61959=VERTEX_POINT ( 'NONE', #67330 ) ;
#61980=ORIENTED_EDGE ( 'NONE', *, *, #52243, .F. ) ;
#61983=ORIENTED_EDGE ( 'NONE', *, *, #54806, .T. ) ;
#61987=EDGE_LOOP ( 'NONE', ( #38339, #41293, #14575, #67404, #44254, #15646, #62692, #17431, #56145, #63114, #13870, #44701, #67661, #60019 ) ) ;
#62003=ORIENTED_EDGE ( 'NONE', *, *, #39095, .F. ) ;
#62006=LINE ( 'NONE', #50357, #52156 ) ;
#62007=DIRECTION ( 'NONE',  ( 0.000000000000000000, 0.000000000000000000, -1.000000000000000000 ) ) ;
#62023=VECTOR ( 'NONE', #24690, 1000.000000000000114 ) ;
#62025=DIRECTION ( 'NONE',  ( -1.000000000000000000, 0.000000000000000000, 0.000000000000000000 ) ) ;
#62035=ADVANCED_FACE ( 'NONE', ( #46106 ), #30194, .F. ) ;
#62040=CARTESIAN_POINT ( 'NONE',  ( 283.0000000000000568, -30.80000000000000071, -8.900000000000000355 ) ) ;
#62051=EDGE_CURVE ( 'NONE', #42130, #69904, #37004, .T. ) ;
#62059=DIRECTION ( 'NONE',  ( 0.000000000000000000, -1.000000000000000000, 0.000000000000000000 ) ) ;
#62073=ORIENTED_EDGE ( 'NONE', *, *, #7734, .T. ) ;
#62079=DIRECTION ( 'NONE',  ( -1.000000000000000000, 0.000000000000000000, 0.000000000000000000 ) ) ;
#62087=CARTESIAN_POINT ( 'NONE',  ( 7.000000000000000000, -37.14999999999894698, -8.200000000002349410 ) ) ;
#62106=DIRECTION ( 'NONE',  ( 1.000000000000000000, 0.000000000000000000, 0.000000000000000000 ) ) ;
#62123=CARTESIAN_POINT ( 'NONE',  ( 7.000000000000000000, -25.60000000000000142, 15.10000000000000142 ) ) ;
#62178=EDGE_CURVE ( 'NONE', #2683, #32021, #58487, .T. ) ;
#62189=EDGE_CURVE ( 'NONE', #44075, #16486, #5437, .T. ) ;
#62198=EDGE_LOOP ( 'NONE', ( #42674, #31676, #14011, #41834 ) ) ;
#62209=CARTESIAN_POINT ( 'NONE',  ( 275.0000000000000000, -42.50000000000000000, 9.950000000000001066 ) ) ;
#62222=LINE ( 'NONE', #3191, #56813 ) ;
#62223=ORIENTED_EDGE ( 'NONE', *, *, #64402, .T. ) ;
#62248=VERTEX_POINT ( 'NONE', #43927 ) ;
#62253=LINE ( 'NONE', #29376, #51911 ) ;
#62258=CARTESIAN_POINT ( 'NONE',  ( 7.000000000000000000, -37.15000000000001279, -7.700000000000000178 ) ) ;
#62280=ADVANCED_FACE ( 'NONE', ( #6783 ), #27341, .F. ) ;
#62310=VECTOR ( 'NONE', #67383, 1000.000000000000000 ) ;
#62341=EDGE_CURVE ( 'NONE', #56310, #61891, #65844, .T. ) ;
#62346=ORIENTED_EDGE ( 'NONE', *, *, #69164, .F. ) ;
#62353=CARTESIAN_POINT ( 'NONE',  ( 275.0000000000000000, -30.80000000000000071, 12.20000000000000107 ) ) ;
#62354=LINE ( 'NONE', #45390, #41960 ) ;
#62394=CIRCLE ( 'NONE', #59038, 0.5000000000009441337 ) ;
#62423=DIRECTION ( 'NONE',  ( -0.5773502691896270633, 0.5773502691896270633, -0.5773502691896230665 ) ) ;
#62428=EDGE_CURVE ( 'NONE', #11348, #61661, #44603, .T. ) ;
#62454=DIRECTION ( 'NONE',  ( -1.000000000000000000, 0.000000000000000000, 0.000000000000000000 ) ) ;
#62458=VECTOR ( 'NONE', #46487, 1000.000000000000114 ) ;
#62467=DIRECTION ( 'NONE',  ( -0.5773502691896230665, -0.5773502691896271743, 0.5773502691896271743 ) ) ;
#62476=VERTEX_POINT ( 'NONE', #7477 ) ;
#62491=LINE ( 'NONE', #14064, #9605 ) ;
#62495=DIRECTION ( 'NONE',  ( 0.000000000000000000, 0.000000000000000000, 1.000000000000000000 ) ) ;
#62502=APPLICATION_CONTEXT ( 'automotive_design' ) ;
#62511=EDGE_CURVE ( 'NONE', #187, #41721, #61923, .T. ) ;
#62512=ORIENTED_EDGE ( 'NONE', *, *, #6019, .T. ) ;
#62539=CARTESIAN_POINT ( 'NONE',  ( 283.0000000000000568, -42.50000000000000000, 14.50000000000000000 ) ) ;
#62541=ORIENTED_EDGE ( 'NONE', *, *, #34095, .F. ) ;
#62560=CARTESIAN_POINT ( 'NONE',  ( 7.000000000000000000, -32.94999999999885176, 8.199999999997979572 ) ) ;
#62567=VERTEX_POINT ( 'NONE', #4305 ) ;
#62590=DIRECTION ( 'NONE',  ( -1.000000000000000000, 0.000000000000000000, 0.000000000000000000 ) ) ;
#62591=EDGE_LOOP ( 'NONE', ( #60190, #33237, #23413, #46558 ) ) ;
#62609=ORIENTED_EDGE ( 'NONE', *, *, #5202, .T. ) ;
#62654=EDGE_CURVE ( 'NONE', #33386, #41057, #49504, .T. ) ;
#62664=ORIENTED_EDGE ( 'NONE', *, *, #44886, .F. ) ;
#62668=VERTEX_POINT ( 'NONE', #38551 ) ;
#62674=VECTOR ( 'NONE', #31142, 1000.000000000000000 ) ;
#62678=AXIS2_PLACEMENT_3D ( 'NONE', #8230, #2937, #51735 ) ;
#62692=ORIENTED_EDGE ( 'NONE', *, *, #65262, .F. ) ;
#62700=CARTESIAN_POINT ( 'NONE',  ( 283.0000000000000568, -25.60000000000000142, -15.10000000000000142 ) ) ;
#62701=EDGE_CURVE ( 'NONE', #38703, #10783, #41364, .T. ) ;
#62721=AXIS2_PLACEMENT_3D ( 'NONE', #29673, #19076, #19423 ) ;
#62727=CARTESIAN_POINT ( 'NONE',  ( 277.1811023147819810, -25.34729925119250282, 17.15270074880750428 ) ) ;
#62737=FACE_OUTER_BOUND ( 'NONE', #48270, .T. ) ;
#62755=ADVANCED_FACE ( 'NONE', ( #61127 ), #55503, .T. ) ;
#62765=DIRECTION ( 'NONE',  ( 0.000000000000000000, 0.000000000000000000, 1.000000000000000000 ) ) ;
#62781=CARTESIAN_POINT ( 'NONE',  ( 7.000000000000000000, -21.00000000000000000, -12.50000000000000000 ) ) ;
#62791=DIRECTION ( 'NONE',  ( 1.000000000000000000, 0.000000000000000000, 0.000000000000000000 ) ) ;
#62799=EDGE_CURVE ( 'NONE', #11956, #2551, #23351, .T. ) ;
#62819=EDGE_LOOP ( 'NONE', ( #6859, #27460, #10978, #65100 ) ) ;
#62826=ADVANCED_FACE ( 'NONE', ( #1403 ), #50875, .F. ) ;
#62839=CIRCLE ( 'NONE', #35734, 4.000000000000000000 ) ;
#62845=DIRECTION ( 'NONE',  ( 0.000000000000000000, 0.000000000000000000, 1.000000000000000000 ) ) ;
#62846=AXIS2_PLACEMENT_3D ( 'NONE', #4993, #42471, #37183 ) ;
#62847=ORIENTED_EDGE ( 'NONE', *, *, #69164, .T. ) ;
#62877=DIRECTION ( 'NONE',  ( 0.000000000000000000, -0.7071067811865077157, 0.7071067811865873187 ) ) ;
#62882=CARTESIAN_POINT ( 'NONE',  ( 275.5000000000000000, -42.50000000000000000, -15.10000000000000142 ) ) ;
#62902=VERTEX_POINT ( 'NONE', #41671 ) ;
#62919=DIRECTION ( 'NONE',  ( 0.000000000000000000, 0.000000000000000000, 1.000000000000000000 ) ) ;
#62927=VECTOR ( 'NONE', #40377, 1000.000000000000000 ) ;
#62939=EDGE_CURVE ( 'NONE', #55991, #21614, #57588, .T. ) ;
#62945=DIRECTION ( 'NONE',  ( 0.000000000000000000, 0.000000000000000000, -1.000000000000000000 ) ) ;
#62959=DIRECTION ( 'NONE',  ( 0.000000000000000000, 0.000000000000000000, -1.000000000000000000 ) ) ;
#62984=DIRECTION ( 'NONE',  ( 0.000000000000000000, -1.000000000000000000, 0.000000000000000000 ) ) ;
#62991=ADVANCED_FACE ( 'NONE', ( #36368 ), #4561, .F. ) ;
#63002=VERTEX_POINT ( 'NONE', #47682 ) ;
#63013=CARTESIAN_POINT ( 'NONE',  ( 276.8000000000000682, -53.81370849898476649, 17.60000000000000142 ) ) ;
#63017=EDGE_CURVE ( 'NONE', #9842, #42028, #36729, .T. ) ;
#63054=ORIENTED_EDGE ( 'NONE', *, *, #47589, .T. ) ;
#63057=EDGE_LOOP ( 'NONE', ( #22972, #39544, #50369, #59487 ) ) ;
#63062=DIRECTION ( 'NONE',  ( 1.000000000000000000, 0.000000000000000000, 0.000000000000000000 ) ) ;
#63075=CARTESIAN_POINT ( 'NONE',  ( 7.000000000000000000, -20.40000000000000213, 17.60000000000000142 ) ) ;
#63096=CIRCLE ( 'NONE', #6615, 0.5000000000009302559 ) ;
#63113=CARTESIAN_POINT ( 'NONE',  ( 283.0000000000000568, -38.10000000000000142, -8.400000000000000355 ) ) ;
#63114=ORIENTED_EDGE ( 'NONE', *, *, #45539, .F. ) ;
#63136=ORIENTED_EDGE ( 'NONE', *, *, #33846, .F. ) ;
#63143=AXIS2_PLACEMENT_3D ( 'NONE', #20392, #31716, #63539 ) ;
#63171=CIRCLE ( 'NONE', #17985, 0.4999999999979843901 ) ;
#63184=LINE ( 'NONE', #31011, #731 ) ;
#63210=DIRECTION ( 'NONE',  ( 1.000000000000000000, 0.000000000000000000, 0.000000000000000000 ) ) ;
#63217=ORIENTED_EDGE ( 'NONE', *, *, #34684, .F. ) ;
#63218=CARTESIAN_POINT ( 'NONE',  ( 7.000000000000000000, -39.80000000000000426, -12.69999999999999929 ) ) ;
#63231=ORIENTED_EDGE ( 'NONE', *, *, #7471, .F. ) ;
#63236=ADVANCED_FACE ( 'NONE', ( #66709 ), #66008, .F. ) ;
#63237=EDGE_CURVE ( 'NONE', #10783, #26250, #65678, .T. ) ;
#63241=DIRECTION ( 'NONE',  ( 0.000000000000000000, 0.000000000000000000, 1.000000000000000000 ) ) ;
#63252=ORIENTED_EDGE ( 'NONE', *, *, #58301, .T. ) ;
#63254=ORIENTED_EDGE ( 'NONE', *, *, #1487, .F. ) ;
#63271=CARTESIAN_POINT ( 'NONE',  ( 283.0000000000000568, -25.56180396883900130, -14.25872597390799967 ) ) ;
#63274=PLANE ( 'NONE',  #7990 ) ;
#63284=DIRECTION ( 'NONE',  ( 0.000000000000000000, 0.7071067811865474617, -0.7071067811865474617 ) ) ;
#63286=EDGE_LOOP ( 'NONE', ( #24835, #65147, #25273, #710 ) ) ;
#63299=CIRCLE ( 'NONE', #69, 3.999999999999993339 ) ;
#63307=CARTESIAN_POINT ( 'NONE',  ( 14.75000000000000178, -42.25000000000000000, -26.75000000000000000 ) ) ;
#63317=DIRECTION ( 'NONE',  ( 1.000000000000000000, 0.000000000000000000, 0.000000000000000000 ) ) ;
#63335=CARTESIAN_POINT ( 'NONE',  ( 7.500000000000000000, -20.49999999999999645, 20.00000000000000000 ) ) ;
#63351=VERTEX_POINT ( 'NONE', #67759 ) ;
#63387=PLANE ( 'NONE',  #34883 ) ;
#63407=ORIENTED_EDGE ( 'NONE', *, *, #29875, .T. ) ;
#63429=ADVANCED_FACE ( 'NONE', ( #68469 ), #30291, .F. ) ;
#63444=AXIS2_PLACEMENT_3D ( 'NONE', #10502, #36324, #47292 ) ;
#63458=ORIENTED_EDGE ( 'NONE', *, *, #45744, .T. ) ;
#63462=ADVANCED_FACE ( 'NONE', ( #58208 ), #57849, .F. ) ;
#63465=EDGE_LOOP ( 'NONE', ( #56774, #1117, #30614, #38428 ) ) ;
#63483=VECTOR ( 'NONE', #8091, 1000.000000000000000 ) ;
#63508=DIRECTION ( 'NONE',  ( 0.000000000000000000, 0.000000000000000000, 1.000000000000000000 ) ) ;
#63527=CARTESIAN_POINT ( 'NONE',  ( 7.000000000000000000, -30.45000000000000639, 15.00000000000000000 ) ) ;
#63539=DIRECTION ( 'NONE',  ( 0.000000000000000000, 0.000000000000000000, -1.000000000000000000 ) ) ;
#63545=LINE ( 'NONE', #25721, #68180 ) ;
#63549=LINE ( 'NONE', #31013, #56953 ) ;
#63562=DIRECTION ( 'NONE',  ( -1.000000000000000000, 0.000000000000000000, 0.000000000000000000 ) ) ;
#63566=ORIENTED_EDGE ( 'NONE', *, *, #61939, .F. ) ;
#63567=VECTOR ( 'NONE', #30733, 1000.000000000000000 ) ;
#63574=PLANE ( 'NONE',  #5064 ) ;
#63580=ORIENTED_EDGE ( 'NONE', *, *, #33711, .T. ) ;
#63582=AXIS2_PLACEMENT_3D ( 'NONE', #12128, #1518, #6820 ) ;
#63584=EDGE_CURVE ( 'NONE', #47821, #25376, #29407, .T. ) ;
#63588=VECTOR ( 'NONE', #62877, 1000.000000000000114 ) ;
#63602=ORIENTED_EDGE ( 'NONE', *, *, #33695, .F. ) ;
#63612=AXIS2_PLACEMENT_3D ( 'NONE', #50580, #56230, #7774 ) ;
#63615=LINE ( 'NONE', #34964, #63483 ) ;
#63623=DIRECTION ( 'NONE',  ( 1.000000000000000000, -0.000000000000000000, -0.000000000000000000 ) ) ;
#63632=CARTESIAN_POINT ( 'NONE',  ( 275.0000000000000000, -25.93000000000544958, 9.412893218815410634 ) ) ;
#63634=ORIENTED_EDGE ( 'NONE', *, *, #60842, .T. ) ;
#63651=DIRECTION ( 'NONE',  ( 0.000000000000000000, 1.000000000000000000, 0.000000000000000000 ) ) ;
#63667=AXIS2_PLACEMENT_3D ( 'NONE', #323, #61819, #54078 ) ;
#63674=CARTESIAN_POINT ( 'NONE',  ( 280.0000000000000000, -25.60000000000000142, 20.00000000000000000 ) ) ;
#63678=AXIS2_PLACEMENT_3D ( 'NONE', #2515, #40348, #61915 ) ;
#63711=VECTOR ( 'NONE', #1544, 1000.000000000000000 ) ;
#63714=DIRECTION ( 'NONE',  ( 0.000000000000000000, 0.000000000000000000, 1.000000000000000000 ) ) ;
#63739=EDGE_LOOP ( 'NONE', ( #60946, #23965, #16242, #31254, #69057, #6076 ) ) ;
#63750=VECTOR ( 'NONE', #13780, 1000.000000000000000 ) ;
#63756=EDGE_CURVE ( 'NONE', #42484, #35695, #21272, .T. ) ;
#63760=ORIENTED_EDGE ( 'NONE', *, *, #34401, .T. ) ;
#63766=CIRCLE ( 'NONE', #61448, 4.000000000000000000 ) ;
#63770=LINE ( 'NONE', #59505, #5722 ) ;
#63774=ORIENTED_EDGE ( 'NONE', *, *, #40814, .F. ) ;
#63799=CYLINDRICAL_SURFACE ( 'NONE', #22354, 0.5000000000009284795 ) ;
#63807=DIRECTION ( 'NONE',  ( -1.000000000000000000, 0.000000000000000000, 0.000000000000000000 ) ) ;
#63814=CARTESIAN_POINT ( 'NONE',  ( 283.0000000000000568, -30.80000000000000071, 12.20000000000000107 ) ) ;
#63822=CARTESIAN_POINT ( 'NONE',  ( 283.0000000000000568, -25.50000000000000355, 14.74860679774999994 ) ) ;
#63823=CIRCLE ( 'NONE', #3960, 4.000000000000000000 ) ;
#63831=ORIENTED_EDGE ( 'NONE', *, *, #62701, .T. ) ;
#63832=ORIENTED_EDGE ( 'NONE', *, *, #5202, .F. ) ;
#63834=CARTESIAN_POINT ( 'NONE',  ( 275.4999999999998863, -0.5000000000000781597, 27.00000000000004263 ) ) ;
#63837=DIRECTION ( 'NONE',  ( 0.000000000000000000, 0.000000000000000000, -1.000000000000000000 ) ) ;
#63845=ORIENTED_EDGE ( 'NONE', *, *, #35031, .F. ) ;
#63860=AXIS2_PLACEMENT_3D ( 'NONE', #60928, #66589, #49636 ) ;
#63874=EDGE_CURVE ( 'NONE', #45978, #13397, #17959, .T. ) ;
#63882=DIRECTION ( 'NONE',  ( 0.000000000000000000, 0.000000000000000000, 1.000000000000000000 ) ) ;
#63888=DIRECTION ( 'NONE',  ( 0.000000000000000000, 0.000000000000000000, -1.000000000000000000 ) ) ;
#63967=DIRECTION ( 'NONE',  ( -1.000000000000000000, 0.000000000000000000, 0.000000000000000000 ) ) ;
#63972=EDGE_CURVE ( 'NONE', #29119, #68211, #745, .T. ) ;
#63979=ORIENTED_EDGE ( 'NONE', *, *, #47846, .F. ) ;
#64018=AXIS2_PLACEMENT_3D ( 'NONE', #19606, #13257, #40829 ) ;
#64021=LINE ( 'NONE', #15582, #16623 ) ;
#64024=ORIENTED_EDGE ( 'NONE', *, *, #31834, .T. ) ;
#64040=EDGE_CURVE ( 'NONE', #37208, #30152, #40525, .T. ) ;
#64046=DIRECTION ( 'NONE',  ( -1.000000000000000000, 0.000000000000000000, 0.000000000000000000 ) ) ;
#64050=CARTESIAN_POINT ( 'NONE',  ( 7.000000000000000000, -26.28355339059299922, 9.766446609406699508 ) ) ;
#64066=EDGE_CURVE ( 'NONE', #8058, #29091, #44893, .T. ) ;
#64078=CARTESIAN_POINT ( 'NONE',  ( 7.000000000000000000, -32.95000000000000284, -13.19999999999999929 ) ) ;
#64093=CARTESIAN_POINT ( 'NONE',  ( 14.75000000000000178, -42.25000000000000000, 26.75000000000000000 ) ) ;
#64095=FACE_OUTER_BOUND ( 'NONE', #7691, .T. ) ;
#64135=DIRECTION ( 'NONE',  ( 0.000000000000000000, 0.000000000000000000, -1.000000000000000000 ) ) ;
#64136=VERTEX_POINT ( 'NONE', #22979 ) ;
#64141=DIRECTION ( 'NONE',  ( 1.000000000000000000, 0.000000000000000000, 0.000000000000000000 ) ) ;
#64150=CARTESIAN_POINT ( 'NONE',  ( 7.000000000000000000, -53.81370849898476649, -16.03137303340311348 ) ) ;
#64152=EDGE_CURVE ( 'NONE', #48227, #41721, #34970, .T. ) ;
#64164=LINE ( 'NONE', #52490, #57309 ) ;
#64165=CIRCLE ( 'NONE', #49461, 0.4999999999945534124 ) ;
#64170=AXIS2_PLACEMENT_3D ( 'NONE', #50525, #11635, #66436 ) ;
#64179=CARTESIAN_POINT ( 'NONE',  ( 275.0000000000000000, -25.00000000000000000, 17.50000000000000000 ) ) ;
#64197=CARTESIAN_POINT ( 'NONE',  ( 289.7500000000001137, -0.2499999999999414080, 26.75000000000004263 ) ) ;
#64216=CARTESIAN_POINT ( 'NONE',  ( 277.1811023147819810, -25.34729925119250282, -17.15270074880750784 ) ) ;
#64225=DIRECTION ( 'NONE',  ( 0.000000000000000000, 1.000000000000000000, 0.000000000000000000 ) ) ;
#64229=LINE ( 'NONE', #26738, #4832 ) ;
#64239=LINE ( 'NONE', #32405, #8555 ) ;
#64243=DIRECTION ( 'NONE',  ( 1.000000000000000000, -0.000000000000000000, -0.000000000000000000 ) ) ;
#64253=SHAPE_REPRESENTATION ( 'LINEAR ACTUATOR', ( #45918 ), #825 ) ;
#64255=CARTESIAN_POINT ( 'NONE',  ( 283.0000000000000568, -26.42999999999999972, -9.412893218813501051 ) ) ;
#64270=AXIS2_PLACEMENT_3D ( 'NONE', #33823, #32472, #54041 ) ;
#64271=CARTESIAN_POINT ( 'NONE',  ( 277.3542486889354564, -20.49999999999999645, -17.00000000000000000 ) ) ;
#64279=EDGE_CURVE ( 'NONE', #63002, #69628, #25083, .T. ) ;
#64289=ORIENTED_EDGE ( 'NONE', *, *, #61832, .F. ) ;
#64294=AXIS2_PLACEMENT_3D ( 'NONE', #42610, #55646, #65898 ) ;
#64295=DIRECTION ( 'NONE',  ( 0.5773502691896230665, -0.5773502691896271743, -0.5773502691896271743 ) ) ;
#64312=DIRECTION ( 'NONE',  ( -1.000000000000000000, 0.000000000000000000, 0.000000000000000000 ) ) ;
#64329=EDGE_LOOP ( 'NONE', ( #58888, #18124, #58870, #10459 ) ) ;
#64344=CARTESIAN_POINT ( 'NONE',  ( 15.00000000000000000, -23.65000000000000568, -12.40000000000000213 ) ) ;
#64370=DIRECTION ( 'NONE',  ( -0.5773502691896230665, 0.5773502691896271743, -0.5773502691896271743 ) ) ;
#64389=CIRCLE ( 'NONE', #20311, 1.499999999997024602 ) ;
#64395=ORIENTED_EDGE ( 'NONE', *, *, #64040, .T. ) ;
#64402=EDGE_CURVE ( 'NONE', #42019, #28379, #32129, .T. ) ;
#64410=ORIENTED_EDGE ( 'NONE', *, *, #26442, .F. ) ;
#64416=CARTESIAN_POINT ( 'NONE',  ( 283.0000000000000568, -28.94999999999999929, -13.50000000000000000 ) ) ;
#64418=ORIENTED_EDGE ( 'NONE', *, *, #52783, .F. ) ;
#64428=CARTESIAN_POINT ( 'NONE',  ( 283.0000000000000568, -41.99999999999906208, -14.49999999999903899 ) ) ;
#64433=FACE_OUTER_BOUND ( 'NONE', #6810, .T. ) ;
#64436=EDGE_CURVE ( 'NONE', #61056, #53553, #22918, .T. ) ;
#64439=VECTOR ( 'NONE', #12670, 1000.000000000000000 ) ;
#64445=EDGE_LOOP ( 'NONE', ( #27775, #59642, #24874, #9465, #34131, #46507 ) ) ;
#64471=DIRECTION ( 'NONE',  ( 0.000000000000000000, 0.000000000000000000, 1.000000000000000000 ) ) ;
#64476=DIRECTION ( 'NONE',  ( -1.000000000000000000, 0.000000000000000000, 0.000000000000000000 ) ) ;
#64530=EDGE_CURVE ( 'NONE', #61661, #27061, #28882, .T. ) ;
#64536=EDGE_CURVE ( 'NONE', #13015, #2551, #1665, .T. ) ;
#64548=ORIENTED_EDGE ( 'NONE', *, *, #18680, .F. ) ;
#64549=CARTESIAN_POINT ( 'NONE',  ( 289.5000000000000000, -0.5000000000000000000, 27.00000000000000000 ) ) ;
#64569=EDGE_CURVE ( 'NONE', #41347, #57661, #61398, .T. ) ;
#64571=PLANE ( 'NONE',  #52835 ) ;
#64572=EDGE_CURVE ( 'NONE', #44582, #47818, #33842, .T. ) ;
#64587=DIRECTION ( 'NONE',  ( 0.000000000000000000, 0.000000000000000000, -1.000000000000000000 ) ) ;
#64620=ORIENTED_EDGE ( 'NONE', *, *, #23655, .F. ) ;
#64657=VECTOR ( 'NONE', #15453, 1000.000000000000114 ) ;
#64665=DIRECTION ( 'NONE',  ( 0.000000000000000000, 0.000000000000000000, -1.000000000000000000 ) ) ;
#64673=ORIENTED_EDGE ( 'NONE', *, *, #20555, .T. ) ;
#64682=ORIENTED_EDGE ( 'NONE', *, *, #37480, .T. ) ;
#64685=CARTESIAN_POINT ( 'NONE',  ( 7.000000000000000000, -28.95000000000155183, -14.49999999999845990 ) ) ;
#64696=CARTESIAN_POINT ( 'NONE',  ( 283.0000000000000568, -37.61196062927500350, 8.008708659369300875 ) ) ;
#64716=LINE ( 'NONE', #43838, #37966 ) ;
#64720=DIRECTION ( 'NONE',  ( -1.000000000000000000, 0.000000000000000000, 0.000000000000000000 ) ) ;
#64738=CARTESIAN_POINT ( 'NONE',  ( 283.0000000000000568, -29.94999999999999929, -14.50000000000000000 ) ) ;
#64741=ORIENTED_EDGE ( 'NONE', *, *, #31630, .F. ) ;
#64763=ORIENTED_EDGE ( 'NONE', *, *, #28435, .T. ) ;
#64767=DIRECTION ( 'NONE',  ( -1.000000000000000000, 0.000000000000000000, 0.000000000000000000 ) ) ;
#64804=ORIENTED_EDGE ( 'NONE', *, *, #53905, .T. ) ;
#64841=CIRCLE ( 'NONE', #38871, 0.5000000000009302559 ) ;
#64877=ORIENTED_EDGE ( 'NONE', *, *, #29222, .T. ) ;
#64910=DIRECTION ( 'NONE',  ( -1.000000000000000000, 0.000000000000000000, 0.000000000000000000 ) ) ;
#64914=ADVANCED_FACE ( 'NONE', ( #39416 ), #45416, .T. ) ;
#64916=DIRECTION ( 'NONE',  ( 0.5773502691896257311, -0.5773502691896298389, -0.5773502691896216232 ) ) ;
#64925=FACE_OUTER_BOUND ( 'NONE', #64445, .T. ) ;
#64959=DIRECTION ( 'NONE',  ( -1.000000000000000000, 0.000000000000000000, 0.000000000000000000 ) ) ;
#65015=ADVANCED_FACE ( 'NONE', ( #43231 ), #27328, .F. ) ;
#65024=CARTESIAN_POINT ( 'NONE',  ( 275.0000000000000000, -32.94999999999885176, -8.199999999997979572 ) ) ;
#65041=DIRECTION ( 'NONE',  ( 0.000000000000000000, 0.7071067811865474617, -0.7071067811865474617 ) ) ;
#65074=VECTOR ( 'NONE', #25387, 1000.000000000000000 ) ;
#65090=CARTESIAN_POINT ( 'NONE',  ( 290.0000000000000000, -42.00000000000000000, -27.00000000000000000 ) ) ;
#65100=ORIENTED_EDGE ( 'NONE', *, *, #61834, .T. ) ;
#65116=EDGE_CURVE ( 'NONE', #54496, #54832, #16721, .T. ) ;
#65135=ORIENTED_EDGE ( 'NONE', *, *, #413, .F. ) ;
#65137=ORIENTED_EDGE ( 'NONE', *, *, #42767, .F. ) ;
#65140=VECTOR ( 'NONE', #23758, 1000.000000000000000 ) ;
#65147=ORIENTED_EDGE ( 'NONE', *, *, #15835, .F. ) ;
#65152=DIRECTION ( 'NONE',  ( -1.000000000000000000, 0.000000000000000000, 0.000000000000000000 ) ) ;
#65156=ORIENTED_EDGE ( 'NONE', *, *, #38066, .T. ) ;
#65157=VECTOR ( 'NONE', #67531, 1000.000000000000000 ) ;
#65178=ORIENTED_EDGE ( 'NONE', *, *, #61800, .T. ) ;
#65183=VECTOR ( 'NONE', #69300, 1000.000000000000000 ) ;
#65188=AXIS2_PLACEMENT_3D ( 'NONE', #35210, #18255, #61749 ) ;
#65189=ORIENTED_EDGE ( 'NONE', *, *, #56762, .F. ) ;
#65196=LINE ( 'NONE', #43948, #22370 ) ;
#65197=CYLINDRICAL_SURFACE ( 'NONE', #37421, 0.4999999999945534124 ) ;
#65200=DIRECTION ( 'NONE',  ( -1.000000000000000000, 0.000000000000000000, 0.000000000000000000 ) ) ;
#65207=EDGE_LOOP ( 'NONE', ( #22542, #54749, #3264, #11248 ) ) ;
#65211=CARTESIAN_POINT ( 'NONE',  ( 0.2500000000000008882, -0.2499999999999991396, -26.75000000000000000 ) ) ;
#65248=EDGE_CURVE ( 'NONE', #68268, #27121, #44956, .T. ) ;
#65259=VECTOR ( 'NONE', #65200, 1000.000000000000000 ) ;
#65262=EDGE_CURVE ( 'NONE', #22100, #22191, #36553, .T. ) ;
#65263=ADVANCED_FACE ( 'NONE', ( #55917 ), #56264, .F. ) ;
#65264=EDGE_CURVE ( 'NONE', #16188, #23962, #13473, .T. ) ;
#65277=DIRECTION ( 'NONE',  ( 0.000000000000000000, 0.7071067811865480168, -0.7071067811865470176 ) ) ;
#65288=DIRECTION ( 'NONE',  ( -1.000000000000000000, 0.000000000000000000, 0.000000000000000000 ) ) ;
#65298=DIRECTION ( 'NONE',  ( 0.000000000000000000, 0.7071067811865475727, 0.7071067811865475727 ) ) ;
#65332=VERTEX_POINT ( 'NONE', #53080 ) ;
#65336=VERTEX_POINT ( 'NONE', #41044 ) ;
#65339=DIRECTION ( 'NONE',  ( 1.000000000000000000, 0.000000000000000000, 0.000000000000000000 ) ) ;
#65361=FACE_OUTER_BOUND ( 'NONE', #29785, .T. ) ;
#65376=DIRECTION ( 'NONE',  ( 1.000000000000000000, 0.000000000000000000, 0.000000000000000000 ) ) ;
#65385=FACE_OUTER_BOUND ( 'NONE', #48892, .T. ) ;
#65386=CARTESIAN_POINT ( 'NONE',  ( 275.0000000000000000, -20.50000000000000000, 17.00000000000000000 ) ) ;
#65388=VERTEX_POINT ( 'NONE', #62258 ) ;
#65394=DIRECTION ( 'NONE',  ( 0.000000000000000000, -1.000000000000000000, 0.000000000000000000 ) ) ;
#65397=FACE_OUTER_BOUND ( 'NONE', #26993, .T. ) ;
#65402=CARTESIAN_POINT ( 'NONE',  ( 7.000000000000000000, -40.30000000000000426, -12.20000000000000107 ) ) ;
#65406=EDGE_CURVE ( 'NONE', #10776, #31223, #8870, .T. ) ;
#65425=LINE ( 'NONE', #60103, #22699 ) ;
#65427=VERTEX_POINT ( 'NONE', #12805 ) ;
#65434=CYLINDRICAL_SURFACE ( 'NONE', #61711, 0.4999999999945534124 ) ;
#65453=CARTESIAN_POINT ( 'NONE',  ( 0.5000000000000000000, -42.00000000000000000, 27.00000000000000000 ) ) ;
#65456=VECTOR ( 'NONE', #3452, 1000.000000000000000 ) ;
#65460=LINE ( 'NONE', #21971, #46325 ) ;
#65465=LINE ( 'NONE', #48163, #26375 ) ;
#65473=ORIENTED_EDGE ( 'NONE', *, *, #59770, .F. ) ;
#65480=DIRECTION ( 'NONE',  ( 0.000000000000000000, 0.000000000000000000, -1.000000000000000000 ) ) ;
#65481=FACE_OUTER_BOUND ( 'NONE', #439, .T. ) ;
#65483=DIRECTION ( 'NONE',  ( 0.000000000000000000, 1.000000000000000000, 0.000000000000000000 ) ) ;
#65488=EDGE_CURVE ( 'NONE', #39543, #53282, #13866, .T. ) ;
#65495=VERTEX_POINT ( 'NONE', #18462 ) ;
#65503=EDGE_CURVE ( 'NONE', #38982, #58107, #60904, .T. ) ;
#65514=CIRCLE ( 'NONE', #59854, 8.000000000000000000 ) ;
#65527=LINE ( 'NONE', #6804, #59612 ) ;
#65538=DIRECTION ( 'NONE',  ( 1.000000000000000000, -0.000000000000000000, -0.000000000000000000 ) ) ;
#65545=LINE ( 'NONE', #43280, #25540 ) ;
#65555=CARTESIAN_POINT ( 'NONE',  ( 290.0000000000000000, -42.50000000000000000, 26.50000000000000000 ) ) ;
#65556=CARTESIAN_POINT ( 'NONE',  ( 7.000000000000000000, -26.28355339059299922, 9.766446609406699508 ) ) ;
#65576=CARTESIAN_POINT ( 'NONE',  ( 283.0000000000000568, -25.60000000000000142, -17.35424868893542438 ) ) ;
#65578=ADVANCED_FACE ( 'NONE', ( #67969 ), #53466, .T. ) ;
#65584=FACE_OUTER_BOUND ( 'NONE', #67398, .T. ) ;
#65585=ORIENTED_EDGE ( 'NONE', *, *, #52429, .F. ) ;
#65591=CYLINDRICAL_SURFACE ( 'NONE', #37391, 0.5000000000004202194 ) ;
#65609=CARTESIAN_POINT ( 'NONE',  ( 283.0000000000000568, -20.40000000000000213, -17.60000000000000142 ) ) ;
#65614=LINE ( 'NONE', #21789, #42856 ) ;
#65616=ADVANCED_FACE ( 'NONE', ( #14223 ), #35785, .F. ) ;
#65621=DIRECTION ( 'NONE',  ( 0.000000000000000000, -1.000000000000000000, 0.000000000000000000 ) ) ;
#65651=EDGE_CURVE ( 'NONE', #68084, #24330, #33864, .T. ) ;
#65668=CARTESIAN_POINT ( 'NONE',  ( 283.0000000000000568, -25.93000000000544958, -9.412893218815410634 ) ) ;
#65678=LINE ( 'NONE', #33831, #39191 ) ;
#65681=ORIENTED_EDGE ( 'NONE', *, *, #2236, .T. ) ;
#65682=CARTESIAN_POINT ( 'NONE',  ( 283.0000000000000568, -39.80000000000000426, 8.400000000000000355 ) ) ;
#65685=CARTESIAN_POINT ( 'NONE',  ( 7.500000000000000000, -25.60000000000000142, -20.00000000000000000 ) ) ;
#65706=CARTESIAN_POINT ( 'NONE',  ( 283.0000000000000568, -25.60000000000000142, -15.10000000000000142 ) ) ;
#65733=LINE ( 'NONE', #38850, #68242 ) ;
#65735=CARTESIAN_POINT ( 'NONE',  ( 280.0000000000000000, -53.81370849898476649, -20.00000000000000000 ) ) ;
#65743=DIRECTION ( 'NONE',  ( 0.000000000000000000, 0.000000000000000000, 1.000000000000000000 ) ) ;
#65755=LINE ( 'NONE', #49500, #24436 ) ;
#65769=DIRECTION ( 'NONE',  ( 0.000000000000000000, -1.000000000000000000, 0.000000000000000000 ) ) ;
#65778=SURFACE_SIDE_STYLE ('',( #59093 ) ) ;
#65808=VERTEX_POINT ( 'NONE', #51174 ) ;
#65810=CARTESIAN_POINT ( 'NONE',  ( 283.0000000000000568, -38.64999999999999858, -15.00000000000000000 ) ) ;
#65823=LINE ( 'NONE', #98, #58202 ) ;
#65844=LINE ( 'NONE', #8173, #51677 ) ;
#65885=ORIENTED_EDGE ( 'NONE', *, *, #63584, .F. ) ;
#65887=CARTESIAN_POINT ( 'NONE',  ( 283.0000000000000568, -23.65000000000000568, -12.40000000000000213 ) ) ;
#65896=DIRECTION ( 'NONE',  ( 0.000000000000000000, 0.000000000000000000, 1.000000000000000000 ) ) ;
#65898=DIRECTION ( 'NONE',  ( 0.000000000000000000, 0.6801302850037830305, 0.7330912599538155217 ) ) ;
#65906=ORIENTED_EDGE ( 'NONE', *, *, #6019, .F. ) ;
#65937=CYLINDRICAL_SURFACE ( 'NONE', #9898, 3.999999999999993339 ) ;
#65940=ADVANCED_FACE ( 'NONE', ( #48330 ), #15108, .T. ) ;
#65974=EDGE_LOOP ( 'NONE', ( #21387, #56827, #52586, #32052, #33479, #43464 ) ) ;
#65978=DIRECTION ( 'NONE',  ( -1.000000000000000000, 0.000000000000000000, 0.000000000000000000 ) ) ;
#65979=VERTEX_POINT ( 'NONE', #34122 ) ;
#65980=VECTOR ( 'NONE', #10250, 1000.000000000000000 ) ;
#65981=EDGE_LOOP ( 'NONE', ( #49479, #18868, #44333, #11785, #49738, #55571 ) ) ;
#66008=CYLINDRICAL_SURFACE ( 'NONE', #56156, 5.000000000000000000 ) ;
#66022=DIRECTION ( 'NONE',  ( 0.000000000000000000, 0.000000000000000000, -1.000000000000000000 ) ) ;
#66035=ORIENTED_EDGE ( 'NONE', *, *, #31068, .T. ) ;
#66036=PLANE ( 'NONE',  #47000 ) ;
#66048=EDGE_LOOP ( 'NONE', ( #68018, #37378, #36316, #6800 ) ) ;
#66065=VERTEX_POINT ( 'NONE', #45083 ) ;
#66088=DIRECTION ( 'NONE',  ( 0.000000000000000000, 0.7840980155806945850, 0.6206370130458033207 ) ) ;
#66105=VECTOR ( 'NONE', #36686, 1000.000000000000000 ) ;
#66106=CIRCLE ( 'NONE', #62678, 5.000000000000000000 ) ;
#66110=EDGE_CURVE ( 'NONE', #13089, #16097, #17353, .T. ) ;
#66116=CYLINDRICAL_SURFACE ( 'NONE', #41363, 0.5000000000023475666 ) ;
#66121=VERTEX_POINT ( 'NONE', #46139 ) ;
#66122=VECTOR ( 'NONE', #47872, 1000.000000000000000 ) ;
#66123=CARTESIAN_POINT ( 'NONE',  ( 283.0000000000000568, -31.30000000000000071, -12.69999999999999929 ) ) ;
#66137=CARTESIAN_POINT ( 'NONE',  ( 283.0000000000000568, -42.50000000000000000, -15.10000000000000142 ) ) ;
#66148=FACE_OUTER_BOUND ( 'NONE', #18515, .T. ) ;
#66149=VERTEX_POINT ( 'NONE', #34823 ) ;
#66179=EDGE_CURVE ( 'NONE', #35695, #45355, #3019, .T. ) ;
#66181=EDGE_CURVE ( 'NONE', #17331, #34291, #44391, .T. ) ;
#66183=EDGE_CURVE ( 'NONE', #37466, #41057, #56746, .T. ) ;
#66193=CARTESIAN_POINT ( 'NONE',  ( 7.500000000000000000, -53.81370849898476649, 20.00000000000000000 ) ) ;
#66222=VECTOR ( 'NONE', #8963, 1000.000000000000114 ) ;
#66227=ORIENTED_EDGE ( 'NONE', *, *, #24610, .F. ) ;
#66232=DIRECTION ( 'NONE',  ( 0.000000000000000000, 0.000000000000000000, -1.000000000000000000 ) ) ;
#66259=EDGE_CURVE ( 'NONE', #13174, #68211, #9439, .T. ) ;
#66290=VERTEX_POINT ( 'NONE', #63814 ) ;
#66297=DIRECTION ( 'NONE',  ( 0.000000000000000000, -0.7071067811865470176, -0.7071067811865480168 ) ) ;
#66298=CARTESIAN_POINT ( 'NONE',  ( 290.0000000000000000, 0.000000000000000000, -26.50000000000000000 ) ) ;
#66318=AXIS2_PLACEMENT_3D ( 'NONE', #16952, #65394, #33203 ) ;
#66319=CARTESIAN_POINT ( 'NONE',  ( 280.0000000000000000, -25.50000000000000355, -20.00000000000000000 ) ) ;
#66335=DIRECTION ( 'NONE',  ( -0.5773502691896175154, 0.5773502691896339467, -0.5773502691896257311 ) ) ;
#66336=ORIENTED_EDGE ( 'NONE', *, *, #32695, .T. ) ;
#66337=ORIENTED_EDGE ( 'NONE', *, *, #52517, .T. ) ;
#66349=CIRCLE ( 'NONE', #44891, 0.5000000000009302559 ) ;
#66378=LINE ( 'NONE', #33152, #56931 ) ;
#66419=ORIENTED_EDGE ( 'NONE', *, *, #32695, .F. ) ;
#66421=CARTESIAN_POINT ( 'NONE',  ( 283.0000000000000568, -40.30000000000000426, 12.20000000000000107 ) ) ;
#66422=DIRECTION ( 'NONE',  ( 0.000000000000000000, 0.5017180897718492849, 0.8650311892618014475 ) ) ;
#66434=CARTESIAN_POINT ( 'NONE',  ( 0.000000000000000000, -42.50000000000000000, 26.50000000000000000 ) ) ;
#66436=DIRECTION ( 'NONE',  ( 0.000000000000000000, 0.000000000000000000, 1.000000000000000000 ) ) ;
#66447=PLANE ( 'NONE',  #49743 ) ;
#66479=LINE ( 'NONE', #2471, #63750 ) ;
#66482=FACE_OUTER_BOUND ( 'NONE', #35014, .T. ) ;
#66485=ORIENTED_EDGE ( 'NONE', *, *, #64436, .T. ) ;
#66496=EDGE_LOOP ( 'NONE', ( #59923, #61980, #22851, #67483 ) ) ;
#66498=PLANE ( 'NONE',  #56921 ) ;
#66528=ORIENTED_EDGE ( 'NONE', *, *, #69921, .T. ) ;
#66540=CARTESIAN_POINT ( 'NONE',  ( 275.0000000000000000, -31.30000000000045191, 8.900000000000430234 ) ) ;
#66542=CARTESIAN_POINT ( 'NONE',  ( 280.0000000000000000, -20.49999999999999645, 20.00000000000000000 ) ) ;
#66558=CARTESIAN_POINT ( 'NONE',  ( 283.0000000000000568, -25.60000000000000142, 15.10000000000000142 ) ) ;
#66565=ADVANCED_FACE ( 'NONE', ( #3273 ), #61253, .T. ) ;
#66572=DIRECTION ( 'NONE',  ( 0.000000000000000000, -0.8650311892618017806, -0.5017180897718488408 ) ) ;
#66589=DIRECTION ( 'NONE',  ( 0.000000000000000000, 0.000000000000000000, 1.000000000000000000 ) ) ;
#66605=AXIS2_PLACEMENT_3D ( 'NONE', #9071, #4131, #25701 ) ;
#66609=VERTEX_POINT ( 'NONE', #14940 ) ;
#66619=FACE_OUTER_BOUND ( 'NONE', #59794, .T. ) ;
#66632=DIRECTION ( 'NONE',  ( -1.000000000000000000, 0.000000000000000000, 0.000000000000000000 ) ) ;
#66661=LINE ( 'NONE', #29172, #6840 ) ;
#66675=CARTESIAN_POINT ( 'NONE',  ( 289.7500000000001705, -42.24999999999996447, -26.75000000000008527 ) ) ;
#66690=DIRECTION ( 'NONE',  ( 0.000000000000000000, -0.7066873191085842887, -0.7075259945833242137 ) ) ;
#66692=ORIENTED_EDGE ( 'NONE', *, *, #60739, .F. ) ;
#66700=ADVANCED_FACE ( 'NONE', ( #64095 ), #52791, .F. ) ;
#66705=DIRECTION ( 'NONE',  ( -1.000000000000000000, 0.000000000000000000, 0.000000000000000000 ) ) ;
#66707=VECTOR ( 'NONE', #33709, 1000.000000000000000 ) ;
#66709=FACE_OUTER_BOUND ( 'NONE', #28564, .T. ) ;
#66755=ORIENTED_EDGE ( 'NONE', *, *, #68038, .F. ) ;
#66770=CYLINDRICAL_SURFACE ( 'NONE', #9589, 4.000000000000000000 ) ;
#66777=CARTESIAN_POINT ( 'NONE',  ( 275.0000000000000000, -23.50007830495750127, -12.28007262201345995 ) ) ;
#66792=VERTEX_POINT ( 'NONE', #27631 ) ;
#66816=PLANE ( 'NONE',  #54924 ) ;
#66834=DIRECTION ( 'NONE',  ( 0.000000000000000000, 0.000000000000000000, 1.000000000000000000 ) ) ;
#66845=VECTOR ( 'NONE', #65483, 1000.000000000000000 ) ;
#66851=ORIENTED_EDGE ( 'NONE', *, *, #59944, .T. ) ;
#66856=LINE ( 'NONE', #45634, #28178 ) ;
#66875=FACE_OUTER_BOUND ( 'NONE', #58096, .T. ) ;
#66878=LINE ( 'NONE', #25162, #65140 ) ;
#66882=CARTESIAN_POINT ( 'NONE',  ( 14.50000000000000000, -42.50000000000000000, -15.10000000000000142 ) ) ;
#66891=LINE ( 'NONE', #55947, #7649 ) ;
#66906=ADVANCED_FACE ( 'NONE', ( #51273 ), #18046, .F. ) ;
#66912=DIRECTION ( 'NONE',  ( 0.000000000000000000, 0.000000000000000000, -1.000000000000000000 ) ) ;
#66914=ORIENTED_EDGE ( 'NONE', *, *, #18813, .F. ) ;
#66918=DIRECTION ( 'NONE',  ( 0.000000000000000000, 0.000000000000000000, -1.000000000000000000 ) ) ;
#66924=EDGE_CURVE ( 'NONE', #42177, #135, #23056, .T. ) ;
#66932=VECTOR ( 'NONE', #54596, 1000.000000000000000 ) ;
#66936=ORIENTED_EDGE ( 'NONE', *, *, #50688, .T. ) ;
#66951=EDGE_CURVE ( 'NONE', #31022, #48227, #14142, .T. ) ;
#66998=DIRECTION ( 'NONE',  ( -1.000000000000000000, 0.000000000000000000, 0.000000000000000000 ) ) ;
#67004=DIRECTION ( 'NONE',  ( 1.000000000000000000, -0.000000000000000000, -0.000000000000000000 ) ) ;
#67006=EDGE_CURVE ( 'NONE', #19038, #1462, #33317, .T. ) ;
#67012=VECTOR ( 'NONE', #8493, 1000.000000000000000 ) ;
#67032=FACE_OUTER_BOUND ( 'NONE', #5067, .T. ) ;
#67044=VERTEX_POINT ( 'NONE', #53738 ) ;
#67061=ORIENTED_EDGE ( 'NONE', *, *, #6291, .T. ) ;
#67069=DIRECTION ( 'NONE',  ( 0.5773502691896270633, -0.5773502691896270633, -0.5773502691896230665 ) ) ;
#67070=EDGE_LOOP ( 'NONE', ( #49346, #3046, #49967, #46188 ) ) ;
#67074=DIRECTION ( 'NONE',  ( 1.000000000000000000, 0.000000000000000000, 0.000000000000000000 ) ) ;
#67076=DIRECTION ( 'NONE',  ( 0.000000000000000000, 1.000000000000000000, 0.000000000000000000 ) ) ;
#67078=CARTESIAN_POINT ( 'NONE',  ( 283.0000000000000568, -42.50000000000000000, 9.700000000000002842 ) ) ;
#67083=LINE ( 'NONE', #56476, #53781 ) ;
#67084=DIRECTION ( 'NONE',  ( 0.000000000000000000, 1.000000000000000000, 0.000000000000000000 ) ) ;
#67091=ORIENTED_EDGE ( 'NONE', *, *, #13294, .T. ) ;
#67094=AXIS2_PLACEMENT_3D ( 'NONE', #32326, #6140, #33360 ) ;
#67121=DIRECTION ( 'NONE',  ( 0.000000000000000000, -0.7071067811865077157, 0.7071067811865873187 ) ) ;
#67128=EDGE_CURVE ( 'NONE', #67348, #42310, #55121, .T. ) ;
#67139=ADVANCED_FACE ( 'NONE', ( #65385 ), #27216, .F. ) ;
#67158=CARTESIAN_POINT ( 'NONE',  ( 7.000000000000000000, -32.95000000000000284, 14.50000000000000000 ) ) ;
#67162=AXIS2_PLACEMENT_3D ( 'NONE', #55857, #17001, #61490 ) ;
#67165=FACE_OUTER_BOUND ( 'NONE', #44042, .T. ) ;
#67170=FACE_OUTER_BOUND ( 'NONE', #876, .T. ) ;
#67181=ORIENTED_EDGE ( 'NONE', *, *, #12211, .F. ) ;
#67182=EDGE_CURVE ( 'NONE', #18617, #63002, #16240, .T. ) ;
#67209=AXIS2_PLACEMENT_3D ( 'NONE', #69642, #21201, #54073 ) ;
#67211=VECTOR ( 'NONE', #62791, 1000.000000000000000 ) ;
#67219=VECTOR ( 'NONE', #52263, 1000.000000000000114 ) ;
#67220=VECTOR ( 'NONE', #41108, 1000.000000000000000 ) ;
#67221=DIRECTION ( 'NONE',  ( 0.000000000000000000, -0.6875000000000001110, -0.7261843774138906360 ) ) ;
#67225=CARTESIAN_POINT ( 'NONE',  ( 289.7500000000000000, -42.25000000000000711, -26.75000000000000711 ) ) ;
#67235=DIRECTION ( 'NONE',  ( 0.000000000000000000, 1.000000000000000000, 0.000000000000000000 ) ) ;
#67242=CARTESIAN_POINT ( 'NONE',  ( 283.0000000000000568, -42.00000000000000000, 7.000000000000000000 ) ) ;
#67252=ADVANCED_BREP_SHAPE_REPRESENTATION ( '', ( #20363, #45918 ), #825 ) ;
#67263=DIRECTION ( 'NONE',  ( 0.000000000000000000, 1.000000000000000000, 0.000000000000000000 ) ) ;
#67265=VECTOR ( 'NONE', #46486, 1000.000000000000000 ) ;
#67272=CARTESIAN_POINT ( 'NONE',  ( 7.000000000000000000, -38.15000000000000568, -13.19999999999999929 ) ) ;
#67288=ORIENTED_EDGE ( 'NONE', *, *, #62428, .T. ) ;
#67289=PRODUCT ( 'LINEAR ACTUATOR', 'LINEAR ACTUATOR', '', ( #57916 ) ) ;
#67325=VECTOR ( 'NONE', #51769, 1000.000000000000114 ) ;
#67330=CARTESIAN_POINT ( 'NONE',  ( 7.000000000000000000, -20.40000000000000213, -12.40000000000000213 ) ) ;
#67335=AXIS2_PLACEMENT_3D ( 'NONE', #65735, #48440, #60415 ) ;
#67338=CARTESIAN_POINT ( 'NONE',  ( 283.0000000000000568, -26.06132420600899735, 10.13999572156699891 ) ) ;
#67348=VERTEX_POINT ( 'NONE', #36592 ) ;
#67351=DIRECTION ( 'NONE',  ( 0.000000000000000000, 0.000000000000000000, -1.000000000000000000 ) ) ;
#67363=LINE ( 'NONE', #62040, #49696 ) ;
#67383=DIRECTION ( 'NONE',  ( -1.000000000000000000, 0.000000000000000000, 0.000000000000000000 ) ) ;
#67398=EDGE_LOOP ( 'NONE', ( #50769, #4545, #31677, #50113, #57690 ) ) ;
#67400=EDGE_CURVE ( 'NONE', #44075, #12124, #23547, .T. ) ;
#67404=ORIENTED_EDGE ( 'NONE', *, *, #2676, .T. ) ;
#67424=AXIS2_PLACEMENT_3D ( 'NONE', #2564, #66572, #46054 ) ;
#67426=CARTESIAN_POINT ( 'NONE',  ( 7.000000000000000000, -30.80000000000000071, -8.900000000000000355 ) ) ;
#67443=ADVANCED_FACE ( 'NONE', ( #6523 ), #6161, .F. ) ;
#67448=CARTESIAN_POINT ( 'NONE',  ( 283.0000000000000568, -26.06128899128900045, -10.14003097807800025 ) ) ;
#67468=CIRCLE ( 'NONE', #18908, 0.2999999999994937827 ) ;
#67474=FACE_OUTER_BOUND ( 'NONE', #15751, .T. ) ;
#67481=DIRECTION ( 'NONE',  ( -1.000000000000000000, 0.000000000000000000, 0.000000000000000000 ) ) ;
#67483=ORIENTED_EDGE ( 'NONE', *, *, #32813, .T. ) ;
#67484=CARTESIAN_POINT ( 'NONE',  ( 283.0000000000000568, -32.95000000000000284, -14.50000000000000000 ) ) ;
#67486=VECTOR ( 'NONE', #65978, 1000.000000000000000 ) ;
#67499=CARTESIAN_POINT ( 'NONE',  ( 7.000000000000000000, -32.46196062927499781, -8.091291340630698770 ) ) ;
#67506=LINE ( 'NONE', #68191, #28961 ) ;
#67518=ORIENTED_EDGE ( 'NONE', *, *, #19800, .F. ) ;
#67531=DIRECTION ( 'NONE',  ( -1.000000000000000000, 0.000000000000000000, 0.000000000000000000 ) ) ;
#67535=VERTEX_POINT ( 'NONE', #50672 ) ;
#67542=EDGE_CURVE ( 'NONE', #30661, #22096, #66106, .T. ) ;
#67548=DIRECTION ( 'NONE',  ( -0.5773502691896230665, -0.5773502691896271743, 0.5773502691896271743 ) ) ;
#67550=EDGE_CURVE ( 'NONE', #57368, #13785, #46762, .T. ) ;
#67555=ORIENTED_EDGE ( 'NONE', *, *, #24124, .F. ) ;
#67576=LINE ( 'NONE', #56947, #42014 ) ;
#67587=ORIENTED_EDGE ( 'NONE', *, *, #69644, .T. ) ;
#67595=EDGE_CURVE ( 'NONE', #26444, #59688, #57025, .T. ) ;
#67598=CARTESIAN_POINT ( 'NONE',  ( 15.00000000000000000, -26.28355339059299922, 9.766446609406699508 ) ) ;
#67604=ORIENTED_EDGE ( 'NONE', *, *, #64402, .F. ) ;
#67620=ORIENTED_EDGE ( 'NONE', *, *, #30980, .T. ) ;
#67630=DIRECTION ( 'NONE',  ( 1.000000000000000000, -0.000000000000000000, -0.000000000000000000 ) ) ;
#67651=CARTESIAN_POINT ( 'NONE',  ( 15.00000000000000000, -25.60000000000000142, 17.60000000000000142 ) ) ;
#67653=CARTESIAN_POINT ( 'NONE',  ( 1.000000000000000000, -21.00000000000000000, 4.000000000000000000 ) ) ;
#67661=ORIENTED_EDGE ( 'NONE', *, *, #36016, .F. ) ;
#67671=CARTESIAN_POINT ( 'NONE',  ( 289.5000000000000000, 0.000000000000000000, 26.50000000000000000 ) ) ;
#67730=VECTOR ( 'NONE', #47449, 1000.000000000000114 ) ;
#67741=DIRECTION ( 'NONE',  ( 0.000000000000000000, 0.000000000000000000, -1.000000000000000000 ) ) ;
#67744=CARTESIAN_POINT ( 'NONE',  ( 275.0000000000000000, -38.09999999999885034, 7.900000000002049383 ) ) ;
#67759=CARTESIAN_POINT ( 'NONE',  ( 290.0000000000000000, -0.5000000000000000000, -26.50000000000000000 ) ) ;
#67762=CARTESIAN_POINT ( 'NONE',  ( 0.2499999999999975020, -42.25000000000000000, 26.75000000000000000 ) ) ;
#67774=FACE_OUTER_BOUND ( 'NONE', #55738, .T. ) ;
#67780=EDGE_CURVE ( 'NONE', #39731, #24136, #90, .T. ) ;
#67794=CARTESIAN_POINT ( 'NONE',  ( 7.000000000000000000, -38.15000000000000568, 14.50000000000000000 ) ) ;
#67812=CARTESIAN_POINT ( 'NONE',  ( 275.0000000000000000, -42.50000000000000000, 7.500000000000000000 ) ) ;
#67829=EDGE_LOOP ( 'NONE', ( #55256, #13962, #31554, #12502 ) ) ;
#67843=EDGE_CURVE ( 'NONE', #36514, #22100, #55966, .T. ) ;
#67864=CARTESIAN_POINT ( 'NONE',  ( 0.5000000000000000000, 0.000000000000000000, 26.50000000000000000 ) ) ;
#67873=DIRECTION ( 'NONE',  ( -1.000000000000000000, 0.000000000000000000, 0.000000000000000000 ) ) ;
#67878=CARTESIAN_POINT ( 'NONE',  ( 283.0000000000000568, -37.14999999999894698, -8.200000000002349410 ) ) ;
#67918=DIRECTION ( 'NONE',  ( 0.000000000000000000, 0.000000000000000000, -1.000000000000000000 ) ) ;
#67969=FACE_OUTER_BOUND ( 'NONE', #68797, .T. ) ;
#67974=PLANE ( 'NONE',  #51624 ) ;
#67979=DIRECTION ( 'NONE',  ( 0.000000000000000000, 0.000000000000000000, -1.000000000000000000 ) ) ;
#67984=VERTEX_POINT ( 'NONE', #31140 ) ;
#68008=DIRECTION ( 'NONE',  ( 0.000000000000000000, -0.9239212585478484563, -0.3825826812642726948 ) ) ;
#68017=DIRECTION ( 'NONE',  ( 0.000000000000000000, 0.000000000000000000, -1.000000000000000000 ) ) ;
#68018=ORIENTED_EDGE ( 'NONE', *, *, #55150, .T. ) ;
#68019=ORIENTED_EDGE ( 'NONE', *, *, #11342, .T. ) ;
#68020=FACE_OUTER_BOUND ( 'NONE', #28345, .T. ) ;
#68022=DIRECTION ( 'NONE',  ( 0.000000000000000000, 1.000000000000000000, 0.000000000000000000 ) ) ;
#68038=EDGE_CURVE ( 'NONE', #66121, #26706, #20868, .T. ) ;
#68039=EDGE_LOOP ( 'NONE', ( #55059, #68726, #3976, #13440 ) ) ;
#68043=VECTOR ( 'NONE', #7854, 1000.000000000000000 ) ;
#68055=CYLINDRICAL_SURFACE ( 'NONE', #44779, 0.3000000000005393908 ) ;
#68074=ORIENTED_EDGE ( 'NONE', *, *, #45765, .T. ) ;
#68084=VERTEX_POINT ( 'NONE', #63307 ) ;
#68091=ORIENTED_EDGE ( 'NONE', *, *, #7230, .F. ) ;
#68105=CIRCLE ( 'NONE', #34212, 0.5000000000009320322 ) ;
#68106=CARTESIAN_POINT ( 'NONE',  ( 283.0000000000000568, -26.06132420600899735, 10.13999572156699891 ) ) ;
#68119=ADVANCED_FACE ( 'NONE', ( #19803 ), #4959, .T. ) ;
#68136=CIRCLE ( 'NONE', #39898, 0.5000000000009302559 ) ;
#68138=CARTESIAN_POINT ( 'NONE',  ( 275.0000000000000000, -41.99999999999906208, 14.49999999999903899 ) ) ;
#68180=VECTOR ( 'NONE', #20050, 1000.000000000000000 ) ;
#68191=CARTESIAN_POINT ( 'NONE',  ( 283.0000000000000568, -20.40000000000000213, 12.40000000000000213 ) ) ;
#68210=EDGE_CURVE ( 'NONE', #56785, #53395, #38191, .T. ) ;
#68211=VERTEX_POINT ( 'NONE', #37833 ) ;
#68219=CYLINDRICAL_SURFACE ( 'NONE', #10410, 0.5000000000023396840 ) ;
#68223=ADVANCED_FACE ( 'NONE', ( #65397 ), #5997, .T. ) ;
#68231=VECTOR ( 'NONE', #22006, 1000.000000000000000 ) ;
#68240=EDGE_CURVE ( 'NONE', #9842, #20615, #27559, .T. ) ;
#68242=VECTOR ( 'NONE', #60412, 1000.000000000000000 ) ;
#68243=CARTESIAN_POINT ( 'NONE',  ( 15.00000000000000000, -21.00000000000000000, 8.000000000000000000 ) ) ;
#68248=EDGE_CURVE ( 'NONE', #12315, #44134, #49482, .T. ) ;
#68249=ORIENTED_EDGE ( 'NONE', *, *, #57163, .F. ) ;
#68268=VERTEX_POINT ( 'NONE', #64696 ) ;
#68281=LINE ( 'NONE', #19484, #56497 ) ;
#68289=ORIENTED_EDGE ( 'NONE', *, *, #67128, .T. ) ;
#68300=VERTEX_POINT ( 'NONE', #19372 ) ;
#68307=DIRECTION ( 'NONE',  ( 1.000000000000000000, 0.000000000000000000, 0.000000000000000000 ) ) ;
#68322=CARTESIAN_POINT ( 'NONE',  ( 275.0000000000000000, -30.45000000000000639, 15.00000000000000000 ) ) ;
#68357=CIRCLE ( 'NONE', #37880, 0.5000000000009302559 ) ;
#68361=VERTEX_POINT ( 'NONE', #67484 ) ;
#68369=DIRECTION ( 'NONE',  ( 0.000000000000000000, 0.000000000000000000, 1.000000000000000000 ) ) ;
#68375=DIRECTION ( 'NONE',  ( 0.000000000000000000, -0.7066873191084664940, 0.7075259945834416753 ) ) ;
#68405=CARTESIAN_POINT ( 'NONE',  ( 0.000000000000000000, -0.5000000000000000000, 26.50000000000000000 ) ) ;
#68409=FACE_OUTER_BOUND ( 'NONE', #66048, .T. ) ;
#68422=DIRECTION ( 'NONE',  ( 1.000000000000000000, -0.000000000000000000, -0.000000000000000000 ) ) ;
#68423=CARTESIAN_POINT ( 'NONE',  ( 7.000000000000000000, -23.29603921945599865, 12.50000000000000000 ) ) ;
#68431=EDGE_CURVE ( 'NONE', #16805, #33051, #58268, .T. ) ;
#68443=EDGE_CURVE ( 'NONE', #57359, #9842, #52261, .T. ) ;
#68463=ORIENTED_EDGE ( 'NONE', *, *, #54907, .T. ) ;
#68469=FACE_OUTER_BOUND ( 'NONE', #45900, .T. ) ;
#68480=EDGE_CURVE ( 'NONE', #21570, #54832, #56067, .T. ) ;
#68511=ORIENTED_EDGE ( 'NONE', *, *, #7773, .T. ) ;
#68520=VERTEX_POINT ( 'NONE', #68875 ) ;
#68548=VERTEX_POINT ( 'NONE', #11888 ) ;
#68579=FACE_OUTER_BOUND ( 'NONE', #55601, .T. ) ;
#68584=DIRECTION ( 'NONE',  ( 1.000000000000000000, -0.000000000000000000, -0.000000000000000000 ) ) ;
#68591=EDGE_CURVE ( 'NONE', #40253, #19785, #69915, .T. ) ;
#68601=FACE_OUTER_BOUND ( 'NONE', #46669, .T. ) ;
#68624=ORIENTED_EDGE ( 'NONE', *, *, #59511, .T. ) ;
#68641=VECTOR ( 'NONE', #49883, 1000.000000000000000 ) ;
#68644=EDGE_CURVE ( 'NONE', #32305, #15923, #10868, .T. ) ;
#68645=CARTESIAN_POINT ( 'NONE',  ( 283.0000000000000568, -27.13000000000000611, 13.50000000000000000 ) ) ;
#68646=CIRCLE ( 'NONE', #56217, 4.000000000000000000 ) ;
#68659=ORIENTED_EDGE ( 'NONE', *, *, #39218, .F. ) ;
#68663=ORIENTED_EDGE ( 'NONE', *, *, #39762, .T. ) ;
#68726=ORIENTED_EDGE ( 'NONE', *, *, #7123, .F. ) ;
#68741=ORIENTED_EDGE ( 'NONE', *, *, #40898, .F. ) ;
#68752=ADVANCED_FACE ( 'NONE', ( #67032 ), #7278, .T. ) ;
#68758=DIRECTION ( 'NONE',  ( 0.000000000000000000, -1.000000000000000000, 0.000000000000000000 ) ) ;
#68797=EDGE_LOOP ( 'NONE', ( #62512, #42944, #5029, #179 ) ) ;
#68809=CARTESIAN_POINT ( 'NONE',  ( 275.0000000000000000, -28.94999999999999929, -13.50000000000000000 ) ) ;
#68836=VECTOR ( 'NONE', #41724, 1000.000000000000000 ) ;
#68846=FACE_OUTER_BOUND ( 'NONE', #9310, .T. ) ;
#68860=AXIS2_PLACEMENT_3D ( 'NONE', #51064, #41856, #36198 ) ;
#68861=DIRECTION ( 'NONE',  ( 0.000000000000000000, 0.7071067811865470176, -0.7071067811865480168 ) ) ;
#68862=ORIENTED_EDGE ( 'NONE', *, *, #48380, .T. ) ;
#68875=CARTESIAN_POINT ( 'NONE',  ( 283.0000000000000568, -28.94999999999999929, -13.50000000000000000 ) ) ;
#68877=FACE_OUTER_BOUND ( 'NONE', #19875, .T. ) ;
#68879=ORIENTED_EDGE ( 'NONE', *, *, #58976, .F. ) ;
#68902=ORIENTED_EDGE ( 'NONE', *, *, #1244, .F. ) ;
#68906=EDGE_LOOP ( 'NONE', ( #33799, #29483 ) ) ;
#68911=VECTOR ( 'NONE', #69138, 1000.000000000000000 ) ;
#68947=AXIS2_PLACEMENT_3D ( 'NONE', #64179, #9005, #14331 ) ;
#68948=CARTESIAN_POINT ( 'NONE',  ( 0.000000000000000000, -42.00000000000000000, 26.50000000000000000 ) ) ;
#68956=CARTESIAN_POINT ( 'NONE',  ( 290.0000000000000000, -21.00000000000000000, 0.000000000000000000 ) ) ;
#68974=CARTESIAN_POINT ( 'NONE',  ( 15.00000000000000000, -21.00000000000000000, -8.000000000000000000 ) ) ;
#68989=AXIS2_PLACEMENT_3D ( 'NONE', #29682, #51253, #30043 ) ;
#68994=AXIS2_PLACEMENT_3D ( 'NONE', #55468, #39871, #7701 ) ;
#68997=ORIENTED_EDGE ( 'NONE', *, *, #26721, .F. ) ;
#69006=EDGE_CURVE ( 'NONE', #24136, #13736, #46675, .T. ) ;
#69025=DIRECTION ( 'NONE',  ( 0.000000000000000000, 0.000000000000000000, -1.000000000000000000 ) ) ;
#69043=ORIENTED_EDGE ( 'NONE', *, *, #59324, .T. ) ;
#69045=CIRCLE ( 'NONE', #59997, 0.5000000000023507862 ) ;
#69057=ORIENTED_EDGE ( 'NONE', *, *, #62654, .F. ) ;
#69064=VERTEX_POINT ( 'NONE', #43466 ) ;
#69067=CIRCLE ( 'NONE', #9263, 0.2500000000000002220 ) ;
#69089=PLANE ( 'NONE',  #46023 ) ;
#69100=EDGE_CURVE ( 'NONE', #43188, #23628, #53058, .T. ) ;
#69109=ORIENTED_EDGE ( 'NONE', *, *, #30980, .F. ) ;
#69116=VERTEX_POINT ( 'NONE', #52712 ) ;
#69122=VERTEX_POINT ( 'NONE', #53747 ) ;
#69126=ORIENTED_EDGE ( 'NONE', *, *, #33846, .T. ) ;
#69128=EDGE_CURVE ( 'NONE', #49901, #30525, #5319, .T. ) ;
#69132=EDGE_CURVE ( 'NONE', #53553, #61056, #60661, .T. ) ;
#69134=CARTESIAN_POINT ( 'NONE',  ( 0.2500000000000105471, -42.24999999999999289, 26.74999999999999289 ) ) ;
#69138=DIRECTION ( 'NONE',  ( 0.000000000000000000, -1.000000000000000000, 0.000000000000000000 ) ) ;
#69147=EDGE_CURVE ( 'NONE', #38091, #62476, #64021, .T. ) ;
#69164=EDGE_CURVE ( 'NONE', #1040, #22191, #49812, .T. ) ;
#69177=DIRECTION ( 'NONE',  ( 0.7071067811865474617, 0.000000000000000000, -0.7071067811865474617 ) ) ;
#69182=EDGE_CURVE ( 'NONE', #1141, #22560, #11285, .T. ) ;
#69187=PLANE ( 'NONE',  #45913 ) ;
#69199=CARTESIAN_POINT ( 'NONE',  ( 7.000000000000000000, -25.60000000000000142, 16.03137303340311348 ) ) ;
#69221=CARTESIAN_POINT ( 'NONE',  ( 276.8775010008008053, -25.00000000000000000, -17.50000000000000000 ) ) ;
#69224=ADVANCED_FACE ( 'NONE', ( #33882 ), #39534, .F. ) ;
#69226=ORIENTED_EDGE ( 'NONE', *, *, #46389, .T. ) ;
#69253=VERTEX_POINT ( 'NONE', #60410 ) ;
#69279=CARTESIAN_POINT ( 'NONE',  ( 7.000000000000000000, -28.94999999999999929, -13.50000000000000000 ) ) ;
#69294=ORIENTED_EDGE ( 'NONE', *, *, #56131, .F. ) ;
#69300=DIRECTION ( 'NONE',  ( 0.5773502691896230665, 0.5773502691896271743, 0.5773502691896271743 ) ) ;
#69323=DIRECTION ( 'NONE',  ( -1.000000000000000000, 0.000000000000000000, 0.000000000000000000 ) ) ;
#69329=ORIENTED_EDGE ( 'NONE', *, *, #2176, .T. ) ;
#69338=PLANE ( 'NONE',  #32939 ) ;
#69348=FACE_OUTER_BOUND ( 'NONE', #21545, .T. ) ;
#69356=VECTOR ( 'NONE', #55137, 1000.000000000000000 ) ;
#69369=DIRECTION ( 'NONE',  ( 0.000000000000000000, 1.000000000000000000, 0.000000000000000000 ) ) ;
#69394=PLANE ( 'NONE',  #31114 ) ;
#69440=CARTESIAN_POINT ( 'NONE',  ( 275.5000000000000000, -0.5000000000000000000, 27.00000000000000000 ) ) ;
#69444=DIRECTION ( 'NONE',  ( -1.000000000000000000, 0.000000000000000000, 0.000000000000000000 ) ) ;
#69450=CARTESIAN_POINT ( 'NONE',  ( 15.00000000000000000, -26.28355339059299922, -9.766446609406699508 ) ) ;
#69478=ADVANCED_FACE ( 'NONE', ( #9121 ), #52617, .T. ) ;
#69484=ORIENTED_EDGE ( 'NONE', *, *, #58778, .T. ) ;
#69490=ORIENTED_EDGE ( 'NONE', *, *, #2236, .F. ) ;
#69491=EDGE_LOOP ( 'NONE', ( #42798, #65135, #39868, #25356 ) ) ;
#69496=EDGE_LOOP ( 'NONE', ( #128, #68659, #25132, #27233 ) ) ;
#69497=EDGE_CURVE ( 'NONE', #21753, #39731, #10512, .T. ) ;
#69499=AXIS2_PLACEMENT_3D ( 'NONE', #28099, #58896, #59590 ) ;
#69519=DIRECTION ( 'NONE',  ( 0.000000000000000000, -0.7071067811865076047, 0.7071067811865875408 ) ) ;
#69521=LINE ( 'NONE', #4824, #1431 ) ;
#69525=ORIENTED_EDGE ( 'NONE', *, *, #61880, .T. ) ;
#69550=VECTOR ( 'NONE', #10713, 1000.000000000000114 ) ;
#69580=ORIENTED_EDGE ( 'NONE', *, *, #48835, .F. ) ;
#69584=LINE ( 'NONE', #15493, #61549 ) ;
#69591=EDGE_LOOP ( 'NONE', ( #19219, #35560, #37909, #62003 ) ) ;
#69621=CARTESIAN_POINT ( 'NONE',  ( 283.0000000000000568, -27.13000000000000611, 13.50000000000000000 ) ) ;
#69628=VERTEX_POINT ( 'NONE', #11206 ) ;
#69629=( BOUNDED_CURVE ( )  B_SPLINE_CURVE ( 3, ( #34013, #841, #43941, #18439 ),
 .UNSPECIFIED., .F., .F. ) 
 B_SPLINE_CURVE_WITH_KNOTS ( ( 4, 4 ),
 ( 0.7227342478134158865, 0.8956647938578649049 ),
 .UNSPECIFIED. ) 
 CURVE ( )  GEOMETRIC_REPRESENTATION_ITEM ( )  RATIONAL_B_SPLINE_CURVE ( ( 1.000000000000000000, 0.9975094710839674805, 0.9975094710839674805, 1.000000000000000000 ) ) 
 REPRESENTATION_ITEM ( '' )  );
#69642=CARTESIAN_POINT ( 'NONE',  ( 15.00000000000000000, -21.00000000000000000, 0.000000000000000000 ) ) ;
#69644=EDGE_CURVE ( 'NONE', #6527, #24350, #59656, .T. ) ;
#69645=CARTESIAN_POINT ( 'NONE',  ( 14.50000000000000000, -42.00000000000000000, 27.00000000000000000 ) ) ;
#69651=AXIS2_PLACEMENT_3D ( 'NONE', #9262, #68307, #51703 ) ;
#69652=ORIENTED_EDGE ( 'NONE', *, *, #65248, .T. ) ;
#69664=VERTEX_POINT ( 'NONE', #60326 ) ;
#69673=VECTOR ( 'NONE', #5699, 1000.000000000000000 ) ;
#69674=CARTESIAN_POINT ( 'NONE',  ( 10.14575131106465378, -25.50000000000000355, 17.00000000000000000 ) ) ;
#69680=VECTOR ( 'NONE', #57495, 1000.000000000000000 ) ;
#69699=CARTESIAN_POINT ( 'NONE',  ( 10.62249899919925866, -21.00000000000000000, 17.50000000000000000 ) ) ;
#69702=EDGE_LOOP ( 'NONE', ( #24782, #10137, #14369, #13380 ) ) ;
#69704=DIRECTION ( 'NONE',  ( 0.000000000000000000, -0.7071067811865475727, -0.7071067811865475727 ) ) ;
#69706=DIRECTION ( 'NONE',  ( 0.000000000000000000, 0.000000000000000000, 1.000000000000000000 ) ) ;
#69717=CARTESIAN_POINT ( 'NONE',  ( 283.0000000000000568, -38.64999999999999858, -12.69999999999999929 ) ) ;
#69725=EDGE_CURVE ( 'NONE', #43188, #34214, #38439, .T. ) ;
#69729=EDGE_CURVE ( 'NONE', #7638, #6527, #54353, .T. ) ;
#69743=DIRECTION ( 'NONE',  ( 1.000000000000000000, 0.000000000000000000, 0.000000000000000000 ) ) ;
#69774=DIRECTION ( 'NONE',  ( -1.000000000000000000, 0.000000000000000000, 0.000000000000000000 ) ) ;
#69782=VERTEX_POINT ( 'NONE', #24607 ) ;
#69790=CARTESIAN_POINT ( 'NONE',  ( 7.000000000000000000, -25.60000000000000142, -15.10000000000000142 ) ) ;
#69807=ORIENTED_EDGE ( 'NONE', *, *, #69132, .F. ) ;
#69808=CARTESIAN_POINT ( 'NONE',  ( 7.000000000000000000, -23.50007830495750127, 12.28007262201345995 ) ) ;
#69824=CIRCLE ( 'NONE', #23514, 8.000000000000000000 ) ;
#69833=CARTESIAN_POINT ( 'NONE',  ( 275.0000000000000000, -31.30000000000095284, -12.19999999999906315 ) ) ;
#69847=ORIENTED_EDGE ( 'NONE', *, *, #66924, .F. ) ;
#69878=LINE ( 'NONE', #37030, #60606 ) ;
#69879=DIRECTION ( 'NONE',  ( 1.000000000000000000, -0.000000000000000000, -0.000000000000000000 ) ) ;
#69893=EDGE_LOOP ( 'NONE', ( #26577, #16859, #12970, #14803 ) ) ;
#69904=VERTEX_POINT ( 'NONE', #24248 ) ;
#69915=LINE ( 'NONE', #48356, #10957 ) ;
#69918=DIRECTION ( 'NONE',  ( -0.000000000000000000, -1.000000000000000000, -0.000000000000000000 ) ) ;
#69921=EDGE_CURVE ( 'NONE', #10806, #31022, #57819, .T. ) ;
#69932=VERTEX_POINT ( 'NONE', #47568 ) ;
#69933=AXIS2_PLACEMENT_3D ( 'NONE', #53813, #17342, #5383 ) ;
#69944=ORIENTED_EDGE ( 'NONE', *, *, #49777, .T. ) ;
#69958=CARTESIAN_POINT ( 'NONE',  ( 283.0000000000000568, -28.94999999999999929, 13.50000000000000000 ) ) ;
#69960=EDGE_CURVE ( 'NONE', #6538, #992, #52898, .T. ) ;
ENDSEC;
END-ISO-10303-21;
